ISO-10303-21;
HEADER;
FILE_DESCRIPTION (('STEP AP214'),
    '1' );
FILE_NAME ('Valve Operating Stem.step',
    '2026-10-09T13:48:35',
    ( '' ),
    ( '' ),
    'SwSTEP 2.0',
    'SolidWorks 2026',
    '' );
FILE_SCHEMA (( 'AUTOMOTIVE_DESIGN' ));
ENDSEC;

DATA;
#5=FACE_OUTER_BOUND ( 'NONE', #6433, .T. ) ;
#8=CARTESIAN_POINT ( 'NONE',  ( -1.666640107417000083, 24.57716808515000295, 1.349687702108000043 ) ) ;
#12=CARTESIAN_POINT ( 'NONE',  ( -0.8753480283797999695, 29.83343345458000329, -2.192249794771000015 ) ) ;
#18=CARTESIAN_POINT ( 'NONE',  ( -2.277512614005948954, 24.29165256314995958, 1.108113113897667867 ) ) ;
#27=CARTESIAN_POINT ( 'NONE',  ( 1.652809762273000027, 26.39462896667000180, -2.096579189799000265 ) ) ;
#28=EDGE_CURVE ( 'NONE', #3560, #10250, #9953, .T. ) ;
#37=DIRECTION ( 'NONE',  ( 0.7071067811905932254, -0.7071067811824932603, 1.099460906822990477E-07 ) ) ;
#40=CARTESIAN_POINT ( 'NONE',  ( -1.922540451232000125, 30.13691161737000002, -1.339163193283000153 ) ) ;
#43=CARTESIAN_POINT ( 'NONE',  ( 2.033420667506555812, 29.75788411540394307, 0.7685308260835450600 ) ) ;
#45=CARTESIAN_POINT ( 'NONE',  ( 0.5694918563224000696, 25.42220128840000015, 2.110394011463000208 ) ) ;
#47=CARTESIAN_POINT ( 'NONE',  ( -0.9075693228094323661, 23.65758229563746795, -1.957493242368112840 ) ) ;
#48=ORIENTED_EDGE ( 'NONE', *, *, #10021, .F. ) ;
#52=ORIENTED_EDGE ( 'NONE', *, *, #12758, .F. ) ;
#55=CARTESIAN_POINT ( 'NONE',  ( -1.999167105995447224, 29.68333333333333357, 1.536366799937292305 ) ) ;
#63=CARTESIAN_POINT ( 'NONE',  ( 2.213005609277820529, 26.38948373505501266, -0.6062005036607733821 ) ) ;
#64=FACE_OUTER_BOUND ( 'NONE', #4786, .T. ) ;
#68=ORIENTED_EDGE ( 'NONE', *, *, #2410, .F. ) ;
#70=CARTESIAN_POINT ( 'NONE',  ( 0.5551539414043799026, 26.26248452079970619, 2.089084675604010233 ) ) ;
#73=CARTESIAN_POINT ( 'NONE',  ( 1.850881008969999852, 26.55271896306000201, 1.344743706340999934 ) ) ;
#75=CARTESIAN_POINT ( 'NONE',  ( -2.123790204974259410, 30.86901160495731133, 0.1750885401383986684 ) ) ;
#77=ORIENTED_EDGE ( 'NONE', *, *, #21426, .F. ) ;
#81=EDGE_CURVE ( 'NONE', #16646, #13895, #14967, .T. ) ;
#82=DIRECTION ( 'NONE',  ( -1.000000000000000000, 0.000000000000000000, 0.000000000000000000 ) ) ;
#84=CARTESIAN_POINT ( 'NONE',  ( 0.000000000000000000, 22.00000000000000000, -2.704938617610999654E-14 ) ) ;
#87=CARTESIAN_POINT ( 'NONE',  ( -1.259047450927242018, 29.16753006952333038, 2.184465970885648201 ) ) ;
#88=CARTESIAN_POINT ( 'NONE',  ( -1.813125266397999980, 29.53638408233999968, 1.482067624179000065 ) ) ;
#90=CARTESIAN_POINT ( 'NONE',  ( 0.8889003272348959817, 24.49999999999999289, 2.308449506161659226 ) ) ;
#91=VECTOR ( 'NONE', #21222, 1000.000000000000114 ) ;
#92=B_SPLINE_CURVE_WITH_KNOTS ( 'NONE', 3,
 ( #2075, #11646, #16720, #15021, #5828, #18780, #22295, #18555, #5709, #11170 ),
 .UNSPECIFIED., .F., .F.,
 ( 4, 2, 2, 2, 4 ),
 ( 0.000000000000000000, 0.2500000000000000000, 0.5000000000000000000, 0.7500000000000000000, 1.000000000000000000 ),
 .UNSPECIFIED. ) ;
#97=ORIENTED_EDGE ( 'NONE', *, *, #6382, .F. ) ;
#101=CARTESIAN_POINT ( 'NONE',  ( 1.956501129450092469, 29.05944223948321792, -0.9149880855959362513 ) ) ;
#102=DIRECTION ( 'NONE',  ( 0.000000000000000000, 1.000000000000000000, 0.000000000000000000 ) ) ;
#104=CARTESIAN_POINT ( 'NONE',  ( -0.8133812233904295086, 23.73829498092657531, 2.103014135165154563 ) ) ;
#105=ORIENTED_EDGE ( 'NONE', *, *, #9875, .F. ) ;
#106=CARTESIAN_POINT ( 'NONE',  ( 0.9654995472831999770, 25.19530436186999722, -2.146034520375999843 ) ) ;
#109=AXIS2_PLACEMENT_3D ( 'NONE', #17470, #8390, #618 ) ;
#111=CARTESIAN_POINT ( 'NONE',  ( 0.000000000000000000, 19.04999994433000055, -2.949999944334000368 ) ) ;
#115=DIRECTION ( 'NONE',  ( 1.000000000000000000, 0.000000000000000000, 0.000000000000000000 ) ) ;
#120=CARTESIAN_POINT ( 'NONE',  ( 2.047900492968999675, 24.12888028435000010, -0.6367493590249000412 ) ) ;
#122=CARTESIAN_POINT ( 'NONE',  ( -2.000000000000000000, 18.27087121525220681, 0.000000000000000000 ) ) ;
#124=CARTESIAN_POINT ( 'NONE',  ( 0.4673507188188000261, 29.65618993841000162, -2.509968819301999776 ) ) ;
#127=DIRECTION ( 'NONE',  ( 0.000000000000000000, 1.000000000000000000, 0.000000000000000000 ) ) ;
#130=CONICAL_SURFACE ( 'NONE', #12534, 3.049999825846000157, 0.7853981633972997312 ) ;
#133=CARTESIAN_POINT ( 'NONE',  ( 0.000000000000000000, 24.50000000000000000, 0.000000000000000000 ) ) ;
#137=CARTESIAN_POINT ( 'NONE',  ( 0.5721489135196999865, 28.05212896667000066, -2.607696352436000176 ) ) ;
#138=ORIENTED_EDGE ( 'NONE', *, *, #17688, .F. ) ;
#150=CARTESIAN_POINT ( 'NONE',  ( -0.8860051451328000427, 29.33568040543000066, 2.005734967351000098 ) ) ;
#155=CARTESIAN_POINT ( 'NONE',  ( 1.387834333747559601, 29.69250747415173919, 1.655459006554598878 ) ) ;
#157=CARTESIAN_POINT ( 'NONE',  ( -0.7494000042766999492, 23.97278996295999676, 2.212197947947999843 ) ) ;
#160=EDGE_LOOP ( 'NONE', ( #4133, #21661, #12489 ) ) ;
#161=CARTESIAN_POINT ( 'NONE',  ( 0.000000000000000000, 15.00000000000000000, 0.000000000000000000 ) ) ;
#162=CARTESIAN_POINT ( 'NONE',  ( 1.633245533205915478, 30.34494809611083710, -1.942077254787831109 ) ) ;
#166=CARTESIAN_POINT ( 'NONE',  ( 0.000000000000000000, 21.87500000000000000, 0.000000000000000000 ) ) ;
#169=ORIENTED_EDGE ( 'NONE', *, *, #6404, .T. ) ;
#176=CARTESIAN_POINT ( 'NONE',  ( 0.000000000000000000, 22.00000000000000000, 0.000000000000000000 ) ) ;
#177=AXIS2_PLACEMENT_3D ( 'NONE', #2830, #2574, #6813 ) ;
#178=DIRECTION ( 'NONE',  ( 0.000000000000000000, -1.000000000000000000, 0.000000000000000000 ) ) ;
#179=CARTESIAN_POINT ( 'NONE',  ( -2.778011591584000239, 28.82750240009999843, -0.7249434865795999494 ) ) ;
#181=CARTESIAN_POINT ( 'NONE',  ( 2.147278730106622735, 30.61751797242171591, -0.2331274669797682719 ) ) ;
#182=EDGE_LOOP ( 'NONE', ( #11413, #48, #13723 ) ) ;
#186=CARTESIAN_POINT ( 'NONE',  ( 2.048219662131999907, 28.09696440325999944, -1.368576729846999962 ) ) ;
#187=CARTESIAN_POINT ( 'NONE',  ( -2.123217625947178888, 30.87310701895514597, 0.1259251270839611692 ) ) ;
#189=ORIENTED_EDGE ( 'NONE', *, *, #3583, .F. ) ;
#190=EDGE_CURVE ( 'NONE', #10715, #2693, #6863, .T. ) ;
#192=DIRECTION ( 'NONE',  ( -0.000000000000000000, -1.000000000000000000, -0.000000000000000000 ) ) ;
#195=EDGE_CURVE ( 'NONE', #7466, #23288, #17774, .T. ) ;
#196=EDGE_CURVE ( 'NONE', #21988, #11568, #4015, .T. ) ;
#209=DIRECTION ( 'NONE',  ( -1.000000000000000000, 0.000000000000000000, 0.000000000000000000 ) ) ;
#210=ORIENTED_EDGE ( 'NONE', *, *, #15775, .T. ) ;
#214=CARTESIAN_POINT ( 'NONE',  ( -0.8255343667490313564, 29.25365081292461511, -1.996006782196166229 ) ) ;
#218=ORIENTED_EDGE ( 'NONE', *, *, #9354, .F. ) ;
#219=CARTESIAN_POINT ( 'NONE',  ( 1.782743705658000000, 25.02019945177000082, -1.221832406237000068 ) ) ;
#220=CARTESIAN_POINT ( 'NONE',  ( 2.434931691670791931, 28.36666666666666359, 0.6543697108981911814 ) ) ;
#221=FACE_OUTER_BOUND ( 'NONE', #22296, .T. ) ;
#223=CIRCLE ( 'NONE', #13763, 3.100000000000000089 ) ;
#224=CARTESIAN_POINT ( 'NONE',  ( 2.999999956181000016, 17.90000004382000043, -2.609181548331000199E-08 ) ) ;
#232=CARTESIAN_POINT ( 'NONE',  ( 0.02135780212313000137, 24.77319310863999746, -2.715970023235000141 ) ) ;
#236=CARTESIAN_POINT ( 'NONE',  ( 1.879564114486999893, 30.37427879440000211, -1.727888272304000106 ) ) ;
#244=ORIENTED_EDGE ( 'NONE', *, *, #16225, .T. ) ;
#246=ORIENTED_EDGE ( 'NONE', *, *, #14119, .T. ) ;
#248=CARTESIAN_POINT ( 'NONE',  ( 0.000000000000000000, 22.00000000000000000, -4.649999999999999467 ) ) ;
#249=CARTESIAN_POINT ( 'NONE',  ( 0.1526552725783049125, 24.50000000000000000, 2.395140156181688074 ) ) ;
#251=CARTESIAN_POINT ( 'NONE',  ( 2.950000000000001954, 24.50000000000000000, 5.832343053588036738E-08 ) ) ;
#252=CONICAL_SURFACE ( 'NONE', #13040, 1.949955127985000258, 0.7853751480324476786 ) ;
#253=CARTESIAN_POINT ( 'NONE',  ( 1.182158213329999930, 28.43419433610000269, 2.320116128650000054 ) ) ;
#254=EDGE_LOOP ( 'NONE', ( #5726, #17524, #14583, #2895 ) ) ;
#256=CARTESIAN_POINT ( 'NONE',  ( -0.3272492347489394104, 27.25086340285666253, -2.499999999999999112 ) ) ;
#265=CARTESIAN_POINT ( 'NONE',  ( 0.3255751167234999799, 29.40761742610999718, 2.168404648556000236 ) ) ;
#266=AXIS2_PLACEMENT_3D ( 'NONE', #7745, #20699, #7979 ) ;
#268=CARTESIAN_POINT ( 'NONE',  ( 1.671545104861497988, 29.71636722689019194, 1.369186538342708204 ) ) ;
#270=CARTESIAN_POINT ( 'NONE',  ( 1.582682121269000097, 25.73607590313999793, 1.501367095590999901 ) ) ;
#271=CARTESIAN_POINT ( 'NONE',  ( -2.153985071724999756, 30.83999999999999986, 0.1610847937796999751 ) ) ;
#272=DIRECTION ( 'NONE',  ( -1.000000000000000000, 0.000000000000000000, 0.000000000000000000 ) ) ;
#274=EDGE_LOOP ( 'NONE', ( #645, #2365, #19266, #5031 ) ) ;
#275=EDGE_CURVE ( 'NONE', #9922, #21280, #2869, .T. ) ;
#294=CARTESIAN_POINT ( 'NONE',  ( -9.481593150953709039E-06, 28.93474093911251899, 2.386566200631719870 ) ) ;
#295=CARTESIAN_POINT ( 'NONE',  ( -3.025523437588010012, 26.41693820796410463, -2.872015382385962656 ) ) ;
#297=CARTESIAN_POINT ( 'NONE',  ( 2.155060826509969552, 30.59516583461061145, 0.1486681260086218093 ) ) ;
#298=ORIENTED_EDGE ( 'NONE', *, *, #14807, .T. ) ;
#305=CARTESIAN_POINT ( 'NONE',  ( 2.462898805936000191, 27.21946440326000172, 0.04836512055251000058 ) ) ;
#308=CONICAL_SURFACE ( 'NONE', #4587, 4.649999883068000273, 0.7853981633972997312 ) ;
#314=EDGE_CURVE ( 'NONE', #9720, #10966, #3257, .T. ) ;
#315=CARTESIAN_POINT ( 'NONE',  ( 0.000000000000000000, 24.50000000000000000, 0.000000000000000000 ) ) ;
#319=LINE ( 'NONE', #2266, #19710 ) ;
#325=AXIS2_PLACEMENT_3D ( 'NONE', #4418, #15903, #15423 ) ;
#330=CIRCLE ( 'NONE', #15027, 4.000000000000000000 ) ;
#337=CARTESIAN_POINT ( 'NONE',  ( -2.102266727616999731, 23.66000000000000014, 0.4960590750638999569 ) ) ;
#338=AXIS2_PLACEMENT_3D ( 'NONE', #14363, #14706, #10963 ) ;
#339=ORIENTED_EDGE ( 'NONE', *, *, #9210, .F. ) ;
#341=CARTESIAN_POINT ( 'NONE',  ( -1.932944458086000017, 26.02049822780999833, -1.184521108792000010 ) ) ;
#344=CARTESIAN_POINT ( 'NONE',  ( 0.000000000000000000, 24.50000000000000000, 0.000000000000000000 ) ) ;
#348=CONICAL_SURFACE ( 'NONE', #19319, 2.949999944334000368, 0.7853981633972997312 ) ;
#349=DIRECTION ( 'NONE',  ( 1.000000000000000000, 0.000000000000000000, 0.000000000000000000 ) ) ;
#354=CARTESIAN_POINT ( 'NONE',  ( -1.610156619168000125, 25.09339868065000090, 2.187314281954999995 ) ) ;
#358=CARTESIAN_POINT ( 'NONE',  ( 2.300563072390000130, 28.75630017058999854, 0.5287386102487999784 ) ) ;
#364=ORIENTED_EDGE ( 'NONE', *, *, #3722, .T. ) ;
#365=ADVANCED_FACE ( 'NONE', ( #11334 ), #5191, .T. ) ;
#367=VERTEX_POINT ( 'NONE', #10972 ) ;
#376=DIRECTION ( 'NONE',  ( 1.000000000000000000, 0.000000000000000000, 0.000000000000000000 ) ) ;
#377=CARTESIAN_POINT ( 'NONE',  ( -1.864615697012000028, 27.26419433610000098, -2.183184479328999839 ) ) ;
#381=EDGE_CURVE ( 'NONE', #22357, #8048, #20063, .T. ) ;
#385=FACE_OUTER_BOUND ( 'NONE', #7895, .T. ) ;
#392=CARTESIAN_POINT ( 'NONE',  ( -2.192033073580000213, 29.19180636409000229, 0.05448754284059999231 ) ) ;
#394=CARTESIAN_POINT ( 'NONE',  ( 0.5586671089952324198, 29.63706544627255113, 2.086414242290000498 ) ) ;
#395=ORIENTED_EDGE ( 'NONE', *, *, #16929, .T. ) ;
#396=CARTESIAN_POINT ( 'NONE',  ( 0.3885665913385000225, 24.40991835864999970, -2.146603527457000116 ) ) ;
#397=CARTESIAN_POINT ( 'NONE',  ( -4.649999999999999467, 15.00000000000000000, 0.000000000000000000 ) ) ;
#400=CARTESIAN_POINT ( 'NONE',  ( -0.3006329639645716756, 24.53729095029033758, -2.348355141549282710 ) ) ;
#402=CARTESIAN_POINT ( 'NONE',  ( 0.000000000000000000, 19.09999999999999787, 0.000000000000000000 ) ) ;
#404=ORIENTED_EDGE ( 'NONE', *, *, #21965, .F. ) ;
#406=DIRECTION ( 'NONE',  ( 0.000000000000000000, 1.000000000000000000, 0.000000000000000000 ) ) ;
#414=ORIENTED_CLOSED_SHELL ( 'NONE', *, #20462, .F. );
#418=SURFACE_STYLE_USAGE ( .BOTH. , #3952 ) ;
#419=CARTESIAN_POINT ( 'NONE',  ( -0.6543697108982035049, 28.06753006952333962, -2.434931691670788823 ) ) ;
#420=CARTESIAN_POINT ( 'NONE',  ( 2.138730754459550631, 30.58610565302236139, 0.3009471218714359630 ) ) ;
#426=CARTESIAN_POINT ( 'NONE',  ( 2.425010641684000046, 27.99946440325999930, 0.4330518317348999724 ) ) ;
#429=CARTESIAN_POINT ( 'NONE',  ( 0.000000000000000000, 13.04999996922999905, 0.000000000000000000 ) ) ;
#430=CARTESIAN_POINT ( 'NONE',  ( -2.000000000000000000, 18.89999999999999858, -5.041390465489999878E-11 ) ) ;
#431=DIRECTION ( 'NONE',  ( 0.000000000000000000, -1.000000000000000000, 0.000000000000000000 ) ) ;
#433=ORIENTED_EDGE ( 'NONE', *, *, #18501, .F. ) ;
#436=EDGE_CURVE ( 'NONE', #17309, #8075, #16408, .T. ) ;
#437=DIRECTION ( 'NONE',  ( 1.000000000000000000, 0.000000000000000000, 0.000000000000000000 ) ) ;
#441=CARTESIAN_POINT ( 'NONE',  ( 2.500000000000000000, 29.43419673618999965, 0.000000000000000000 ) ) ;
#445=ORIENTED_EDGE ( 'NONE', *, *, #2462, .F. ) ;
#446=LINE ( 'NONE', #20929, #10787 ) ;
#447=CARTESIAN_POINT ( 'NONE',  ( -2.183184479328999839, 27.17000240009999956, -1.864615697012000028 ) ) ;
#449=CARTESIAN_POINT ( 'NONE',  ( 1.973182983453731110, 28.95032424988295361, 0.8828346089906928817 ) ) ;
#457=CARTESIAN_POINT ( 'NONE',  ( 0.5071914623445000769, 28.61256359724000120, 2.254114612530000006 ) ) ;
#464=EDGE_CURVE ( 'NONE', #9967, #1877, #3712, .T. ) ;
#466=FACE_OUTER_BOUND ( 'NONE', #8013, .T. ) ;
#467=CARTESIAN_POINT ( 'NONE',  ( -2.300703130192000234, 23.53376433680000090, 1.041687086677999918 ) ) ;
#472=CARTESIAN_POINT ( 'NONE',  ( 0.2468081092584000213, 28.97172682739000038, -2.347611320519999545 ) ) ;
#477=EDGE_CURVE ( 'NONE', #16405, #15685, #7206, .T. ) ;
#478=CARTESIAN_POINT ( 'NONE',  ( -1.259047450927251788, 29.70086340285667603, -2.184465970885643316 ) ) ;
#479=VERTEX_POINT ( 'NONE', #11804 ) ;
#480=CIRCLE ( 'NONE', #22909, 2.000000000000000000 ) ;
#484=CARTESIAN_POINT ( 'NONE',  ( -2.453480368351999896, 24.91848166633000261, 1.213420540718000096 ) ) ;
#486=CARTESIAN_POINT ( 'NONE',  ( 0.6591105980973780420, 24.04252312545441583, 2.091938566331359883 ) ) ;
#487=CARTESIAN_POINT ( 'NONE',  ( 1.640193969998194001, 24.74015355458762144, 1.405240085690787843 ) ) ;
#488=ORIENTED_EDGE ( 'NONE', *, *, #1439, .F. ) ;
#492=CARTESIAN_POINT ( 'NONE',  ( -1.955724675740084795, 26.26076676662178855, 0.9180910909140133080 ) ) ;
#504=DIRECTION ( 'NONE',  ( 0.000000000000000000, -1.000000000000000000, 0.000000000000000000 ) ) ;
#507=CARTESIAN_POINT ( 'NONE',  ( -0.7069816488115999720, 28.78845002726000146, 1.950778716412999936 ) ) ;
#508=VECTOR ( 'NONE', #15268, 1000.000000000000000 ) ;
#510=CARTESIAN_POINT ( 'NONE',  ( 0.6475450134985413220, 29.64256677160481956, 2.060670777103924767 ) ) ;
#513=CARTESIAN_POINT ( 'NONE',  ( 0.4803641815392999947, 23.81685268192000038, 2.132454625199999843 ) ) ;
#514=EDGE_CURVE ( 'NONE', #17995, #19991, #13664, .T. ) ;
#515=CARTESIAN_POINT ( 'NONE',  ( 0.000000000000000000, 26.50000000000000355, -2.399999999999955502 ) ) ;
#519=CARTESIAN_POINT ( 'NONE',  ( 0.000000000000000000, 18.00000000000000000, 0.000000000000000000 ) ) ;
#526=CARTESIAN_POINT ( 'NONE',  ( 0.000000000000000000, 18.00000000000000000, 0.000000000000000000 ) ) ;
#533=CARTESIAN_POINT ( 'NONE',  ( -3.821520914465099672, 26.24995697614779644, -2.412446024836691461 ) ) ;
#534=CARTESIAN_POINT ( 'NONE',  ( 0.000000000000000000, 26.20000000000000284, -4.618802153517000519 ) ) ;
#536=CARTESIAN_POINT ( 'NONE',  ( 0.3085936222218769731, 30.42196597467193087, 2.139114131937794205 ) ) ;
#543=CARTESIAN_POINT ( 'NONE',  ( 0.4030006639746999686, 26.21114211382000292, 2.256729627096000002 ) ) ;
#544=DIRECTION ( 'NONE',  ( 0.000000000000000000, -1.000000000000000000, 0.000000000000000000 ) ) ;
#548=CIRCLE ( 'NONE', #19927, 0.09999999999999939493 ) ;
#549=FACE_OUTER_BOUND ( 'NONE', #13999, .T. ) ;
#551=VERTEX_POINT ( 'NONE', #18822 ) ;
#557=CARTESIAN_POINT ( 'NONE',  ( -1.783084334938916715, 30.87983632939971557, -1.147531989998553215 ) ) ;
#558=DIRECTION ( 'NONE',  ( 0.000000000000000000, 1.000000000000000000, 0.000000000000000000 ) ) ;
#561=ORIENTED_EDGE ( 'NONE', *, *, #8358, .F. ) ;
#563=CARTESIAN_POINT ( 'NONE',  ( -1.394936847711000016, 28.62456776951999871, -2.276308483783000103 ) ) ;
#566=CARTESIAN_POINT ( 'NONE',  ( 0.2179091018266194058, 28.81668098355705254, 2.159923230666197291 ) ) ;
#570=EDGE_LOOP ( 'NONE', ( #6840, #10937, #15562, #10507 ) ) ;
#571=ADVANCED_FACE ( 'NONE', ( #21002 ), #130, .F. ) ;
#573=CARTESIAN_POINT ( 'NONE',  ( 2.500000000000000000, 28.40000000000000213, 0.000000000000000000 ) ) ;
#578=CIRCLE ( 'NONE', #21874, 4.625000000000000000 ) ;
#585=CARTESIAN_POINT ( 'NONE',  ( 1.924317348631999991, 23.78992879440000152, 1.635700662827000107 ) ) ;
#597=DIRECTION ( 'NONE',  ( 0.000000000000000000, -1.000000000000000000, 0.000000000000000000 ) ) ;
#600=CARTESIAN_POINT ( 'NONE',  ( 0.000000000000000000, 22.19999999999999574, 0.000000000000000000 ) ) ;
#603=CARTESIAN_POINT ( 'NONE',  ( 2.457689475042000193, 26.10287641827000016, -0.8603483806163000347 ) ) ;
#606=DIRECTION ( 'NONE',  ( 0.000000000000000000, -1.000000000000000000, 0.000000000000000000 ) ) ;
#609=CARTESIAN_POINT ( 'NONE',  ( 0.5047246425491000998, 25.99669433610000269, 2.826365205286999860 ) ) ;
#616=ADVANCED_FACE ( 'NONE', ( #13361 ), #18050, .F. ) ;
#618=DIRECTION ( 'NONE',  ( 0.8571428571428744148, 0.000000000000000000, -0.5150787536376840725 ) ) ;
#619=AXIS2_PLACEMENT_3D ( 'NONE', #16490, #18560, #23879 ) ;
#620=DIRECTION ( 'NONE',  ( 0.000000000000000000, 1.000000000000000000, 0.000000000000000000 ) ) ;
#624=DIRECTION ( 'NONE',  ( 0.000000000000000000, 1.000000000000000000, 0.000000000000000000 ) ) ;
#628=CARTESIAN_POINT ( 'NONE',  ( 0.9831177708813756411, 29.66411096424411298, 1.923123576622347120 ) ) ;
#631=CARTESIAN_POINT ( 'NONE',  ( 1.951212462256999958, 24.89714145383999622, -1.307686770928999875 ) ) ;
#633=ORIENTED_EDGE ( 'NONE', *, *, #7921, .T. ) ;
#636=CARTESIAN_POINT ( 'NONE',  ( -0.8571723963710232708, 30.47784972801583692, -2.388390780044352013 ) ) ;
#638=AXIS2_PLACEMENT_3D ( 'NONE', #10074, #6308, #11771 ) ;
#645=ORIENTED_EDGE ( 'NONE', *, *, #11625, .F. ) ;
#647=CARTESIAN_POINT ( 'NONE',  ( -2.206474594537332301, 24.66792226721002734, 0.3902536378939148176 ) ) ;
#648=CARTESIAN_POINT ( 'NONE',  ( 0.000000000000000000, 19.00000000000000000, 0.000000000000000000 ) ) ;
#655=CARTESIAN_POINT ( 'NONE',  ( -0.1784790855350541494, 26.24995697614779644, 4.515757205439222766 ) ) ;
#659=CARTESIAN_POINT ( 'NONE',  ( 0.2265999339602371709, 30.41708343718551077, 2.150008283823798383 ) ) ;
#660=ORIENTED_EDGE ( 'NONE', *, *, #21953, .T. ) ;
#664=DIRECTION ( 'NONE',  ( 0.000000000000000000, -1.000000000000000000, 0.000000000000000000 ) ) ;
#667=CARTESIAN_POINT ( 'NONE',  ( 1.525059720042999833, 26.53696440326000072, -1.934529033667000020 ) ) ;
#670=CARTESIAN_POINT ( 'NONE',  ( -3.316026328260925471, 24.63336607546987267, -2.704152903936609231 ) ) ;
#683=FACE_OUTER_BOUND ( 'NONE', #12131, .T. ) ;
#686=AXIS2_PLACEMENT_3D ( 'NONE', #14903, #16842, #9819 ) ;
#690=CARTESIAN_POINT ( 'NONE',  ( 3.999987874060709991, 24.60222989788993431, -1.328900689436832261 ) ) ;
#691=EDGE_LOOP ( 'NONE', ( #20065, #169, #1554, #10397 ) ) ;
#693=CARTESIAN_POINT ( 'NONE',  ( 2.052373795670999979, 28.32413313894999973, -1.371352433351999744 ) ) ;
#695=CARTESIAN_POINT ( 'NONE',  ( 1.836104782222518272, 28.93328551889701927, 1.137863805830989783 ) ) ;
#697=ORIENTED_EDGE ( 'NONE', *, *, #21937, .T. ) ;
#698=CARTESIAN_POINT ( 'NONE',  ( -1.600000000000000089, 9.000000000000000000, 0.000000000000000000 ) ) ;
#700=DIRECTION ( 'NONE',  ( -1.160410170730938003E-09, 2.689653288266210374E-16, -1.000000000000000000 ) ) ;
#704=CARTESIAN_POINT ( 'NONE',  ( -4.649999849441000421, 19.99999984944626874, 6.648422602291999773E-08 ) ) ;
#707=CARTESIAN_POINT ( 'NONE',  ( -2.500000000000000000, 27.19999999999999929, 0.000000000000000000 ) ) ;
#711=CARTESIAN_POINT ( 'NONE',  ( 0.2939441912399000101, 30.67376943012999746, 2.707931486699000079 ) ) ;
#712=CARTESIAN_POINT ( 'NONE',  ( 0.6575429675851000022, 24.04609325200999947, -2.438473339150000196 ) ) ;
#713=CIRCLE ( 'NONE', #14639, 1.600000000000000089 ) ;
#718=ADVANCED_FACE ( 'NONE', ( #10105 ), #8276, .T. ) ;
#724=DIRECTION ( 'NONE',  ( 0.000000000000000000, 1.000000000000000000, 0.000000000000000000 ) ) ;
#735=CARTESIAN_POINT ( 'NONE',  ( 1.699986466736000068, 9.100024030970999434, -1.053574575520999757 ) ) ;
#737=CARTESIAN_POINT ( 'NONE',  ( 2.844001364980000002, 26.19169433609999942, -0.3933730402103999824 ) ) ;
#738=EDGE_LOOP ( 'NONE', ( #3127, #3699, #18368, #8559 ) ) ;
#739=ORIENTED_EDGE ( 'NONE', *, *, #9983, .F. ) ;
#747=FACE_OUTER_BOUND ( 'NONE', #13182, .T. ) ;
#750=CIRCLE ( 'NONE', #8500, 1.500000000000000000 ) ;
#751=EDGE_CURVE ( 'NONE', #9876, #8499, #3436, .T. ) ;
#752=CARTESIAN_POINT ( 'NONE',  ( 0.3930574723085999977, 29.80062481890999848, -2.323201669609999964 ) ) ;
#754=DIRECTION ( 'NONE',  ( 0.000000000000000000, 1.000000000000000000, 0.000000000000000000 ) ) ;
#755=CARTESIAN_POINT ( 'NONE',  ( -1.524638832331740579, 29.50412033714126281, 1.529828458804661340 ) ) ;
#758=CARTESIAN_POINT ( 'NONE',  ( 1.561610636931999974, 24.12936603334999930, -1.754607357718999783 ) ) ;
#760=EDGE_LOOP ( 'NONE', ( #18118, #12193, #17888, #4633 ) ) ;
#761=CARTESIAN_POINT ( 'NONE',  ( 2.063594504837999888E-14, 28.80370090847999975, 2.160000000000000142 ) ) ;
#764=CARTESIAN_POINT ( 'NONE',  ( -2.125680721937184270, 30.86389948294139174, 0.2107507025189759575 ) ) ;
#769=CARTESIAN_POINT ( 'NONE',  ( 2.500000000000000000, 26.80000000000000071, 0.000000000000000000 ) ) ;
#782=CARTESIAN_POINT ( 'NONE',  ( 0.6543697108981985089, 28.80086340285667035, -2.434931691670790599 ) ) ;
#783=DIRECTION ( 'NONE',  ( 0.5000000000000169864, 0.000000000000000000, -0.8660254037844289376 ) ) ;
#784=CARTESIAN_POINT ( 'NONE',  ( -2.159368856259221925, 30.20672668618349732, 0.05129505110700336573 ) ) ;
#792=EDGE_CURVE ( 'NONE', #20057, #2983, #19245, .T. ) ;
#794=ORIENTED_EDGE ( 'NONE', *, *, #514, .F. ) ;
#797=DIRECTION ( 'NONE',  ( -1.511005198495999796E-08, -0.9999999999999997780, -8.997177385936997916E-09 ) ) ;
#801=ORIENTED_EDGE ( 'NONE', *, *, #7489, .F. ) ;
#813=CYLINDRICAL_SURFACE ( 'NONE', #4199, 2.500000000000000000 ) ;
#816=CARTESIAN_POINT ( 'NONE',  ( 2.621867217767999581, 26.03250240010000027, 0.5899383557787000187 ) ) ;
#818=CARTESIAN_POINT ( 'NONE',  ( 2.051290025358256663, 28.96319104023008251, 0.6762458295797231234 ) ) ;
#824=CARTESIAN_POINT ( 'NONE',  ( 2.749999993363999806, 22.20000000663619844, -7.185653629187000299E-09 ) ) ;
#825=DIRECTION ( 'NONE',  ( 0.000000000000000000, -0.7071067811866525998, -0.7071067811864425456 ) ) ;
#830=CARTESIAN_POINT ( 'NONE',  ( -1.536366799937282090, 27.31666666666666643, 1.999167105995454552 ) ) ;
#839=CARTESIAN_POINT ( 'NONE',  ( 2.654275184457999703, 29.40713753664000052, -0.7025011426262000036 ) ) ;
#844=CARTESIAN_POINT ( 'NONE',  ( 2.434931691670788823, 29.46753006952333465, -0.6543697108982007293 ) ) ;
#846=CARTESIAN_POINT ( 'NONE',  ( 0.000000000000000000, 16.94999982584599962, 0.000000000000000000 ) ) ;
#850=CARTESIAN_POINT ( 'NONE',  ( 1.259047450927267331, 28.50086340285666964, 2.184465970885634434 ) ) ;
#852=CIRCLE ( 'NONE', #19843, 3.000000000000000000 ) ;
#855=ORIENTED_CLOSED_SHELL ( 'NONE', *, #19304, .F. );
#856=CARTESIAN_POINT ( 'NONE',  ( -0.7249434865795999494, 25.60669433610000212, -2.778011591584000239 ) ) ;
#857=ORIENTED_EDGE ( 'NONE', *, *, #16914, .F. ) ;
#868=CARTESIAN_POINT ( 'NONE',  ( 0.5078888037730999727, 28.64963248812999907, 2.300764967654999715 ) ) ;
#870=TOROIDAL_SURFACE ( 'NONE', #14801, 2.500000000000000000, 0.5500000000000000444 ) ;
#873=CARTESIAN_POINT ( 'NONE',  ( -1.078583570490634580, 29.53717604031488264, 1.871305732765136121 ) ) ;
#874=ORIENTED_EDGE ( 'NONE', *, *, #21732, .F. ) ;
#875=CARTESIAN_POINT ( 'NONE',  ( -1.197401029466999889, 24.51483033690999846, 1.828754584808999883 ) ) ;
#877=ORIENTED_EDGE ( 'NONE', *, *, #1121, .T. ) ;
#878=LINE ( 'NONE', #6334, #10288 ) ;
#882=EDGE_CURVE ( 'NONE', #17082, #17341, #6494, .T. ) ;
#884=ORIENTED_EDGE ( 'NONE', *, *, #314, .T. ) ;
#889=VERTEX_POINT ( 'NONE', #16732 ) ;
#890=CARTESIAN_POINT ( 'NONE',  ( -3.000000000000000000, 23.00000000000000000, 0.000000000000000000 ) ) ;
#892=CARTESIAN_POINT ( 'NONE',  ( 0.000000000000000000, 24.50000000000000000, 0.000000000000000000 ) ) ;
#897=FACE_OUTER_BOUND ( 'NONE', #22469, .T. ) ;
#899=CARTESIAN_POINT ( 'NONE',  ( -0.7318187998270080374, 26.37490599056236817, 4.196286372439437251 ) ) ;
#902=CARTESIAN_POINT ( 'NONE',  ( -2.152354865182170673, 30.19285038283803502, -0.1835425803383945731 ) ) ;
#903=VERTEX_POINT ( 'NONE', #1855 ) ;
#907=CARTESIAN_POINT ( 'NONE',  ( -2.500000000000000444, 27.45086340285666537, 0.3272492347489422415 ) ) ;
#908=CARTESIAN_POINT ( 'NONE',  ( 1.127279431983196911, 24.69814275126839576, 1.904603634755329900 ) ) ;
#911=ORIENTED_EDGE ( 'NONE', *, *, #23001, .F. ) ;
#914=AXIS2_PLACEMENT_3D ( 'NONE', #18012, #10626, #23575 ) ;
#915=DIRECTION ( 'NONE',  ( 0.000000000000000000, 1.000000000000000000, 0.000000000000000000 ) ) ;
#916=CARTESIAN_POINT ( 'NONE',  ( -0.07248595781348986244, 27.43395343009157727, -2.169876273640742870 ) ) ;
#917=ORIENTED_EDGE ( 'NONE', *, *, #4812, .T. ) ;
#918=ORIENTED_EDGE ( 'NONE', *, *, #14010, .F. ) ;
#919=DIRECTION ( 'NONE',  ( 0.000000000000000000, -1.000000000000000000, 0.000000000000000000 ) ) ;
#925=CARTESIAN_POINT ( 'NONE',  ( -2.000000000000000000, 24.50000000000000000, 3.464101615137999968 ) ) ;
#934=CARTESIAN_POINT ( 'NONE',  ( -0.2814148094397999622, 27.07250240009999942, -2.857252503208999705 ) ) ;
#936=EDGE_CURVE ( 'NONE', #12389, #16342, #3624, .T. ) ;
#938=CARTESIAN_POINT ( 'NONE',  ( -2.137330684254000079, 28.67937716036000140, 1.196956196243999848 ) ) ;
#942=DIRECTION ( 'NONE',  ( 0.000000000000000000, 1.000000000000000000, 0.000000000000000000 ) ) ;
#948=CARTESIAN_POINT ( 'NONE',  ( 0.000000000000000000, 15.09999999999999964, 0.000000000000000000 ) ) ;
#952=CARTESIAN_POINT ( 'NONE',  ( 0.6543697108982093891, 27.43333333333333357, 2.434931691670787046 ) ) ;
#953=VERTEX_POINT ( 'NONE', #23892 ) ;
#956=CARTESIAN_POINT ( 'NONE',  ( 0.9155719665318000633, 29.41635474111000192, -2.565350663984000246 ) ) ;
#960=CARTESIAN_POINT ( 'NONE',  ( 0.000000000000000000, -1.550000000000000044, 0.000000000000000000 ) ) ;
#961=CYLINDRICAL_SURFACE ( 'NONE', #4239, 3.000000000000000000 ) ;
#963=DIRECTION ( 'NONE',  ( 0.000000000000000000, 1.000000000000000000, 0.000000000000000000 ) ) ;
#967=FACE_OUTER_BOUND ( 'NONE', #16594, .T. ) ;
#968=EDGE_LOOP ( 'NONE', ( #9129, #8222, #23654, #14263 ) ) ;
#971=ORIENTED_EDGE ( 'NONE', *, *, #12390, .T. ) ;
#973=EDGE_CURVE ( 'NONE', #3560, #2047, #14455, .T. ) ;
#974=CARTESIAN_POINT ( 'NONE',  ( -1.502369499347320447, 23.90757363759589893, 1.597718646107638474 ) ) ;
#978=CARTESIAN_POINT ( 'NONE',  ( 4.000000000000000000, 26.50000000000000355, 0.000000000000000000 ) ) ;
#979=CARTESIAN_POINT ( 'NONE',  ( 0.05636985319968999819, 26.77669433610000382, 2.870524099806999629 ) ) ;
#980=B_SPLINE_CURVE_WITH_KNOTS ( 'NONE', 3,
 ( #19590, #14009, #21765, #10745, #21650, #23577, #23323, #10513, #17896, #6622 ),
 .UNSPECIFIED., .F., .F.,
 ( 4, 2, 2, 2, 4 ),
 ( 0.2499810176238006776, 0.4374857632178505984, 0.6249905088119004359, 0.8124952544059501625, 1.000000000000000000 ),
 .UNSPECIFIED. ) ;
#982=ADVANCED_BREP_SHAPE_REPRESENTATION ( '', ( #8659, #4390 ), #23331 ) ;
#984=DIRECTION ( 'NONE',  ( 0.000000000000000000, 1.000000000000000000, 0.000000000000000000 ) ) ;
#986=ORIENTED_EDGE ( 'NONE', *, *, #7332, .T. ) ;
#993=VECTOR ( 'NONE', #6073, 1000.000000000000000 ) ;
#997=AXIS2_PLACEMENT_3D ( 'NONE', #14640, #5794, #3629 ) ;
#998=CARTESIAN_POINT ( 'NONE',  ( 0.000000000000000000, 23.00000000000000000, 0.000000000000000000 ) ) ;
#999=CARTESIAN_POINT ( 'NONE',  ( -2.174360314446455611, 29.40514713709596961, 0.02075030649910500347 ) ) ;
#1001=CARTESIAN_POINT ( 'NONE',  ( -0.1522890450232986803, 24.04166422735650954, -2.528496764073642211 ) ) ;
#1003=EDGE_LOOP ( 'NONE', ( #15205, #18643, #14623, #7226 ) ) ;
#1008=ORIENTED_EDGE ( 'NONE', *, *, #13699, .F. ) ;
#1012=CARTESIAN_POINT ( 'NONE',  ( 1.999167105995449889, 26.88333333333333641, -1.536366799937288086 ) ) ;
#1015=DIRECTION ( 'NONE',  ( 0.000000000000000000, 0.000000000000000000, -1.000000000000000000 ) ) ;
#1020=DIRECTION ( 'NONE',  ( 0.7071067750626029991, 0.7071067873022029993, -3.423807777995014990E-06 ) ) ;
#1024=CARTESIAN_POINT ( 'NONE',  ( 0.000000000000000000, 15.04999987253367877, 0.000000000000000000 ) ) ;
#1028=CARTESIAN_POINT ( 'NONE',  ( -1.997348637187154052, 30.15409434752375972, -0.8235051463819260675 ) ) ;
#1029=EDGE_LOOP ( 'NONE', ( #20191, #6223, #8135, #10918 ) ) ;
#1034=CARTESIAN_POINT ( 'NONE',  ( -1.536366799937282313, 27.55086340285666680, 1.999167105995454552 ) ) ;
#1035=CARTESIAN_POINT ( 'NONE',  ( -1.523618227440715955, 24.32489914943822029, -1.660063800766738984 ) ) ;
#1040=CARTESIAN_POINT ( 'NONE',  ( -3.999709959627196110, 24.53198827073818578, -0.7544996412928929308 ) ) ;
#1045=VERTEX_POINT ( 'NONE', #20976 ) ;
#1053=CARTESIAN_POINT ( 'NONE',  ( 1.246850352501936765, 28.32748383450717711, -1.804444192914298695 ) ) ;
#1054=CARTESIAN_POINT ( 'NONE',  ( 0.000000000000000000, 22.00000000000000000, 0.000000000000000000 ) ) ;
#1056=CARTESIAN_POINT ( 'NONE',  ( 1.699986747157999911, 9.000014340785000400, 0.8485215224771999187 ) ) ;
#1057=ORIENTED_EDGE ( 'NONE', *, *, #17739, .F. ) ;
#1059=CARTESIAN_POINT ( 'NONE',  ( 2.361836001938000251, 25.88663313894999973, -0.7160459369172998967 ) ) ;
#1064=DIRECTION ( 'NONE',  ( 0.000000000000000000, 0.000000000000000000, -1.000000000000000000 ) ) ;
#1065=ORIENTED_EDGE ( 'NONE', *, *, #23915, .F. ) ;
#1072=DIRECTION ( 'NONE',  ( 0.000000000000000000, -1.000000000000000000, 0.000000000000000000 ) ) ;
#1073=CARTESIAN_POINT ( 'NONE',  ( -1.999167105995453442, 27.35086340285666395, -1.536366799937283645 ) ) ;
#1077=ADVANCED_FACE ( 'NONE', ( #19151, #385 ), #18683, .F. ) ;
#1079=ORIENTED_EDGE ( 'NONE', *, *, #8643, .T. ) ;
#1081=CARTESIAN_POINT ( 'NONE',  ( -0.6543697108982037269, 28.63333333333333641, -2.434931691670788823 ) ) ;
#1082=CARTESIAN_POINT ( 'NONE',  ( -1.273196900314999880, 30.92615821231000339, -1.841387178119999968 ) ) ;
#1083=PLANE ( 'NONE',  #21533 ) ;
#1088=DIRECTION ( 'NONE',  ( 1.000000000000000000, 0.000000000000000000, 0.000000000000000000 ) ) ;
#1089=EDGE_CURVE ( 'NONE', #18064, #16087, #22309, .T. ) ;
#1090=DIRECTION ( 'NONE',  ( 0.000000000000000000, 0.000000000000000000, 1.000000000000000000 ) ) ;
#1091=CARTESIAN_POINT ( 'NONE',  ( -2.000000000000000000, 23.50000000000000000, 0.000000000000000000 ) ) ;
#1094=CARTESIAN_POINT ( 'NONE',  ( 0.000000000000000000, 22.00000000000000000, 0.000000000000000000 ) ) ;
#1101=CARTESIAN_POINT ( 'NONE',  ( -2.389125669399000174, 25.50974983101999882, -0.8775158854510999307 ) ) ;
#1117=CARTESIAN_POINT ( 'NONE',  ( 0.000000000000000000, 19.00000000000000000, 0.000000000000000000 ) ) ;
#1119=CIRCLE ( 'NONE', #15016, 4.750000000000000000 ) ;
#1121=EDGE_CURVE ( 'NONE', #3998, #20964, #9719, .T. ) ;
#1124=ADVANCED_FACE ( 'NONE', ( #22660 ), #11660, .T. ) ;
#1128=CIRCLE ( 'NONE', #19706, 3.100000000000000089 ) ;
#1129=CARTESIAN_POINT ( 'NONE',  ( -1.286443996900747511, 29.52275116942843880, 1.737178360938291144 ) ) ;
#1131=CARTESIAN_POINT ( 'NONE',  ( 1.259047450927246903, 29.33333333333332860, -2.184465970885645536 ) ) ;
#1146=DIRECTION ( 'NONE',  ( -1.000000000000000000, 0.000000000000000000, 0.000000000000000000 ) ) ;
#1149=EDGE_LOOP ( 'NONE', ( #20634, #17980, #22228, #22921, #20107, #8861, #1065, #23136 ) ) ;
#1151=DIRECTION ( 'NONE',  ( 0.000000000000000000, -1.000000000000000000, 0.000000000000000000 ) ) ;
#1153=VECTOR ( 'NONE', #22123, 999.9999999999998863 ) ;
#1160=CARTESIAN_POINT ( 'NONE',  ( -1.172166007576319391, 30.07693318280233541, -1.814140047937379707 ) ) ;
#1161=ORIENTED_EDGE ( 'NONE', *, *, #13164, .T. ) ;
#1166=CARTESIAN_POINT ( 'NONE',  ( -1.751083909111127657, 24.51702249263829003, 1.418072448255935925 ) ) ;
#1169=VERTEX_POINT ( 'NONE', #17954 ) ;
#1174=CARTESIAN_POINT ( 'NONE',  ( 1.304922239495370340, 27.34765878667958461, -1.734344529965001325 ) ) ;
#1175=DIRECTION ( 'NONE',  ( 0.000000000000000000, 0.000000000000000000, 1.000000000000000000 ) ) ;
#1176=ORIENTED_EDGE ( 'NONE', *, *, #2264, .F. ) ;
#1177=DIRECTION ( 'NONE',  ( 0.000000000000000000, 1.000000000000000000, 0.000000000000000000 ) ) ;
#1183=CARTESIAN_POINT ( 'NONE',  ( 0.1826013610580650148, 28.39373671405435218, -2.164540525022182749 ) ) ;
#1184=CARTESIAN_POINT ( 'NONE',  ( 2.900806500513820829, 26.43562577624027199, -2.944020739578862234 ) ) ;
#1189=CARTESIAN_POINT ( 'NONE',  ( 0.6890999691677728300, 24.78398118435500308, 2.016836597077809046 ) ) ;
#1190=CARTESIAN_POINT ( 'NONE',  ( 3.821520914465099228, 26.24995697614777868, 2.412446024836691461 ) ) ;
#1196=CARTESIAN_POINT ( 'NONE',  ( 3.000000000000000000, 23.00000000000000000, 0.000000000000000000 ) ) ;
#1204=CARTESIAN_POINT ( 'NONE',  ( 1.259047450927256895, 27.46666666666666501, 2.184465970885639763 ) ) ;
#1207=CARTESIAN_POINT ( 'NONE',  ( -1.961028468976000028, 29.64181871290999837, 1.602965254429000064 ) ) ;
#1211=ORIENTED_EDGE ( 'NONE', *, *, #20206, .F. ) ;
#1213=CARTESIAN_POINT ( 'NONE',  ( 0.000000000000000000, 23.69744247139000137, 0.000000000000000000 ) ) ;
#1215=DIRECTION ( 'NONE',  ( 1.000000000000000000, 0.000000000000000000, 0.000000000000000000 ) ) ;
#1224=VERTEX_POINT ( 'NONE', #21342 ) ;
#1225=CARTESIAN_POINT ( 'NONE',  ( -0.2548307053832999935, 23.76799284288000180, -2.407861897382000294 ) ) ;
#1229=CARTESIAN_POINT ( 'NONE',  ( 2.184465970885645092, 27.66666666666667140, -1.259047450927249123 ) ) ;
#1230=ADVANCED_FACE ( 'NONE', ( #23382 ), #15983, .F. ) ;
#1232=ORIENTED_EDGE ( 'NONE', *, *, #22821, .T. ) ;
#1233=FACE_OUTER_BOUND ( 'NONE', #14772, .T. ) ;
#1234=CARTESIAN_POINT ( 'NONE',  ( -1.959116242179748779, 26.23461873539890021, 0.8476554397138756913 ) ) ;
#1241=CARTESIAN_POINT ( 'NONE',  ( -2.163699527451000026, 30.08248585635000083, -0.1363395057005999944 ) ) ;
#1247=AXIS2_PLACEMENT_3D ( 'NONE', #16175, #1177, #15929 ) ;
#1248=CARTESIAN_POINT ( 'NONE',  ( -1.638949455867213079, 29.31355001292886797, -1.406705521346627297 ) ) ;
#1249=ORIENTED_EDGE ( 'NONE', *, *, #11485, .T. ) ;
#1250=DIRECTION ( 'NONE',  ( 0.000000000000000000, 0.000000000000000000, 1.000000000000000000 ) ) ;
#1254=CARTESIAN_POINT ( 'NONE',  ( -2.218105065315603142, 30.46568852542990768, 1.261346933442557772 ) ) ;
#1259=CARTESIAN_POINT ( 'NONE',  ( -1.603077936557000038, 27.47506359724000191, -1.876963106047000007 ) ) ;
#1261=EDGE_CURVE ( 'NONE', #11307, #551, #2937, .T. ) ;
#1262=ORIENTED_EDGE ( 'NONE', *, *, #16370, .T. ) ;
#1264=DIRECTION ( 'NONE',  ( 1.000000000000000000, 0.000000000000000000, 0.000000000000000000 ) ) ;
#1270=VECTOR ( 'NONE', #13225, 1000.000000000000114 ) ;
#1274=DIRECTION ( 'NONE',  ( -0.000000000000000000, 1.000000000000000000, 0.000000000000000000 ) ) ;
#1277=CARTESIAN_POINT ( 'NONE',  ( 0.6950034797113096019, 26.37418302490043587, 4.217541707417931995 ) ) ;
#1279=CARTESIAN_POINT ( 'NONE',  ( -1.606116587811105001, 30.11053178658430340, -1.444150352961293793 ) ) ;
#1280=ORIENTED_EDGE ( 'NONE', *, *, #7489, .T. ) ;
#1281=CARTESIAN_POINT ( 'NONE',  ( -0.2703868746345000074, 25.22914974194000237, -2.319981033806999715 ) ) ;
#1284=CARTESIAN_POINT ( 'NONE',  ( -2.097612193317242024, 23.63127982162329133, -0.4251272349260063477 ) ) ;
#1293=EDGE_LOOP ( 'NONE', ( #2027, #12212 ) ) ;
#1302=ADVANCED_FACE ( 'NONE', ( #22900 ), #11770, .F. ) ;
#1303=ADVANCED_FACE ( 'NONE', ( #6315 ), #5575, .F. ) ;
#1305=CARTESIAN_POINT ( 'NONE',  ( -2.004270392011611612, 26.94942393816377191, -0.9183958586233323951 ) ) ;
#1307=CARTESIAN_POINT ( 'NONE',  ( 3.304996520289660733, 26.37418302490023692, -2.710661522857508388 ) ) ;
#1308=DIRECTION ( 'NONE',  ( 0.000000000000000000, 1.000000000000000000, 0.000000000000000000 ) ) ;
#1312=CARTESIAN_POINT ( 'NONE',  ( 2.245636445399999737, 26.56119850838000218, -0.3106091461882000138 ) ) ;
#1314=CARTESIAN_POINT ( 'NONE',  ( 3.560623727957782592, 26.31534065533139710, 2.563075085697512190 ) ) ;
#1317=EDGE_LOOP ( 'NONE', ( #11536, #22718, #18025, #6085 ) ) ;
#1322=CIRCLE ( 'NONE', #14832, 2.399999999999999911 ) ;
#1331=CARTESIAN_POINT ( 'NONE',  ( 2.487975651965000257, 29.17856066959000216, -0.4744621780437000003 ) ) ;
#1341=LINE ( 'NONE', #10303, #13747 ) ;
#1345=ORIENTED_EDGE ( 'NONE', *, *, #20031, .F. ) ;
#1347=CARTESIAN_POINT ( 'NONE',  ( -4.000000000000000000, 26.24995697614769341, 2.103311180602513986 ) ) ;
#1349=CARTESIAN_POINT ( 'NONE',  ( -0.2740503536635999771, 23.87342747345000049, -2.589465832062999961 ) ) ;
#1362=FACE_OUTER_BOUND ( 'NONE', #5374, .T. ) ;
#1365=CARTESIAN_POINT ( 'NONE',  ( 3.999709959623201971, 24.53198827073818933, 0.7544996413140969693 ) ) ;
#1366=CARTESIAN_POINT ( 'NONE',  ( 2.322667919087999966, 30.40790453936999782, -0.4211969760945999952 ) ) ;
#1369=ORIENTED_EDGE ( 'NONE', *, *, #23767, .T. ) ;
#1371=EDGE_CURVE ( 'NONE', #11130, #22702, #21894, .T. ) ;
#1374=DIRECTION ( 'NONE',  ( 0.000000000000000000, 1.000000000000000000, 0.000000000000000000 ) ) ;
#1380=CARTESIAN_POINT ( 'NONE',  ( 0.04846321314155000587, 26.98756359724000120, 2.467893978438000069 ) ) ;
#1381=ADVANCED_FACE ( 'NONE', ( #5 ), #10686, .T. ) ;
#1391=CARTESIAN_POINT ( 'NONE',  ( 0.000000000000000000, 20.00000000000000000, 0.000000000000000000 ) ) ;
#1394=DIRECTION ( 'NONE',  ( -1.345659694784736864E-09, -1.000000000000000000, 0.000000000000000000 ) ) ;
#1396=CARTESIAN_POINT ( 'NONE',  ( -1.018716668670999859, 30.37106448208000131, 1.936711703186000166 ) ) ;
#1399=CARTESIAN_POINT ( 'NONE',  ( 0.9774796333180513219, 29.94423007303124251, -1.927981652679361391 ) ) ;
#1400=ORIENTED_EDGE ( 'NONE', *, *, #8012, .F. ) ;
#1403=CARTESIAN_POINT ( 'NONE',  ( -1.182437155214619562, 23.61728437556105931, -1.756346252138746289 ) ) ;
#1404=ORIENTED_EDGE ( 'NONE', *, *, #22713, .F. ) ;
#1406=DIRECTION ( 'NONE',  ( 1.000000000000000000, 0.000000000000000000, 0.000000000000000000 ) ) ;
#1412=VERTEX_POINT ( 'NONE', #3304 ) ;
#1413=CARTESIAN_POINT ( 'NONE',  ( -2.037157279014845113, 26.87920215101449273, 0.8280411290571204619 ) ) ;
#1416=ORIENTED_EDGE ( 'NONE', *, *, #2707, .T. ) ;
#1423=CARTESIAN_POINT ( 'NONE',  ( -1.829580058295768197, 27.87696425337853157, 1.172525041583718952 ) ) ;
#1427=ADVANCED_FACE ( 'NONE', ( #9215 ), #13691, .F. ) ;
#1428=CARTESIAN_POINT ( 'NONE',  ( 0.8316999784727749923, 30.75381617240658727, -2.001085836244213656 ) ) ;
#1429=VERTEX_POINT ( 'NONE', #14321 ) ;
#1430=ADVANCED_FACE ( 'NONE', ( #12620, #20130 ), #16593, .F. ) ;
#1431=CARTESIAN_POINT ( 'NONE',  ( -2.000000000000000000, 26.50000000000000355, -3.464101615137999968 ) ) ;
#1433=CARTESIAN_POINT ( 'NONE',  ( -2.456483904114000083, 27.83663313894999902, -0.2419425476017999788 ) ) ;
#1434=CARTESIAN_POINT ( 'NONE',  ( -1.271041439915000071, 26.35771896306000173, 1.902247796447000150 ) ) ;
#1437=DIRECTION ( 'NONE',  ( -1.000000000000000000, 0.000000000000000000, 0.000000000000000000 ) ) ;
#1439=EDGE_CURVE ( 'NONE', #6590, #8278, #6877, .T. ) ;
#1445=CARTESIAN_POINT ( 'NONE',  ( -2.181170733482575841, 30.72643194342732897, -0.6746858939111454179 ) ) ;
#1446=DIRECTION ( 'NONE',  ( 0.000000000000000000, 1.000000000000000000, 0.000000000000000000 ) ) ;
#1450=CARTESIAN_POINT ( 'NONE',  ( 1.259047450927246903, 28.53333333333332789, -2.184465970885645536 ) ) ;
#1451=CARTESIAN_POINT ( 'NONE',  ( 1.669522189709000015, 29.04620122864000109, 1.904710300619000263 ) ) ;
#1452=DIRECTION ( 'NONE',  ( -1.000000000000000000, 0.000000000000000000, 0.000000000000000000 ) ) ;
#1453=CARTESIAN_POINT ( 'NONE',  ( 0.000000000000000000, 21.89999999999999858, 0.000000000000000000 ) ) ;
#1454=CIRCLE ( 'NONE', #4153, 2.000000000000000000 ) ;
#1456=CARTESIAN_POINT ( 'NONE',  ( 0.000000000000000000, 21.89999999999999858, 0.000000000000000000 ) ) ;
#1457=DIRECTION ( 'NONE',  ( 1.000000000000000000, 0.000000000000000000, 0.000000000000000000 ) ) ;
#1458=B_SPLINE_SURFACE_WITH_KNOTS ( 'NONE', 3, 3, ( 
 ( #5157, #3570, #16630, #14696, #7307, #5268, #10845, #3225, #5386, #23551, #19925, #3681, #12773, #14352, #40, #11072, #22089, #6961, #12654, #12426, #18455, #16510, #16150, #23781, #1520, #10607, #10721, #14231, #7188, #21626, #20045, #5498, #18339, #3461, #1865 ),
 ( #1748, #5044, #3343, #18229, #19810, #20162, #14577, #8908, #23899, #18115, #17991, #1396, #21744, #16275, #8787, #23668, #7078, #14464, #1631, #21972, #11314, #9726, #13120, #16863, #18578, #4280, #18805, #11549, #22316, #15045, #17109, #5733, #15159, #3802, #507 ),
 ( #20746, #7907, #1983, #2097, #14805, #9486, #11668, #9366, #13468, #12995, #2451, #22440, #5613, #9605, #5960, #15276, #22668, #20626, #5850, #16991, #16741, #265, #150, #7671, #392, #6077, #13233, #22554, #7542, #2213, #14922, #22200, #4036, #11431, #20396 ),
 ( #20871, #7790, #13345, #19041, #18929, #4152, #9843, #2338, #17223, #7423, #11196, #20517, #3922, #18690, #10088, #13588, #752, #11786, #23270, #9961, #21471, #6684, #17474, #12150, #19414, #21349, #12031, #21231, #23151, #15399, #10333, #22788, #868, #3074, #21103 ) ),
 .UNSPECIFIED., .F., .F., .F.,
 ( 4, 4 ),
 ( 4, 1, 1, 1, 1, 1, 1, 1, 1, 1, 1, 1, 1, 1, 1, 1, 1, 1, 1, 1, 1, 1, 1, 1, 1, 1, 1, 1, 1, 1, 1, 1, 4 ),
 ( -0.2678694646895999898, 1.311704223562000005 ),
 ( 0.2474280914112999830, 0.2714070983026000139, 0.2953861051939000171, 0.3193651120852000203, 0.3433441189764999679, 0.3673231258677999711, 0.3913021327591000298, 0.4152811396504000330, 0.4392601465417000361, 0.4632391534331000149, 0.4872181603244000181, 0.5111971672156999658, 0.5351761741069999134, 0.5591551809982999721, 0.5831341878895999198, 0.6071131947808999785, 0.6310922016721999261, 0.6550712085634999848, 0.6790502154547999325, 0.7030292223460999912, 0.7270082292373999389, 0.7509872361286999976, 0.7749662430200000562, 0.7989452499113000039, 0.8229242568026999827, 0.8469032636939999303, 0.8708822705852999890, 0.8948612774765999367, 0.9188402843678999954, 0.9428192912591999431, 0.9667982981504998907, 0.9907773050418000604, 1.014756311932999866 ),
 .UNSPECIFIED. ) ;
#1461=CONICAL_SURFACE ( 'NONE', #9948, 4.699999872533999756, 0.7853981633972997312 ) ;
#1467=EDGE_LOOP ( 'NONE', ( #22447, #19545, #3049 ) ) ;
#1469=CARTESIAN_POINT ( 'NONE',  ( 0.8491321808655799552, 24.60222989789001247, -4.128541458486335358 ) ) ;
#1471=CARTESIAN_POINT ( 'NONE',  ( -1.036892826754999941, 24.70947082776000059, -2.533142039532999767 ) ) ;
#1472=DIRECTION ( 'NONE',  ( 0.000000000000000000, 1.000000000000000000, 0.000000000000000000 ) ) ;
#1474=CIRCLE ( 'NONE', #6092, 4.649999999999999467 ) ;
#1477=CARTESIAN_POINT ( 'NONE',  ( -2.500000000000000000, 24.00000000000000000, 8.181116922990998136E-14 ) ) ;
#1478=ORIENTED_EDGE ( 'NONE', *, *, #19725, .T. ) ;
#1479=CARTESIAN_POINT ( 'NONE',  ( -0.6543697108981929578, 30.00086340285666964, 2.434931691670791487 ) ) ;
#1481=CARTESIAN_POINT ( 'NONE',  ( 0.000000000000000000, 18.89999999999999858, 0.000000000000000000 ) ) ;
#1483=EDGE_LOOP ( 'NONE', ( #2128, #17775, #11631, #210 ) ) ;
#1489=CARTESIAN_POINT ( 'NONE',  ( -1.755728607737000013, 30.01067697075000140, -1.271849504351999949 ) ) ;
#1492=ORIENTED_EDGE ( 'NONE', *, *, #3306, .T. ) ;
#1495=DIRECTION ( 'NONE',  ( 1.000000000000000000, 0.000000000000000000, 0.000000000000000000 ) ) ;
#1497=CARTESIAN_POINT ( 'NONE',  ( -0.1652120097165999946, 23.43138837836000121, -2.228042744016999865 ) ) ;
#1500=TOROIDAL_SURFACE ( 'NONE', #10383, 2.500000000000000000, 0.5500000000000000444 ) ;
#1506=DIRECTION ( 'NONE',  ( 0.000000000000000000, -1.000000000000000000, 0.000000000000000000 ) ) ;
#1507=ORIENTED_EDGE ( 'NONE', *, *, #17841, .T. ) ;
#1519=AXIS2_PLACEMENT_3D ( 'NONE', #892, #19439, #2849 ) ;
#1520=CARTESIAN_POINT ( 'NONE',  ( -2.342248944605000105, 29.41754141063000105, 0.05822147085768999974 ) ) ;
#1523=CARTESIAN_POINT ( 'NONE',  ( 1.058847381058417580, 29.93878768364113085, -1.884670918156025499 ) ) ;
#1528=CARTESIAN_POINT ( 'NONE',  ( -0.8577166501281039412, 23.63976374042652395, -1.960334821351923384 ) ) ;
#1531=CARTESIAN_POINT ( 'NONE',  ( 0.000000000000000000, 7.000000000000000000, 0.000000000000000000 ) ) ;
#1535=CARTESIAN_POINT ( 'NONE',  ( 0.000000000000000000, 24.50000000000000000, -4.000000000000614619 ) ) ;
#1537=VECTOR ( 'NONE', #16304, 1000.000000000000114 ) ;
#1539=CIRCLE ( 'NONE', #16992, 4.549999999999999822 ) ;
#1540=CARTESIAN_POINT ( 'NONE',  ( 0.000000000000000000, 30.75000005827999772, 0.000000000000000000 ) ) ;
#1549=CARTESIAN_POINT ( 'NONE',  ( -1.967423287079686611, 27.74445849415545595, -0.9951881276287170008 ) ) ;
#1550=CARTESIAN_POINT ( 'NONE',  ( 2.870524099806999629, 27.65750240010000027, 0.05636985319957999591 ) ) ;
#1551=CIRCLE ( 'NONE', #7323, 4.549999999999999822 ) ;
#1553=CARTESIAN_POINT ( 'NONE',  ( 2.144633374660529501, 30.61889166568773391, -0.2565629783008914755 ) ) ;
#1554=ORIENTED_EDGE ( 'NONE', *, *, #17032, .T. ) ;
#1557=CARTESIAN_POINT ( 'NONE',  ( -1.259486242684000112, 26.26869850838000175, 1.884954223019000175 ) ) ;
#1559=CARTESIAN_POINT ( 'NONE',  ( 2.252185756629999869, 28.21021896306000087, 0.4021892318948999678 ) ) ;
#1560=CIRCLE ( 'NONE', #5795, 1.999999992708000773 ) ;
#1574=CARTESIAN_POINT ( 'NONE',  ( -0.6543697108981929578, 29.20086340285667248, 2.434931691670791487 ) ) ;
#1575=CARTESIAN_POINT ( 'NONE',  ( 2.300329438417999750, 29.07312603901999992, -0.4386776513298999980 ) ) ;
#1582=EDGE_CURVE ( 'NONE', #9355, #6055, #19428, .T. ) ;
#1583=CARTESIAN_POINT ( 'NONE',  ( 2.500000000000000000, 29.19999999999999929, 0.000000000000000000 ) ) ;
#1584=EDGE_CURVE ( 'NONE', #11323, #18038, #22501, .T. ) ;
#1589=VERTEX_POINT ( 'NONE', #1946 ) ;
#1590=DIRECTION ( 'NONE',  ( 0.000000000000000000, -1.000000000000000000, 0.000000000000000000 ) ) ;
#1591=CARTESIAN_POINT ( 'NONE',  ( 1.800000000175999926, 13.00000000000000000, 1.081665382745000015 ) ) ;
#1593=CARTESIAN_POINT ( 'NONE',  ( -2.372070577900000199, 23.90733340193000345, -0.9226943487805999711 ) ) ;
#1601=CONICAL_SURFACE ( 'NONE', #17442, 4.309401076758999416, 1.119376321708719590 ) ;
#1606=CARTESIAN_POINT ( 'NONE',  ( -2.032167282806999875, 24.44908585634999909, -0.6853045129910999567 ) ) ;
#1608=CARTESIAN_POINT ( 'NONE',  ( 4.000000000000117240, 24.49999999999975486, 0.1904558375517787505 ) ) ;
#1610=CARTESIAN_POINT ( 'NONE',  ( -2.336652659577999724, 30.76694896736999851, -0.3346041500006000091 ) ) ;
#1614=ORIENTED_EDGE ( 'NONE', *, *, #12057, .T. ) ;
#1615=CARTESIAN_POINT ( 'NONE',  ( -2.999999998489146336, 15.10000000000041176, 8.997179835138123378E-10 ) ) ;
#1617=CARTESIAN_POINT ( 'NONE',  ( -4.625000000000000000, 13.00000000000000000, 0.000000000000000000 ) ) ;
#1631=CARTESIAN_POINT ( 'NONE',  ( 2.107129814228999809, 29.86750533736999813, -0.5904572975527000445 ) ) ;
#1633=CARTESIAN_POINT ( 'NONE',  ( 1.813637125157641083, 29.87718600260956947, -1.176169980081204436 ) ) ;
#1634=ORIENTED_EDGE ( 'NONE', *, *, #2422, .F. ) ;
#1640=EDGE_CURVE ( 'NONE', #11953, #23400, #3577, .T. ) ;
#1645=CARTESIAN_POINT ( 'NONE',  ( 0.000000000000000000, 9.050044887908999414, -1.949955127985000258 ) ) ;
#1647=CARTESIAN_POINT ( 'NONE',  ( -1.999167105995441673, 28.31753006952333607, 1.536366799937297856 ) ) ;
#1648=CARTESIAN_POINT ( 'NONE',  ( 1.259047450927256895, 29.86666666666666359, 2.184465970885639763 ) ) ;
#1656=CARTESIAN_POINT ( 'NONE',  ( -0.6576427108141560396, 26.84341933061397611, -2.107288224371474783 ) ) ;
#1657=CARTESIAN_POINT ( 'NONE',  ( 2.387212940976999764, 28.53500240009999800, -1.595084814687000030 ) ) ;
#1658=CARTESIAN_POINT ( 'NONE',  ( 2.001789734241726570, 30.65294125138512626, -0.8114744869051462306 ) ) ;
#1661=DIRECTION ( 'NONE',  ( 0.000000000000000000, 1.000000000000000000, 0.000000000000000000 ) ) ;
#1663=CONICAL_SURFACE ( 'NONE', #21391, 2.249999993279999888, 0.7853981633972997312 ) ;
#1665=CARTESIAN_POINT ( 'NONE',  ( 0.04491825056511999925, 27.23521896306000301, 2.287373719275000106 ) ) ;
#1673=CARTESIAN_POINT ( 'NONE',  ( -2.500000000000000000, 24.00000000000000000, 8.181116922990998136E-14 ) ) ;
#1678=CARTESIAN_POINT ( 'NONE',  ( 2.500000000000001776, 29.41753006952333394, 0.3272492347489266429 ) ) ;
#1679=CARTESIAN_POINT ( 'NONE',  ( -0.7692266288049000034, 29.49712917223999753, 2.008491639871999634 ) ) ;
#1682=ORIENTED_EDGE ( 'NONE', *, *, #28, .T. ) ;
#1691=CARTESIAN_POINT ( 'NONE',  ( 0.2865205186993326492, 29.18676986812987195, -2.140916946558517608 ) ) ;
#1695=EDGE_CURVE ( 'NONE', #11307, #14835, #4740, .T. ) ;
#1696=CARTESIAN_POINT ( 'NONE',  ( -3.999999999999999112, 26.41068681084913194, 1.228746328088897721 ) ) ;
#1697=ORIENTED_EDGE ( 'NONE', *, *, #21953, .F. ) ;
#1698=CARTESIAN_POINT ( 'NONE',  ( -2.120220590722000420, 25.36855084940000182, 0.4191826807252999609 ) ) ;
#1699=CARTESIAN_POINT ( 'NONE',  ( -2.499999999999999556, 28.01666666666666927, 0.3272492347489423525 ) ) ;
#1702=CARTESIAN_POINT ( 'NONE',  ( 2.500000000000000000, 27.59999999999999787, 0.000000000000000000 ) ) ;
#1705=EDGE_CURVE ( 'NONE', #13340, #18875, #16390, .T. ) ;
#1708=CARTESIAN_POINT ( 'NONE',  ( -1.664359855051821491, 26.21279260321131588, 1.307626407210986219 ) ) ;
#1712=CARTESIAN_POINT ( 'NONE',  ( -0.5089225745698999770, 24.32100362754999878, -2.083349215147999978 ) ) ;
#1717=CARTESIAN_POINT ( 'NONE',  ( 0.3968543755643999527, 29.86705919954999899, -2.131358888218999770 ) ) ;
#1729=CARTESIAN_POINT ( 'NONE',  ( 0.000000000000000000, 7.049999902385000183, -1.449999902385000095 ) ) ;
#1735=B_SPLINE_CURVE_WITH_KNOTS ( 'NONE', 3,
 ( #5787, #11487, #16682, #90, #18862, #3974 ),
 .UNSPECIFIED., .F., .F.,
 ( 4, 2, 4 ),
 ( 0.002503788684009304773, 0.003059594342613334954, 0.003615400001217365135 ),
 .UNSPECIFIED. ) ;
#1736=CARTESIAN_POINT ( 'NONE',  ( 2.361836001938000251, 25.62256359724000276, -0.7160459369172998967 ) ) ;
#1738=ORIENTED_EDGE ( 'NONE', *, *, #8654, .T. ) ;
#1747=CARTESIAN_POINT ( 'NONE',  ( 2.100000000000000089, 18.10000000000000142, 2.368341633917999944E-10 ) ) ;
#1748=CARTESIAN_POINT ( 'NONE',  ( -1.865383466706000082, 31.09043468882000028, 0.9086832089919000266 ) ) ;
#1751=CARTESIAN_POINT ( 'NONE',  ( 2.136626277416635133, 29.82246383866652195, -0.3158569418315477217 ) ) ;
#1752=ORIENTED_EDGE ( 'NONE', *, *, #16515, .F. ) ;
#1753=CARTESIAN_POINT ( 'NONE',  ( 2.112124071471999986, 24.20052506214999966, 0.5457312241595999591 ) ) ;
#1757=CARTESIAN_POINT ( 'NONE',  ( -0.1513776656675359655, 24.53216460021022272, -2.367835399791780482 ) ) ;
#1759=B_SPLINE_CURVE_WITH_KNOTS ( 'NONE', 3,
 ( #22778, #2936, #13822, #2696 ),
 .UNSPECIFIED., .F., .F.,
 ( 4, 4 ),
 ( 3.110165528588429006E-14, 0.0001520356277385664402 ),
 .UNSPECIFIED. ) ;
#1765=CARTESIAN_POINT ( 'NONE',  ( -2.184465970885638875, 28.30086340285666680, 1.259047450927259559 ) ) ;
#1769=CARTESIAN_POINT ( 'NONE',  ( 1.999582798912397763, 24.48329780672474598, -1.535796015288176664 ) ) ;
#1775=CARTESIAN_POINT ( 'NONE',  ( -2.020216954725641667, 27.05542854569362632, 0.8542913370163738307 ) ) ;
#1776=CARTESIAN_POINT ( 'NONE',  ( 2.030158388880999976, 27.56000240010000013, 2.030158388880999976 ) ) ;
#1779=CARTESIAN_POINT ( 'NONE',  ( 0.000000000000000000, 21.87500000000000000, 0.000000000000000000 ) ) ;
#1781=VECTOR ( 'NONE', #5397, 1000.000000000000000 ) ;
#1783=CARTESIAN_POINT ( 'NONE',  ( 2.189073617939000016, 25.87021896306000102, -0.6636689712801000507 ) ) ;
#1784=CARTESIAN_POINT ( 'NONE',  ( -2.123501712390408525, 30.87060775419617897, 0.1583979370652605911 ) ) ;
#1788=CARTESIAN_POINT ( 'NONE',  ( 3.000000000000000000, 19.09999999999999787, 0.000000000000000000 ) ) ;
#1791=DIRECTION ( 'NONE',  ( 0.5000000000000169864, 0.000000000000000000, -0.8660254037844288266 ) ) ;
#1793=CIRCLE ( 'NONE', #4902, 3.000000000000000000 ) ;
#1794=CONICAL_SURFACE ( 'NONE', #8852, 1.949955127985000258, 0.7853751480324476786 ) ;
#1798=CARTESIAN_POINT ( 'NONE',  ( 2.184465970885649089, 29.36753006952332967, 1.259047450927240241 ) ) ;
#1800=CARTESIAN_POINT ( 'NONE',  ( 0.000000000000000000, 14.90000000000000036, 0.000000000000000000 ) ) ;
#1802=ORIENTED_EDGE ( 'NONE', *, *, #23005, .F. ) ;
#1805=CARTESIAN_POINT ( 'NONE',  ( -4.000000000000000000, 24.50000000000000000, -2.309401076759000304 ) ) ;
#1807=DIRECTION ( 'NONE',  ( 0.000000000000000000, 1.000000000000000000, 0.000000000000000000 ) ) ;
#1810=CARTESIAN_POINT ( 'NONE',  ( -0.2595857393297835713, 29.21926038359636379, -2.144188719129172860 ) ) ;
#1813=VERTEX_POINT ( 'NONE', #8483 ) ;
#1814=VECTOR ( 'NONE', #7381, 1000.000000000000000 ) ;
#1815=CARTESIAN_POINT ( 'NONE',  ( 1.549127279887130060, 23.82637683446857579, 1.758539927998388652 ) ) ;
#1817=CARTESIAN_POINT ( 'NONE',  ( 2.291555368458999986, 24.21992044851000259, 0.5351892104662999694 ) ) ;
#1825=CARTESIAN_POINT ( 'NONE',  ( 0.000000000000000000, 24.65000000674550051, 0.000000000000000000 ) ) ;
#1828=EDGE_CURVE ( 'NONE', #11598, #17995, #15849, .T. ) ;
#1832=CARTESIAN_POINT ( 'NONE',  ( 1.141652241544000024, 24.92002125539000090, -2.036977516418999823 ) ) ;
#1836=CARTESIAN_POINT ( 'NONE',  ( 1.463521000971000019, 28.89991794178999740, -1.852106567100999968 ) ) ;
#1838=CARTESIAN_POINT ( 'NONE',  ( 0.000000000000000000, 31.00000000000000000, 0.000000000000000000 ) ) ;
#1839=CARTESIAN_POINT ( 'NONE',  ( -2.434931691670788378, 26.66753006952334104, 0.6543697108982053923 ) ) ;
#1844=AXIS2_PLACEMENT_3D ( 'NONE', #8315, #915, #4318 ) ;
#1845=ORIENTED_EDGE ( 'NONE', *, *, #17835, .F. ) ;
#1850=CARTESIAN_POINT ( 'NONE',  ( 0.000000000000000000, 24.00000000000000000, 0.000000000000000000 ) ) ;
#1851=CARTESIAN_POINT ( 'NONE',  ( 1.996953125041000199, 26.30506359724000021, 1.450871306011999984 ) ) ;
#1852=ORIENTED_EDGE ( 'NONE', *, *, #4997, .F. ) ;
#1855=CARTESIAN_POINT ( 'NONE',  ( 0.000000000000000000, 15.09999999999999964, -4.750000000000305533 ) ) ;
#1865=CARTESIAN_POINT ( 'NONE',  ( -0.7569538692457000728, 28.77010822455999772, 2.088667364863999953 ) ) ;
#1869=CARTESIAN_POINT ( 'NONE',  ( 1.939861484286318882, 29.86184696477200262, -0.9499241564717313402 ) ) ;
#1870=EDGE_CURVE ( 'NONE', #5391, #16168, #3123, .T. ) ;
#1871=ORIENTED_EDGE ( 'NONE', *, *, #18001, .T. ) ;
#1872=CARTESIAN_POINT ( 'NONE',  ( 2.137452445837000337, 25.56179681940000137, 0.4573846582827000296 ) ) ;
#1875=CARTESIAN_POINT ( 'NONE',  ( -0.8818583641180756105, 23.65266154262563703, -1.963742263792713549 ) ) ;
#1877=VERTEX_POINT ( 'NONE', #8849 ) ;
#1879=AXIS2_PLACEMENT_3D ( 'NONE', #18294, #3634, #18062 ) ;
#1883=DIRECTION ( 'NONE',  ( 0.000000000000000000, -1.000000000000000000, 0.000000000000000000 ) ) ;
#1889=AXIS2_PLACEMENT_3D ( 'NONE', #5901, #22611, #9901 ) ;
#1895=CARTESIAN_POINT ( 'NONE',  ( 1.421749254172319565, 26.44307886155625198, -1.887007990465741081 ) ) ;
#1898=CARTESIAN_POINT ( 'NONE',  ( 1.635367627583443229, 30.69443307109471419, -1.412121873945937356 ) ) ;
#1900=CARTESIAN_POINT ( 'NONE',  ( 0.000000000000000000, 8.900000000000000355, 0.000000000000000000 ) ) ;
#1904=CARTESIAN_POINT ( 'NONE',  ( -1.739667959131000030, 26.94271896305999903, -1.485816803342000281 ) ) ;
#1907=ORIENTED_EDGE ( 'NONE', *, *, #81, .T. ) ;
#1910=AXIS2_PLACEMENT_3D ( 'NONE', #21327, #16229, #10553 ) ;
#1911=CARTESIAN_POINT ( 'NONE',  ( 0.000000000000000000, 24.29999999999999716, 0.000000000000000000 ) ) ;
#1917=DIRECTION ( 'NONE',  ( -1.000000000000000000, 0.000000000000000000, 0.000000000000000000 ) ) ;
#1918=CARTESIAN_POINT ( 'NONE',  ( -2.017184895920000276, 29.29859001081999992, -0.7461322788111000026 ) ) ;
#1923=CARTESIAN_POINT ( 'NONE',  ( 0.000000000000000000, 15.00000000000000000, 0.000000000000000000 ) ) ;
#1925=CARTESIAN_POINT ( 'NONE',  ( 0.000000000000000000, 22.00131761696259503, 0.000000000000000000 ) ) ;
#1926=ORIENTED_EDGE ( 'NONE', *, *, #8029, .T. ) ;
#1930=CARTESIAN_POINT ( 'NONE',  ( 0.2764502732170818211, 29.18736629261196214, -2.142238836452773576 ) ) ;
#1932=ORIENTED_EDGE ( 'NONE', *, *, #2874, .T. ) ;
#1934=EDGE_CURVE ( 'NONE', #15539, #15097, #1560, .T. ) ;
#1935=CARTESIAN_POINT ( 'NONE',  ( 2.349836359248000051, 25.05596380282000268, -0.1261848867558000020 ) ) ;
#1938=LINE ( 'NONE', #224, #1814 ) ;
#1939=DIRECTION ( 'NONE',  ( 0.000000000000000000, 1.000000000000000000, 0.000000000000000000 ) ) ;
#1944=AXIS2_PLACEMENT_3D ( 'NONE', #1453, #18509, #23612 ) ;
#1946=CARTESIAN_POINT ( 'NONE',  ( 4.649999999999999467, 20.00000000000000000, 0.000000000000000000 ) ) ;
#1947=ORIENTED_EDGE ( 'NONE', *, *, #9271, .T. ) ;
#1950=CARTESIAN_POINT ( 'NONE',  ( -1.384310211871999874, 25.30426794178999828, 1.880513647577999992 ) ) ;
#1954=CARTESIAN_POINT ( 'NONE',  ( 0.1485877089535999895, 30.08704325201000174, 2.548780468506000041 ) ) ;
#1960=CARTESIAN_POINT ( 'NONE',  ( -1.806240660677517873, 24.33331728578134090, 1.776608537230899509 ) ) ;
#1962=ORIENTED_EDGE ( 'NONE', *, *, #6661, .T. ) ;
#1963=EDGE_CURVE ( 'NONE', #6244, #20885, #20141, .T. ) ;
#1968=AXIS2_PLACEMENT_3D ( 'NONE', #17301, #700, #8109 ) ;
#1970=CARTESIAN_POINT ( 'NONE',  ( 0.5485649090616000478, 28.50712896666999896, 2.437990915149000237 ) ) ;
#1972=ORIENTED_EDGE ( 'NONE', *, *, #2264, .T. ) ;
#1983=CARTESIAN_POINT ( 'NONE',  ( -2.179000003682999953, 30.77442081890999859, -0.2443071251729000137 ) ) ;
#1986=CARTESIAN_POINT ( 'NONE',  ( 0.7927445159862746005, 29.65171683346636300, 2.009466139971896492 ) ) ;
#1988=CARTESIAN_POINT ( 'NONE',  ( -2.042880948895999804, 25.38708707564000022, -0.7651981593944000570 ) ) ;
#1999=ORIENTED_EDGE ( 'NONE', *, *, #12962, .T. ) ;
#2002=AXIS2_PLACEMENT_3D ( 'NONE', #526, #8174, #6225 ) ;
#2003=ORIENTED_EDGE ( 'NONE', *, *, #2450, .F. ) ;
#2004=EDGE_CURVE ( 'NONE', #4259, #21619, #1735, .T. ) ;
#2009=FACE_OUTER_BOUND ( 'NONE', #12066, .T. ) ;
#2011=CARTESIAN_POINT ( 'NONE',  ( 0.000000000000000000, 24.29999999999999716, -2.750000000000000000 ) ) ;
#2014=CARTESIAN_POINT ( 'NONE',  ( -0.6556536848882291713, 30.36463005559760120, 2.057991541314201367 ) ) ;
#2019=CARTESIAN_POINT ( 'NONE',  ( 1.741868208726000011, 27.12196440326000157, 1.741868208726000011 ) ) ;
#2027=ORIENTED_EDGE ( 'NONE', *, *, #9911, .F. ) ;
#2033=CARTESIAN_POINT ( 'NONE',  ( 0.3592561569125999887, 29.66874352329000075, 2.314061945504000128 ) ) ;
#2035=CARTESIAN_POINT ( 'NONE',  ( -1.767114192125461614, 30.87940659144713962, -1.172702609216230485 ) ) ;
#2045=CARTESIAN_POINT ( 'NONE',  ( 1.962415512518493221, 29.05860578903570968, -0.9022275906645381705 ) ) ;
#2047=VERTEX_POINT ( 'NONE', #9661 ) ;
#2048=CARTESIAN_POINT ( 'NONE',  ( -1.671768471690028512, 23.69914749046346003, 1.453238603757796232 ) ) ;
#2050=CARTESIAN_POINT ( 'NONE',  ( 1.526497572355999921, 24.35926100756000068, -1.790937938634000082 ) ) ;
#2051=CARTESIAN_POINT ( 'NONE',  ( 1.259047450927256895, 28.26666666666667282, 2.184465970885639763 ) ) ;
#2052=CARTESIAN_POINT ( 'NONE',  ( -1.184521108792000010, 28.36049822781000174, -1.932944458086000017 ) ) ;
#2063=CARTESIAN_POINT ( 'NONE',  ( 1.779182944342999839, 23.89536342497000021, 1.512334087421999929 ) ) ;
#2068=CARTESIAN_POINT ( 'NONE',  ( -1.911670502565000040, 29.90524234017999916, -1.384813786399999858 ) ) ;
#2075=CARTESIAN_POINT ( 'NONE',  ( 0.6634078306992999829, 24.00000000000000000, -2.410371351092000403 ) ) ;
#2079=DIRECTION ( 'NONE',  ( 0.000000000000000000, 0.000000000000000000, -1.000000000000000000 ) ) ;
#2082=DIRECTION ( 'NONE',  ( 0.000000000000000000, -1.000000000000000000, 0.000000000000000000 ) ) ;
#2083=CARTESIAN_POINT ( 'NONE',  ( 2.628147087956000050, 27.85712896667000038, 0.4693273880717999669 ) ) ;
#2087=CARTESIAN_POINT ( 'NONE',  ( -2.100000000000000089, 18.89999999999999858, -1.955010042741999895E-10 ) ) ;
#2088=AXIS2_PLACEMENT_3D ( 'NONE', #1850, #2082, #3907 ) ;
#2089=CARTESIAN_POINT ( 'NONE',  ( 2.309807618587000011, 30.69019238141000017, -7.292675330123999428E-08 ) ) ;
#2091=CARTESIAN_POINT ( 'NONE',  ( 1.699999999999999956, 9.063113307333603430, 0.9835126878571698317 ) ) ;
#2097=CARTESIAN_POINT ( 'NONE',  ( -1.709564223436000008, 30.70248379823999940, -1.373128400647000147 ) ) ;
#2100=CARTESIAN_POINT ( 'NONE',  ( -0.1596195074772966960, 29.59450039907439844, 2.155456660100716793 ) ) ;
#2101=ORIENTED_EDGE ( 'NONE', *, *, #16355, .F. ) ;
#2102=CARTESIAN_POINT ( 'NONE',  ( 1.077617376005999938, 24.89850271714000129, 1.896742336415000008 ) ) ;
#2106=ORIENTED_EDGE ( 'NONE', *, *, #14833, .F. ) ;
#2108=CARTESIAN_POINT ( 'NONE',  ( 0.8814216895542995589, 30.38924864007917037, -2.379548453065109648 ) ) ;
#2109=ADVANCED_FACE ( 'NONE', ( #9541 ), #4653, .F. ) ;
#2115=VERTEX_POINT ( 'NONE', #8209 ) ;
#2118=AXIS2_PLACEMENT_3D ( 'NONE', #19864, #8964, #6539 ) ;
#2119=B_SPLINE_CURVE_WITH_KNOTS ( 'NONE', 3,
 ( #12252, #19992, #19639, #8736, #19763, #16343, #21578, #10673, #14529, #6911 ),
 .UNSPECIFIED., .F., .F.,
 ( 4, 2, 2, 2, 4 ),
 ( 0.000000000000000000, 0.2500000000000000000, 0.5000000000000000000, 0.7500000000000000000, 1.000000000000000000 ),
 .UNSPECIFIED. ) ;
#2123=DIRECTION ( 'NONE',  ( 0.000000000000000000, 1.000000000000000000, 0.000000000000000000 ) ) ;
#2124=DIRECTION ( 'NONE',  ( 0.000000000000000000, 1.000000000000000000, 0.000000000000000000 ) ) ;
#2126=FACE_BOUND ( 'NONE', #7482, .T. ) ;
#2127=CARTESIAN_POINT ( 'NONE',  ( -0.7985131490157234557, 30.35564972260119632, 2.010576473712321288 ) ) ;
#2128=ORIENTED_EDGE ( 'NONE', *, *, #12229, .T. ) ;
#2132=CARTESIAN_POINT ( 'NONE',  ( 2.500000000000001776, 27.81753006952333251, 0.3272492347489266429 ) ) ;
#2134=CARTESIAN_POINT ( 'NONE',  ( 2.193490157264000207, 25.62614211381999851, -0.6650079486841000698 ) ) ;
#2135=ADVANCED_FACE ( 'NONE', ( #8576 ), #23202, .T. ) ;
#2144=EDGE_CURVE ( 'NONE', #551, #18791, #8909, .T. ) ;
#2145=AXIS2_PLACEMENT_3D ( 'NONE', #20981, #620, #2700 ) ;
#2148=EDGE_CURVE ( 'NONE', #5466, #3402, #11260, .T. ) ;
#2152=FACE_BOUND ( 'NONE', #19736, .T. ) ;
#2154=DIRECTION ( 'NONE',  ( -1.000000000000000000, 0.000000000000000000, 0.000000000000000000 ) ) ;
#2156=CARTESIAN_POINT ( 'NONE',  ( 0.000000000000000000, 18.27087121525220681, 0.000000000000000000 ) ) ;
#2166=CARTESIAN_POINT ( 'NONE',  ( 1.834054417453000019, 26.41049822781000245, 1.332518472557000067 ) ) ;
#2167=DIRECTION ( 'NONE',  ( -1.000000000000000000, 0.000000000000000000, 0.000000000000000000 ) ) ;
#2175=ORIENTED_EDGE ( 'NONE', *, *, #6317, .F. ) ;
#2176=CARTESIAN_POINT ( 'NONE',  ( 0.9165514763390999464, 25.32691554002000345, 2.353385513049000011 ) ) ;
#2180=CARTESIAN_POINT ( 'NONE',  ( 1.582905715914000089, 28.79448331121999871, -2.003189615728000028 ) ) ;
#2185=CARTESIAN_POINT ( 'NONE',  ( -0.6543697108982035049, 29.66753006952333038, -2.434931691670788823 ) ) ;
#2186=ORIENTED_EDGE ( 'NONE', *, *, #15398, .F. ) ;
#2188=CARTESIAN_POINT ( 'NONE',  ( 0.000000000000000000, 20.00000000000000000, 0.000000000000000000 ) ) ;
#2189=ORIENTED_EDGE ( 'NONE', *, *, #3215, .T. ) ;
#2191=DIRECTION ( 'NONE',  ( 1.000000000000000000, 0.000000000000000000, 0.000000000000000000 ) ) ;
#2194=ORIENTED_EDGE ( 'NONE', *, *, #2450, .T. ) ;
#2197=CIRCLE ( 'NONE', #23072, 4.750000000000000000 ) ;
#2199=CARTESIAN_POINT ( 'NONE',  ( 2.644546391786999795, 26.29712896667000166, -0.3657850755363000195 ) ) ;
#2207=ORIENTED_EDGE ( 'NONE', *, *, #196, .F. ) ;
#2213=CARTESIAN_POINT ( 'NONE',  ( 2.066101926701000124, 28.83212126072000103, -0.7343076075657000157 ) ) ;
#2216=CARTESIAN_POINT ( 'NONE',  ( 0.9705800173758099003, 29.66328920622348164, 1.929470939684508446 ) ) ;
#2218=VECTOR ( 'NONE', #13396, 1000.000000000000000 ) ;
#2219=CARTESIAN_POINT ( 'NONE',  ( -0.8426916045660000076, 24.46137432145000190, -2.178369093381999910 ) ) ;
#2221=CARTESIAN_POINT ( 'NONE',  ( -1.500000000000000000, 8.900000000000000355, 0.000000000000000000 ) ) ;
#2225=EDGE_CURVE ( 'NONE', #19945, #23711, #22818, .T. ) ;
#2227=ORIENTED_EDGE ( 'NONE', *, *, #19457, .F. ) ;
#2228=CIRCLE ( 'NONE', #13834, 4.000000000000000000 ) ;
#2229=CARTESIAN_POINT ( 'NONE',  ( 0.000000000000000000, 24.50000000000000000, 4.618802153517000519 ) ) ;
#2231=EDGE_LOOP ( 'NONE', ( #561, #23771, #16258, #1932 ) ) ;
#2237=LINE ( 'NONE', #22463, #21144 ) ;
#2239=CARTESIAN_POINT ( 'NONE',  ( 2.171895212930905927, 26.39461574793667964, -0.7558918567651692344 ) ) ;
#2242=CARTESIAN_POINT ( 'NONE',  ( 2.161494655731827752, 30.60562575067124769, -0.02939362918790352705 ) ) ;
#2250=CARTESIAN_POINT ( 'NONE',  ( 2.249552142899000184, 25.59446440325999816, 0.5061648749511999945 ) ) ;
#2255=DIRECTION ( 'NONE',  ( 0.000000000000000000, -1.000000000000000000, 0.000000000000000000 ) ) ;
#2259=CARTESIAN_POINT ( 'NONE',  ( 1.120714571573853569, 28.16129399599262584, -1.892129278840122941 ) ) ;
#2264=EDGE_CURVE ( 'NONE', #12880, #7614, #15467, .T. ) ;
#2266=CARTESIAN_POINT ( 'NONE',  ( -2.949999988794999695, 24.49999998879500041, -5.832343010994999544E-08 ) ) ;
#2271=AXIS2_PLACEMENT_3D ( 'NONE', #12296, #1151, #13730 ) ;
#2273=VERTEX_POINT ( 'NONE', #5761 ) ;
#2275=CARTESIAN_POINT ( 'NONE',  ( 0.4693273880718999980, 26.57706776951999927, 2.628147087956000050 ) ) ;
#2279=CARTESIAN_POINT ( 'NONE',  ( 1.892954172570674443, 28.93993560461466430, 1.040653877296049856 ) ) ;
#2282=CARTESIAN_POINT ( 'NONE',  ( 4.724999978625000097, 14.90000002138000035, 2.519183602109999904E-09 ) ) ;
#2283=VECTOR ( 'NONE', #5334, 1000.000000000000114 ) ;
#2285=ADVANCED_FACE ( 'NONE', ( #5636 ), #13021, .T. ) ;
#2287=CARTESIAN_POINT ( 'NONE',  ( 2.070238309910999774, 25.66299822781000017, 0.4658180156273000194 ) ) ;
#2296=AXIS2_PLACEMENT_3D ( 'NONE', #19510, #17569, #10301 ) ;
#2301=EDGE_CURVE ( 'NONE', #19402, #8374, #11997, .T. ) ;
#2302=CARTESIAN_POINT ( 'NONE',  ( -0.3250653824660000302, 23.76728119616999635, 2.312349103826000007 ) ) ;
#2306=CARTESIAN_POINT ( 'NONE',  ( -2.067612397392999846, 29.79980770961000047, -1.497778068447999766 ) ) ;
#2311=ORIENTED_EDGE ( 'NONE', *, *, #8685, .F. ) ;
#2312=CARTESIAN_POINT ( 'NONE',  ( -1.835060406388425269, 24.49999999999985079, -3.559329533909751486 ) ) ;
#2313=DIRECTION ( 'NONE',  ( 1.160410698086937980E-09, 2.689654613662110334E-16, 1.000000000000000000 ) ) ;
#2315=CARTESIAN_POINT ( 'NONE',  ( 1.383873339091999943, 25.12749250491000197, 2.361535497914000192 ) ) ;
#2323=VERTEX_POINT ( 'NONE', #2011 ) ;
#2328=B_SPLINE_CURVE_WITH_KNOTS ( 'NONE', 3,
 ( #7721, #18622, #13278, #14853 ),
 .UNSPECIFIED., .F., .F.,
 ( 4, 4 ),
 ( 0.2478303497282951795, 0.2499810176238006776 ),
 .UNSPECIFIED. ) ;
#2330=ORIENTED_EDGE ( 'NONE', *, *, #16321, .T. ) ;
#2331=ADVANCED_FACE ( 'NONE', ( #11578, #9396 ), #20540, .T. ) ;
#2334=CARTESIAN_POINT ( 'NONE',  ( 0.000000000000000000, 21.89999999999999858, 0.000000000000000000 ) ) ;
#2336=B_SPLINE_CURVE_WITH_KNOTS ( 'NONE', 3,
 ( #16007, #9005, #1254, #5140, #21954, #17974, #3443, #6946, #16375, #2956, #6695, #16130 ),
 .UNSPECIFIED., .F., .F.,
 ( 4, 1, 1, 1, 1, 1, 1, 1, 1, 4 ),
 ( 0.000000000000000000, 0.03719136591632924566, 0.1695487139369214469, 0.3019060619569148285, 0.4342634099775076750, 0.5666207579975004460, 0.6989781060180932926, 0.8313354540380859525, 0.9636928020586794652, 1.000000000000000000 ),
 .UNSPECIFIED. ) ;
#2338=CARTESIAN_POINT ( 'NONE',  ( 2.306909816657999990, 30.44805800497999826, -0.4795071306118000032 ) ) ;
#2340=CARTESIAN_POINT ( 'NONE',  ( 0.2739778719191235945, 29.61987499151109304, 2.142736234137259999 ) ) ;
#2341=ORIENTED_EDGE ( 'NONE', *, *, #9075, .T. ) ;
#2342=CARTESIAN_POINT ( 'NONE',  ( -2.162054140341999720, 23.60745938542000388, 0.3218784743804999904 ) ) ;
#2345=CARTESIAN_POINT ( 'NONE',  ( -1.395367521490594731, 24.57895749046196343, -1.860951888388887143 ) ) ;
#2353=CARTESIAN_POINT ( 'NONE',  ( 3.000000000000000000, 15.09999999999999964, 0.000000000000000000 ) ) ;
#2362=DIRECTION ( 'NONE',  ( 1.000000000000000000, 0.000000000000000000, 0.000000000000000000 ) ) ;
#2363=EDGE_CURVE ( 'NONE', #3402, #12394, #8689, .T. ) ;
#2364=CARTESIAN_POINT ( 'NONE',  ( 0.5181440266930791294, 30.43466978169055182, 2.096986438083043858 ) ) ;
#2365=ORIENTED_EDGE ( 'NONE', *, *, #15909, .T. ) ;
#2371=CARTESIAN_POINT ( 'NONE',  ( -1.743177805438000050, 26.69864211382000008, -1.488814495283000028 ) ) ;
#2378=LINE ( 'NONE', #23070, #4525 ) ;
#2384=CARTESIAN_POINT ( 'NONE',  ( 0.000000000000000000, 17.00000000000000000, 0.000000000000000000 ) ) ;
#2387=CARTESIAN_POINT ( 'NONE',  ( 2.434931691670791487, 27.00086340285667319, 0.6543697108981911814 ) ) ;
#2389=EDGE_CURVE ( 'NONE', #16978, #15685, #5755, .T. ) ;
#2391=DIRECTION ( 'NONE',  ( 0.000000000000000000, 0.000000000000000000, -1.000000000000000000 ) ) ;
#2394=CARTESIAN_POINT ( 'NONE',  ( 0.5485649090616000478, 28.98206776952000041, 2.437990915149000237 ) ) ;
#2396=CARTESIAN_POINT ( 'NONE',  ( 2.066277796575604953, 28.96607617505452836, 0.6292312681296344801 ) ) ;
#2401=FACE_OUTER_BOUND ( 'NONE', #16062, .T. ) ;
#2402=CARTESIAN_POINT ( 'NONE',  ( -1.289728978252000058, 28.25506359723999950, -2.104626470933999904 ) ) ;
#2405=DIRECTION ( 'NONE',  ( 0.000000000000000000, 0.7071067811866525998, -0.7071067811864425456 ) ) ;
#2410=EDGE_CURVE ( 'NONE', #16380, #6198, #13737, .T. ) ;
#2413=CARTESIAN_POINT ( 'NONE',  ( 1.032299669828999900, 30.21051138681000126, -2.520645439494999973 ) ) ;
#2414=CARTESIAN_POINT ( 'NONE',  ( 0.8975247896630000888, 23.72588767999999959, 2.360713936347000441 ) ) ;
#2422=EDGE_CURVE ( 'NONE', #14961, #12189, #10707, .T. ) ;
#2424=DIRECTION ( 'NONE',  ( 0.000000000000000000, -1.000000000000000000, 0.000000000000000000 ) ) ;
#2431=FACE_OUTER_BOUND ( 'NONE', #1149, .T. ) ;
#2433=CARTESIAN_POINT ( 'NONE',  ( -1.269269236459868555, 23.68265782431019773, -1.789285403925672036 ) ) ;
#2434=ADVANCED_FACE ( 'NONE', ( #19325 ), #5951, .T. ) ;
#2438=CARTESIAN_POINT ( 'NONE',  ( -1.150230160948066294, 26.50000000000000711, 2.153661957585351505 ) ) ;
#2450=EDGE_CURVE ( 'NONE', #4848, #9355, #11382, .T. ) ;
#2451=CARTESIAN_POINT ( 'NONE',  ( 0.1768883900467000114, 30.19892465351999888, 2.185563631071000046 ) ) ;
#2455=CARTESIAN_POINT ( 'NONE',  ( 1.625795934526099940, 29.71217265414515651, 1.423553400153898085 ) ) ;
#2456=ORIENTED_EDGE ( 'NONE', *, *, #21732, .T. ) ;
#2457=CARTESIAN_POINT ( 'NONE',  ( -0.06890087385339001280, 24.58462810240999730, 2.184803246612999850 ) ) ;
#2461=CARTESIAN_POINT ( 'NONE',  ( -2.100000000000000089, 19.00000000000000000, 0.000000000000000000 ) ) ;
#2462=EDGE_CURVE ( 'NONE', #2559, #19778, #13680, .T. ) ;
#2463=CARTESIAN_POINT ( 'NONE',  ( -2.153985071724999756, 30.83999999999999986, 0.1610847937796999751 ) ) ;
#2468=VERTEX_POINT ( 'NONE', #8301 ) ;
#2474=CARTESIAN_POINT ( 'NONE',  ( 0.000000000000000000, 30.84509624898000268, 0.000000000000000000 ) ) ;
#2475=CARTESIAN_POINT ( 'NONE',  ( 3.000000000000000000, 17.89999999999999858, 0.000000000000000000 ) ) ;
#2484=CARTESIAN_POINT ( 'NONE',  ( 0.6543697108981985089, 28.00086340285666964, -2.434931691670790599 ) ) ;
#2485=CARTESIAN_POINT ( 'NONE',  ( 1.613055828956475368, 30.51051290257240822, 1.451212359496641291 ) ) ;
#2491=CARTESIAN_POINT ( 'NONE',  ( 1.990650851275000299, 25.56196440326000285, 1.014287269782000012 ) ) ;
#2494=CARTESIAN_POINT ( 'NONE',  ( 0.000000000000000000, 26.35000000000000142, 0.000000000000000000 ) ) ;
#2496=CARTESIAN_POINT ( 'NONE',  ( -2.999999956181000016, 17.90000004382000043, 2.609181505839000138E-08 ) ) ;
#2504=CARTESIAN_POINT ( 'NONE',  ( 2.000000000000198508, 24.49999999999999645, -3.464101615138341028 ) ) ;
#2507=CARTESIAN_POINT ( 'NONE',  ( -2.015949060104638590, 30.88564367501877683, -0.6669719759398144987 ) ) ;
#2510=CARTESIAN_POINT ( 'NONE',  ( 0.000000000000000000, -1.550000000000000044, 0.000000000000000000 ) ) ;
#2512=DIRECTION ( 'NONE',  ( 0.000000000000000000, 1.000000000000000000, 0.000000000000000000 ) ) ;
#2513=CARTESIAN_POINT ( 'NONE',  ( 0.5721489135196999865, 28.52706776951999856, -2.607696352436000176 ) ) ;
#2516=CARTESIAN_POINT ( 'NONE',  ( 2.125811182162558932, 28.98043553802446937, 0.3935857075586116638 ) ) ;
#2534=CARTESIAN_POINT ( 'NONE',  ( -2.519435264877999625, 25.07075108241999928, -0.1759572809729000042 ) ) ;
#2539=CARTESIAN_POINT ( 'NONE',  ( 2.701604807922000084, 30.19703527822999689, -0.4899141053905000653 ) ) ;
#2543=DIRECTION ( 'NONE',  ( 0.000000000000000000, 0.000000000000000000, -1.000000000000000000 ) ) ;
#2544=CARTESIAN_POINT ( 'NONE',  ( 0.000000000000000000, 16.89999999999999858, 0.000000000000000000 ) ) ;
#2545=FACE_OUTER_BOUND ( 'NONE', #14555, .T. ) ;
#2549=ORIENTED_EDGE ( 'NONE', *, *, #9120, .F. ) ;
#2552=CARTESIAN_POINT ( 'NONE',  ( -2.103837132995996839, 23.84009889363539259, 0.6191421011388187345 ) ) ;
#2557=CARTESIAN_POINT ( 'NONE',  ( -2.449293598294692609E-16, 9.100092063578999912, 1.999999999999988676 ) ) ;
#2559=VERTEX_POINT ( 'NONE', #18913 ) ;
#2562=DIRECTION ( 'NONE',  ( -0.000000000000000000, 1.000000000000000000, 0.000000000000000000 ) ) ;
#2565=CARTESIAN_POINT ( 'NONE',  ( 0.000000000000000000, 7.100000000000000533, 0.000000000000000000 ) ) ;
#2574=DIRECTION ( 'NONE',  ( 0.000000000000000000, -1.000000000000000000, 0.000000000000000000 ) ) ;
#2575=CARTESIAN_POINT ( 'NONE',  ( -1.521839280563020536, 29.50435537852937529, 1.532609397753554648 ) ) ;
#2576=ORIENTED_EDGE ( 'NONE', *, *, #14807, .F. ) ;
#2577=AXIS2_PLACEMENT_3D ( 'NONE', #8303, #2736, #23301 ) ;
#2578=CARTESIAN_POINT ( 'NONE',  ( 2.108233021187000400, 25.66491687433000024, -0.7394748174873000401 ) ) ;
#2587=EDGE_CURVE ( 'NONE', #5160, #16051, #19089, .T. ) ;
#2590=CARTESIAN_POINT ( 'NONE',  ( 0.3272492347489343589, 26.98333333333333428, -2.500000000000000444 ) ) ;
#2592=EDGE_LOOP ( 'NONE', ( #52, #23233, #244 ) ) ;
#2593=DIRECTION ( 'NONE',  ( 0.000000000000000000, -1.000000000000000000, 0.000000000000000000 ) ) ;
#2598=AXIS2_PLACEMENT_3D ( 'NONE', #11856, #17802, #4840 ) ;
#2599=DIRECTION ( 'NONE',  ( 0.000000000000000000, -1.000000000000000000, 0.000000000000000000 ) ) ;
#2600=CARTESIAN_POINT ( 'NONE',  ( 0.000000000000000000, 18.00000000000000000, 0.000000000000000000 ) ) ;
#2602=ADVANCED_FACE ( 'NONE', ( #3668 ), #16397, .T. ) ;
#2607=FACE_OUTER_BOUND ( 'NONE', #7377, .T. ) ;
#2609=CARTESIAN_POINT ( 'NONE',  ( -2.159859212911454662, 30.20451953216726082, 0.01416237932336155032 ) ) ;
#2610=ORIENTED_EDGE ( 'NONE', *, *, #22703, .T. ) ;
#2617=AXIS2_PLACEMENT_3D ( 'NONE', #21150, #7203, #8679 ) ;
#2618=B_SPLINE_CURVE_WITH_KNOTS ( 'NONE', 3,
 ( #8427, #19448, #15910, #23300, #17876, #6715, #21502, #1277, #8662, #21628 ),
 .UNSPECIFIED., .F., .F.,
 ( 4, 1, 1, 2, 2, 4 ),
 ( 0.000000000000000000, 0.2499999999999986677, 0.3749999999999980016, 0.4374999999999982236, 0.4999999999999984457, 1.000000000000000000 ),
 .UNSPECIFIED. ) ;
#2623=DIRECTION ( 'NONE',  ( 1.000000000000000000, 0.000000000000000000, 0.000000000000000000 ) ) ;
#2624=CARTESIAN_POINT ( 'NONE',  ( 2.999999998122344191, 21.89999999999998437, 6.187284373140837446E-09 ) ) ;
#2626=CARTESIAN_POINT ( 'NONE',  ( 0.000000000000000000, 22.00000000000000000, 0.000000000000000000 ) ) ;
#2631=CARTESIAN_POINT ( 'NONE',  ( 3.000000000000000000, 22.00000000000000000, 0.000000000000000000 ) ) ;
#2634=CARTESIAN_POINT ( 'NONE',  ( -4.000000000000000888, 26.42936170367563520, -1.090349405812125916 ) ) ;
#2635=AXIS2_PLACEMENT_3D ( 'NONE', #11556, #20633, #272 ) ;
#2636=CARTESIAN_POINT ( 'NONE',  ( 2.500000000000001776, 27.01753006952333180, 0.3272492347489266429 ) ) ;
#2640=ORIENTED_EDGE ( 'NONE', *, *, #1705, .F. ) ;
#2642=CARTESIAN_POINT ( 'NONE',  ( -1.733846816785000078, 27.84456776952000112, -2.030073792688000367 ) ) ;
#2644=CARTESIAN_POINT ( 'NONE',  ( 2.155020325414803040, 28.99531748523413910, 0.1450810396632776778 ) ) ;
#2646=PRODUCT_DEFINITION ( 'UNKNOWN', '', #13660, #8910 ) ;
#2659=VECTOR ( 'NONE', #23963, 1000.000000000000000 ) ;
#2662=CARTESIAN_POINT ( 'NONE',  ( 2.483627104365000005, 30.80612887107999853, 1.118432463241999963 ) ) ;
#2663=CARTESIAN_POINT ( 'NONE',  ( -1.962698410735999488, 24.36629882400999847, 1.589443273402000090 ) ) ;
#2670=CARTESIAN_POINT ( 'NONE',  ( 0.2870741741112000089, 28.76085756624999945, -2.730617656758999701 ) ) ;
#2673=CARTESIAN_POINT ( 'NONE',  ( 0.000000000000000000, 13.00000000000000000, 0.000000000000000000 ) ) ;
#2677=CARTESIAN_POINT ( 'NONE',  ( 1.259047450927247569, 29.56753006952333607, -2.184465970885645536 ) ) ;
#2678=ORIENTED_EDGE ( 'NONE', *, *, #5292, .F. ) ;
#2679=CARTESIAN_POINT ( 'NONE',  ( 2.309807618587000011, 30.69019238141000017, -7.292675330123999428E-08 ) ) ;
#2680=CARTESIAN_POINT ( 'NONE',  ( 0.7867367962552690441, 24.50000000000000000, -2.267387309971103271 ) ) ;
#2684=CARTESIAN_POINT ( 'NONE',  ( 2.184465970885652641, 28.56753006952332186, 1.259047450927233580 ) ) ;
#2686=AXIS2_PLACEMENT_3D ( 'NONE', #21442, #4856, #12121 ) ;
#2689=VECTOR ( 'NONE', #3314, 1000.000000000000114 ) ;
#2690=CARTESIAN_POINT ( 'NONE',  ( -1.626917502017769523, 26.50000000000000355, 1.884902535258590195 ) ) ;
#2693=VERTEX_POINT ( 'NONE', #251 ) ;
#2696=CARTESIAN_POINT ( 'NONE',  ( -1.888459278277104156E-11, 26.49469377355791977, -2.394693773557865057 ) ) ;
#2700=DIRECTION ( 'NONE',  ( 0.000000000000000000, 0.000000000000000000, -1.000000000000000000 ) ) ;
#2707=EDGE_CURVE ( 'NONE', #19991, #903, #9590, .T. ) ;
#2708=CARTESIAN_POINT ( 'NONE',  ( -2.063376835572392487, 29.44210936106684429, 0.6381193817384768208 ) ) ;
#2710=CARTESIAN_POINT ( 'NONE',  ( 2.243357345374999756, 25.64165095250000093, -0.3542371386884999862 ) ) ;
#2713=ORIENTED_EDGE ( 'NONE', *, *, #2867, .F. ) ;
#2723=CARTESIAN_POINT ( 'NONE',  ( 2.164939593608601776, 24.49999999999984368, -3.368873696368142490 ) ) ;
#2730=EDGE_CURVE ( 'NONE', #16405, #2468, #1322, .T. ) ;
#2736=DIRECTION ( 'NONE',  ( 0.000000000000000000, 1.000000000000000000, 0.000000000000000000 ) ) ;
#2737=EDGE_CURVE ( 'NONE', #10311, #22357, #3267, .T. ) ;
#2738=CARTESIAN_POINT ( 'NONE',  ( -1.850862556816144755, 30.13458432399187004, -1.117312800271740736 ) ) ;
#2739=ORIENTED_EDGE ( 'NONE', *, *, #6904, .T. ) ;
#2744=CARTESIAN_POINT ( 'NONE',  ( -0.6543697108981929578, 27.60086340285666751, 2.434931691670791487 ) ) ;
#2745=CARTESIAN_POINT ( 'NONE',  ( 1.640193969998194001, 24.74015355458762144, 1.405240085690787843 ) ) ;
#2748=VERTEX_POINT ( 'NONE', #978 ) ;
#2752=CARTESIAN_POINT ( 'NONE',  ( -1.960246057973615619, 27.56955929831042695, -0.9957143590686239332 ) ) ;
#2753=CIRCLE ( 'NONE', #13178, 4.000000000000000000 ) ;
#2756=ORIENTED_EDGE ( 'NONE', *, *, #9269, .T. ) ;
#2763=CARTESIAN_POINT ( 'NONE',  ( -4.000000000000000888, 26.46241504948188705, -0.8002143650531428065 ) ) ;
#2768=CARTESIAN_POINT ( 'NONE',  ( -0.7744564004552000336, 28.91706776952000268, 2.554499528901000183 ) ) ;
#2770=CARTESIAN_POINT ( 'NONE',  ( 3.268181200173221335, 26.37490599056235752, 2.731916857836432566 ) ) ;
#2776=LINE ( 'NONE', #824, #20916 ) ;
#2777=ADVANCED_FACE ( 'NONE', ( #6557 ), #4028, .T. ) ;
#2781=FACE_OUTER_BOUND ( 'NONE', #22912, .T. ) ;
#2785=CARTESIAN_POINT ( 'NONE',  ( -2.184465970885641539, 27.26666666666667282, 1.259047450927253120 ) ) ;
#2787=EDGE_LOOP ( 'NONE', ( #19107, #22750, #17271, #10372 ) ) ;
#2789=CARTESIAN_POINT ( 'NONE',  ( 1.487891794119999833, 30.63451452002999886, 2.049709317120999685 ) ) ;
#2791=CARTESIAN_POINT ( 'NONE',  ( -1.627763130269000103, 23.49237082063000059, 2.174264886728999979 ) ) ;
#2797=CARTESIAN_POINT ( 'NONE',  ( -1.330185344530000036, 29.90979973582999918, 2.401934960883000070 ) ) ;
#2804=ORIENTED_EDGE ( 'NONE', *, *, #12744, .T. ) ;
#2806=CARTESIAN_POINT ( 'NONE',  ( 1.626104829127729801, 24.49999999999998224, -1.886740530527200255 ) ) ;
#2808=CARTESIAN_POINT ( 'NONE',  ( -2.569316494495999859, 25.61518446159000106, -0.9436992233395999907 ) ) ;
#2812=CARTESIAN_POINT ( 'NONE',  ( 1.699999999999999956, 10.36668268731399856, -1.053571508039081506 ) ) ;
#2817=CARTESIAN_POINT ( 'NONE',  ( -2.500000000000000000, 29.83419673618999823, 0.000000000000000000 ) ) ;
#2821=VERTEX_POINT ( 'NONE', #17210 ) ;
#2822=CARTESIAN_POINT ( 'NONE',  ( 1.740781276729051363, 12.98239425167962935, -1.065112122026150798 ) ) ;
#2826=CARTESIAN_POINT ( 'NONE',  ( 2.394884942776999814, 23.89488494277999919, 0.000000000000000000 ) ) ;
#2830=CARTESIAN_POINT ( 'NONE',  ( 0.000000000000000000, 7.100000000000000533, 0.000000000000000000 ) ) ;
#2831=CARTESIAN_POINT ( 'NONE',  ( -1.845878792324959550, 29.47323799381988962, 1.121740158063918358 ) ) ;
#2833=CARTESIAN_POINT ( 'NONE',  ( -0.7886471129774000888, 24.23563927490999603, -2.038663358203999909 ) ) ;
#2836=CARTESIAN_POINT ( 'NONE',  ( -1.511391232157798692, 24.58424253752448152, -1.760983478933511925 ) ) ;
#2843=CARTESIAN_POINT ( 'NONE',  ( -1.672509921847626257, 24.50639765414753057, -3.652834497694422033 ) ) ;
#2845=ADVANCED_FACE ( 'NONE', ( #8258, #15868 ), #19144, .F. ) ;
#2847=CARTESIAN_POINT ( 'NONE',  ( 4.000000000000000000, 26.50000000000000711, -0.3708744353061897980 ) ) ;
#2849=DIRECTION ( 'NONE',  ( 0.000000000000000000, 0.000000000000000000, 1.000000000000000000 ) ) ;
#2855=DIRECTION ( 'NONE',  ( 0.000000000000000000, 0.000000000000000000, -1.000000000000000000 ) ) ;
#2858=CARTESIAN_POINT ( 'NONE',  ( -1.115914872543483538, 30.33458863209825296, 1.849708372149318381 ) ) ;
#2859=ORIENTED_EDGE ( 'NONE', *, *, #11485, .F. ) ;
#2862=DIRECTION ( 'NONE',  ( 0.000000000000000000, -1.000000000000000000, 0.000000000000000000 ) ) ;
#2865=CARTESIAN_POINT ( 'NONE',  ( -2.000000000000000000, 24.50000000000000000, -3.464101615137999968 ) ) ;
#2866=ORIENTED_EDGE ( 'NONE', *, *, #10142, .T. ) ;
#2867=EDGE_CURVE ( 'NONE', #1813, #22702, #21828, .T. ) ;
#2869=CIRCLE ( 'NONE', #914, 1.399999999999999911 ) ;
#2871=CARTESIAN_POINT ( 'NONE',  ( -0.04320196544907554947, 27.02713582543505666, 2.171338851202412989 ) ) ;
#2873=CARTESIAN_POINT ( 'NONE',  ( 0.000000000000000000, 17.00000000000000000, 0.000000000000000000 ) ) ;
#2874=EDGE_CURVE ( 'NONE', #18875, #13184, #2896, .T. ) ;
#2876=DIRECTION ( 'NONE',  ( -1.000000000000000000, 0.000000000000000000, 0.000000000000000000 ) ) ;
#2878=AXIS2_PLACEMENT_3D ( 'NONE', #8181, #8426, #8059 ) ;
#2883=CARTESIAN_POINT ( 'NONE',  ( -0.9392386595127586446, 28.45998959359454972, -1.999008173069681371 ) ) ;
#2889=AXIS2_PLACEMENT_3D ( 'NONE', #6465, #14221, #15898 ) ;
#2891=CARTESIAN_POINT ( 'NONE',  ( -1.978081431919000099, 28.60869850838000161, 1.107772814030999919 ) ) ;
#2892=CARTESIAN_POINT ( 'NONE',  ( 4.000000000000000000, 26.20000000000000284, 2.309401076759000304 ) ) ;
#2893=CARTESIAN_POINT ( 'NONE',  ( -1.590840130251000017, 27.70437716036000353, -1.862634475845999837 ) ) ;
#2895=ORIENTED_EDGE ( 'NONE', *, *, #7191, .F. ) ;
#2896=B_SPLINE_CURVE_WITH_KNOTS ( 'NONE', 3,
 ( #1702, #19883, #12730, #1229, #10563, #21930, #23376, #16106, #23510, #6794, #14536, #5230, #23853, #4873, #7145, #3298, #3058, #8870 ),
 .UNSPECIFIED., .F., .F.,
 ( 4, 2, 2, 2, 2, 2, 2, 2, 4 ),
 ( 0.000000000000000000, 0.1250000000000000555, 0.2500000000000001110, 0.3750000000000000555, 0.5000000000000000000, 0.6249999999999998890, 0.7499999999999998890, 0.8749999999999998890, 1.000000000000000000 ),
 .UNSPECIFIED. ) ;
#2900=AXIS2_PLACEMENT_3D ( 'NONE', #8275, #6448, #4518 ) ;
#2901=CARTESIAN_POINT ( 'NONE',  ( -1.802851389305008434, 26.49891402983596222, 1.731858503842447217 ) ) ;
#2906=CARTESIAN_POINT ( 'NONE',  ( 0.6634078306992999829, 24.00000000000000000, -2.410371351092000403 ) ) ;
#2909=VERTEX_POINT ( 'NONE', #12615 ) ;
#2911=CARTESIAN_POINT ( 'NONE',  ( 0.2527145128676999697, 30.46290016897999919, 2.328107194952999670 ) ) ;
#2916=DIRECTION ( 'NONE',  ( -1.000000000000000000, 0.000000000000000000, 0.000000000000000000 ) ) ;
#2917=CARTESIAN_POINT ( 'NONE',  ( 2.545098575468000224, 30.12522639263000102, 1.030125257387999982 ) ) ;
#2919=FACE_BOUND ( 'NONE', #7529, .T. ) ;
#2920=EDGE_CURVE ( 'NONE', #8124, #12420, #16240, .T. ) ;
#2923=DIRECTION ( 'NONE',  ( 1.000000000000000000, 0.000000000000000000, 0.000000000000000000 ) ) ;
#2924=CARTESIAN_POINT ( 'NONE',  ( 4.649999999999999467, 15.00000000000000000, 0.000000000000000000 ) ) ;
#2925=ORIENTED_EDGE ( 'NONE', *, *, #3934, .F. ) ;
#2927=ORIENTED_EDGE ( 'NONE', *, *, #11455, .T. ) ;
#2928=CARTESIAN_POINT ( 'NONE',  ( -0.7063789491035000756, 25.71876066959000084, 2.445197883720000132 ) ) ;
#2931=AXIS2_PLACEMENT_3D ( 'NONE', #12827, #20330, #14634 ) ;
#2932=CARTESIAN_POINT ( 'NONE',  ( 0.000000000000000000, 13.00000000000000000, 0.000000000000000000 ) ) ;
#2933=DIRECTION ( 'NONE',  ( 0.000000000000000000, 0.000000000000000000, -1.000000000000000000 ) ) ;
#2935=CARTESIAN_POINT ( 'NONE',  ( 1.259047450927257339, 30.10086340285667106, 2.184465970885639763 ) ) ;
#2936=CARTESIAN_POINT ( 'NONE',  ( -0.1017505424761079302, 26.49824549261836992, -2.396632052897438303 ) ) ;
#2937=LINE ( 'NONE', #8265, #21043 ) ;
#2938=ORIENTED_EDGE ( 'NONE', *, *, #4806, .T. ) ;
#2945=CARTESIAN_POINT ( 'NONE',  ( 0.000000000000000000, 24.80000000000000426, 4.618802153517000519 ) ) ;
#2948=ORIENTED_EDGE ( 'NONE', *, *, #2410, .T. ) ;
#2949=AXIS2_PLACEMENT_3D ( 'NONE', #10733, #23563, #8799 ) ;
#2951=CARTESIAN_POINT ( 'NONE',  ( -1.668398882160119889, 29.31622934884095244, -1.371800779754721145 ) ) ;
#2952=ORIENTED_EDGE ( 'NONE', *, *, #19783, .T. ) ;
#2956=CARTESIAN_POINT ( 'NONE',  ( 2.461510100158181391, 30.03430034141290150, -0.6707223322621249650 ) ) ;
#2962=CARTESIAN_POINT ( 'NONE',  ( 2.504532394112000003E-14, 28.43419673618999965, 2.500000000000000000 ) ) ;
#2976=CARTESIAN_POINT ( 'NONE',  ( -1.681629395837270557, 30.11728915368498605, -1.356799994207296800 ) ) ;
#2978=CARTESIAN_POINT ( 'NONE',  ( 2.096382098643999825, 25.85732963143999896, -0.7353180384705999550 ) ) ;
#2982=CARTESIAN_POINT ( 'NONE',  ( -1.199159982883566622, 23.61694849536621987, -1.744592755163365094 ) ) ;
#2983=VERTEX_POINT ( 'NONE', #21816 ) ;
#2984=ADVANCED_FACE ( 'NONE', ( #20000 ), #18074, .T. ) ;
#2985=CARTESIAN_POINT ( 'NONE',  ( 2.207668724461689713, 24.00469357743359566, 0.4510245842454297938 ) ) ;
#2987=B_SPLINE_CURVE_WITH_KNOTS ( 'NONE', 3,
 ( #20817, #9321, #22387, #13295 ),
 .UNSPECIFIED., .F., .F.,
 ( 4, 4 ),
 ( 0.000000000000000000, 1.000000000000000000 ),
 .UNSPECIFIED. ) ;
#2991=CARTESIAN_POINT ( 'NONE',  ( 0.000000000000000000, 7.000000000000000000, 0.000000000000000000 ) ) ;
#2992=CIRCLE ( 'NONE', #16511, 4.750000000000000000 ) ;
#2998=EDGE_CURVE ( 'NONE', #22108, #4259, #12657, .T. ) ;
#3005=DIRECTION ( 'NONE',  ( 0.000000000000000000, -1.000000000000000000, 0.000000000000000000 ) ) ;
#3007=CARTESIAN_POINT ( 'NONE',  ( -1.655756533096874872, 28.51299189722077898, -1.457120583913508183 ) ) ;
#3008=CARTESIAN_POINT ( 'NONE',  ( 2.160826008357635164, 26.50000000000000355, -3.371248675920325955 ) ) ;
#3012=CARTESIAN_POINT ( 'NONE',  ( 1.664720809480999986, 27.43869850838000346, -1.538852087555999892 ) ) ;
#3017=B_SPLINE_CURVE_WITH_KNOTS ( 'NONE', 3,
 ( #23129, #19521, #15620, #11651, #23009, #9705, #17328, #21210, #4495, #15256, #4625, #4377, #6426, #8138, #19022, #17581, #21333, #19140, #15503, #22890, #17088, #486, #13811, #7888, #22648, #974, #8376, #2552, #6058, #9823, #20851, #15742, #2433, #6554 ),
 .UNSPECIFIED., .F., .F.,
 ( 4, 2, 2, 2, 2, 2, 2, 2, 2, 2, 2, 2, 2, 2, 2, 2, 4 ),
 ( 0.4963961610726058127, 0.5278714010055679529, 0.5593466409385301485, 0.5908218808714922332, 0.6222971208044543179, 0.6537723607374165136, 0.6852476006703787093, 0.7167228406033407939, 0.7481980805363028786, 0.7796733204692650743, 0.8111485604022272700, 0.8426238003351893546, 0.8740990402681514393, 0.9055742802011136350, 0.9370495201340758307, 0.9685247600670379153, 1.000000000000000000 ),
 .UNSPECIFIED. ) ;
#3027=CARTESIAN_POINT ( 'NONE',  ( 2.000000000000000000, 31.00000000000000000, 0.000000000000000000 ) ) ;
#3028=CIRCLE ( 'NONE', #15375, 2.500000000000000000 ) ;
#3030=DIRECTION ( 'NONE',  ( 0.000000000000000000, -1.000000000000000000, 0.000000000000000000 ) ) ;
#3031=ORIENTED_EDGE ( 'NONE', *, *, #11401, .F. ) ;
#3032=CARTESIAN_POINT ( 'NONE',  ( -2.270871215252209030, 18.00000000000000000, 0.000000000000000000 ) ) ;
#3033=CARTESIAN_POINT ( 'NONE',  ( -2.332700628984000435, 30.30361591766000018, -0.9867309859219000057 ) ) ;
#3034=CARTESIAN_POINT ( 'NONE',  ( -2.474225017569000151, 23.42832970622999866, 1.120252420451000042 ) ) ;
#3039=DIRECTION ( 'NONE',  ( 9.309561455062000780E-11, 0.000000000000000000, -1.000000000000000000 ) ) ;
#3040=VECTOR ( 'NONE', #22225, 1000.000000000000114 ) ;
#3049=ORIENTED_EDGE ( 'NONE', *, *, #3923, .F. ) ;
#3051=EDGE_CURVE ( 'NONE', #23046, #4988, #17687, .T. ) ;
#3054=CARTESIAN_POINT ( 'NONE',  ( -0.04357916811771000293, 24.95238759480999846, 2.544809683028999903 ) ) ;
#3055=CYLINDRICAL_SURFACE ( 'NONE', #6999, 2.500000000000000000 ) ;
#3058=CARTESIAN_POINT ( 'NONE',  ( -2.500000000000000444, 27.98333333333333428, -0.3272492347489320275 ) ) ;
#3059=CIRCLE ( 'NONE', #19688, 4.750000000000000000 ) ;
#3063=ADVANCED_FACE ( 'NONE', ( #7498 ), #9208, .T. ) ;
#3067=CARTESIAN_POINT ( 'NONE',  ( 0.4755391251864483082, 26.25858828695499270, 2.107219116345798948 ) ) ;
#3068=CARTESIAN_POINT ( 'NONE',  ( -3.999895459877826465, 24.70780860099995380, 1.909390889640791622 ) ) ;
#3074=CARTESIAN_POINT ( 'NONE',  ( -0.3656491329547000291, 28.60167447434999843, 2.243838195847999817 ) ) ;
#3078=DIRECTION ( 'NONE',  ( 0.000000000000000000, -1.000000000000000000, 0.000000000000000000 ) ) ;
#3079=CIRCLE ( 'NONE', #17767, 4.000000000000000000 ) ;
#3080=CARTESIAN_POINT ( 'NONE',  ( -1.053212785059553180, 29.53888443595877789, 1.885826740177577676 ) ) ;
#3084=AXIS2_PLACEMENT_3D ( 'NONE', #2384, #6135, #14972 ) ;
#3088=AXIS2_PLACEMENT_3D ( 'NONE', #4126, #597, #15497 ) ;
#3091=EDGE_CURVE ( 'NONE', #18033, #6675, #9446, .T. ) ;
#3094=CARTESIAN_POINT ( 'NONE',  ( 0.000000000000000000, -1.550000000000000044, 0.000000000000000000 ) ) ;
#3095=CARTESIAN_POINT ( 'NONE',  ( 0.000000000000000000, 18.00000000000000000, 0.000000000000000000 ) ) ;
#3098=CARTESIAN_POINT ( 'NONE',  ( 0.000000000000000000, 13.04999996922999905, 0.000000000000000000 ) ) ;
#3105=CARTESIAN_POINT ( 'NONE',  ( 0.000000000000000000, 17.89999999999999858, 0.000000000000000000 ) ) ;
#3109=CARTESIAN_POINT ( 'NONE',  ( -2.158863305921206344, 30.19885671959407603, -0.08137547947002730930 ) ) ;
#3111=CARTESIAN_POINT ( 'NONE',  ( -2.187279742372999713, 25.36874527294000359, -0.8192853498630000564 ) ) ;
#3114=DIRECTION ( 'NONE',  ( 0.000000000000000000, -0.7071067811866525998, -0.7071067811864425456 ) ) ;
#3123=CIRCLE ( 'NONE', #1944, 3.000000000000000000 ) ;
#3124=CARTESIAN_POINT ( 'NONE',  ( -1.921811817508991993, 26.76825189519908577, -1.007139915559144283 ) ) ;
#3127=ORIENTED_EDGE ( 'NONE', *, *, #18558, .F. ) ;
#3135=CARTESIAN_POINT ( 'NONE',  ( -1.211852003089728846, 27.92996655705957920, 1.828385414783800567 ) ) ;
#3141=CARTESIAN_POINT ( 'NONE',  ( 0.4658180156273000194, 28.77119850838000303, 2.070238309910999774 ) ) ;
#3142=CARTESIAN_POINT ( 'NONE',  ( 2.321186682587942141, 26.50000000000000355, 3.278664397485417492 ) ) ;
#3143=EDGE_CURVE ( 'NONE', #20723, #6198, #3615, .T. ) ;
#3144=CARTESIAN_POINT ( 'NONE',  ( -0.7105796827303000329, 28.77687716036000154, 2.343805879471000164 ) ) ;
#3152=CARTESIAN_POINT ( 'NONE',  ( -1.592810637863762091, 30.55640641325078377, -1.866744843515978802 ) ) ;
#3159=CARTESIAN_POINT ( 'NONE',  ( 2.066640458449999773, 30.83305368145999736, -1.464273823065999958 ) ) ;
#3160=CARTESIAN_POINT ( 'NONE',  ( 0.000000000000000000, 22.00131761696259503, 0.000000000000000000 ) ) ;
#3163=DIRECTION ( 'NONE',  ( 0.000000000000000000, -0.7071067811866525998, -0.7071067811864425456 ) ) ;
#3166=CARTESIAN_POINT ( 'NONE',  ( 0.7867367962552690441, 24.50000000000000000, -2.267387309971103271 ) ) ;
#3174=CARTESIAN_POINT ( 'NONE',  ( 0.6838519463944332522, 24.63336607547026702, -4.223839491861407502 ) ) ;
#3176=CARTESIAN_POINT ( 'NONE',  ( -2.281413340844999915, 24.81304703576000037, 1.128321157715000078 ) ) ;
#3178=DIRECTION ( 'NONE',  ( 1.000000000000000000, 0.000000000000000000, 0.000000000000000000 ) ) ;
#3181=ADVANCED_FACE ( 'NONE', ( #9327 ), #5917, .T. ) ;
#3188=ORIENTED_EDGE ( 'NONE', *, *, #22713, .T. ) ;
#3193=CARTESIAN_POINT ( 'NONE',  ( -1.649410120653000078, 30.80057471234000133, -1.407032441706000059 ) ) ;
#3199=EDGE_CURVE ( 'NONE', #21988, #10806, #20769, .T. ) ;
#3200=ORIENTED_EDGE ( 'NONE', *, *, #23093, .T. ) ;
#3202=FACE_OUTER_BOUND ( 'NONE', #21824, .T. ) ;
#3208=CARTESIAN_POINT ( 'NONE',  ( 1.812579491195999815, 27.28006359724000163, -1.675531247043999805 ) ) ;
#3215=EDGE_CURVE ( 'NONE', #22068, #6244, #17608, .T. ) ;
#3216=VERTEX_POINT ( 'NONE', #10166 ) ;
#3217=CYLINDRICAL_SURFACE ( 'NONE', #20834, 2.000000000000000000 ) ;
#3218=EDGE_CURVE ( 'NONE', #4867, #22108, #19629, .T. ) ;
#3221=AXIS2_PLACEMENT_3D ( 'NONE', #14069, #21463, #15988 ) ;
#3225=CARTESIAN_POINT ( 'NONE',  ( 2.293942080512999748, 30.64047076207999964, -0.4768116971341999633 ) ) ;
#3227=CARTESIAN_POINT ( 'NONE',  ( 1.338211323675440934, 29.91862812200778521, -1.695402813922068930 ) ) ;
#3228=EDGE_CURVE ( 'NONE', #9936, #6330, #4469, .T. ) ;
#3233=ORIENTED_EDGE ( 'NONE', *, *, #17032, .F. ) ;
#3240=CARTESIAN_POINT ( 'NONE',  ( 1.613996465941623493, 27.32300317427615965, -1.453135498617304178 ) ) ;
#3249=CARTESIAN_POINT ( 'NONE',  ( -0.7981348345002412525, 27.95646770889779376, 2.019361405941054954 ) ) ;
#3251=DIRECTION ( 'NONE',  ( 1.000000000000000000, 0.000000000000000000, 0.000000000000000000 ) ) ;
#3255=CARTESIAN_POINT ( 'NONE',  ( 2.169172474974999876, 25.78119850838000460, -0.6576354733792000307 ) ) ;
#3257=CIRCLE ( 'NONE', #23743, 4.649999999999999467 ) ;
#3258=CARTESIAN_POINT ( 'NONE',  ( 0.000000000000000000, 9.000000000000000000, 0.000000000000000000 ) ) ;
#3263=CARTESIAN_POINT ( 'NONE',  ( 0.000000000000000000, 24.29999999999999716, 0.000000000000000000 ) ) ;
#3267=CIRCLE ( 'NONE', #18715, 4.750000000000000000 ) ;
#3268=ORIENTED_EDGE ( 'NONE', *, *, #17430, .T. ) ;
#3269=DIRECTION ( 'NONE',  ( 1.000000000000000000, 0.000000000000000000, 0.000000000000000000 ) ) ;
#3273=EDGE_LOOP ( 'NONE', ( #22901, #1492, #19981 ) ) ;
#3275=CARTESIAN_POINT ( 'NONE',  ( 1.923732104253000230, 29.24474039006999959, -1.647538756507999969 ) ) ;
#3277=CIRCLE ( 'NONE', #6749, 4.000000000000000000 ) ;
#3286=CARTESIAN_POINT ( 'NONE',  ( -2.164939593608602220, 24.49999999999984368, 3.368873696368141157 ) ) ;
#3294=CARTESIAN_POINT ( 'NONE',  ( -0.7463595094371999750, 23.89665089995999736, -2.539480043651999974 ) ) ;
#3298=CARTESIAN_POINT ( 'NONE',  ( -2.434931691670790155, 27.96666666666666856, -0.6543697108981958444 ) ) ;
#3301=DIRECTION ( 'NONE',  ( 0.000000000000000000, 1.000000000000000000, 0.000000000000000000 ) ) ;
#3303=CARTESIAN_POINT ( 'NONE',  ( -1.963534593326285549, 26.23539207552441255, 0.8393142750368668414 ) ) ;
#3304=CARTESIAN_POINT ( 'NONE',  ( 0.4755391251864483082, 26.25858828695499270, 2.107219116345798948 ) ) ;
#3305=VERTEX_POINT ( 'NONE', #3389 ) ;
#3306=EDGE_CURVE ( 'NONE', #3998, #19300, #17276, .T. ) ;
#3310=CIRCLE ( 'NONE', #5973, 2.000000000000000000 ) ;
#3311=DIRECTION ( 'NONE',  ( 0.000000000000000000, 1.000000000000000000, 0.000000000000000000 ) ) ;
#3313=CARTESIAN_POINT ( 'NONE',  ( 2.095827788178000084, 29.72344142836000103, -0.5546981053674999718 ) ) ;
#3314=DIRECTION ( 'NONE',  ( -0.7071067811823850136, 0.7071067811898851252, -1.080116767747976029E-06 ) ) ;
#3317=CARTESIAN_POINT ( 'NONE',  ( -1.955724675740084795, 26.26076676662178855, 0.9180910909140133080 ) ) ;
#3325=CARTESIAN_POINT ( 'NONE',  ( -2.899999999999999911, 18.00000000000000000, 0.000000000000000000 ) ) ;
#3331=CARTESIAN_POINT ( 'NONE',  ( 2.899999999999999911, 18.00000000000000000, 0.000000000000000000 ) ) ;
#3335=ORIENTED_EDGE ( 'NONE', *, *, #21504, .T. ) ;
#3339=AXIS2_PLACEMENT_3D ( 'NONE', #19096, #558, #6018 ) ;
#3343=CARTESIAN_POINT ( 'NONE',  ( -2.174612639932000047, 31.01849766815000109, -0.2438152186914000208 ) ) ;
#3347=CARTESIAN_POINT ( 'NONE',  ( 1.707696274334971287, 29.88778704512333206, -1.322457110828678228 ) ) ;
#3351=CARTESIAN_POINT ( 'NONE',  ( -1.120021599579974714, 23.61859144982829051, -1.799604945664644351 ) ) ;
#3353=EDGE_CURVE ( 'NONE', #17972, #2909, #21429, .T. ) ;
#3354=CYLINDRICAL_SURFACE ( 'NONE', #9131, 1.500000000000000000 ) ;
#3356=EDGE_CURVE ( 'NONE', #19694, #7466, #2197, .T. ) ;
#3361=ORIENTED_EDGE ( 'NONE', *, *, #19554, .F. ) ;
#3362=CARTESIAN_POINT ( 'NONE',  ( 1.785052107064501126, 26.50936796496311132, -1.283493281972921451 ) ) ;
#3368=EDGE_CURVE ( 'NONE', #21355, #20086, #9928, .T. ) ;
#3373=CARTESIAN_POINT ( 'NONE',  ( -0.1931865607023463827, 26.39289974830605345, 2.197767691045115157 ) ) ;
#3374=CARTESIAN_POINT ( 'NONE',  ( 0.1690226414553999690, 27.85250240010000056, -2.866097959738999723 ) ) ;
#3375=CARTESIAN_POINT ( 'NONE',  ( 1.407170236475686842, 30.71340226525985173, -1.638603115233653540 ) ) ;
#3377=CARTESIAN_POINT ( 'NONE',  ( -1.595510613210902928, 26.49040384242091761, -3.697633671484740425 ) ) ;
#3379=CARTESIAN_POINT ( 'NONE',  ( -1.472309056329999866, 27.63369850838000374, -1.723852419406000092 ) ) ;
#3381=CARTESIAN_POINT ( 'NONE',  ( 2.343805879471000164, 25.85187716036000083, -0.7105796827304000640 ) ) ;
#3382=CONICAL_SURFACE ( 'NONE', #20750, 3.049999825846000157, 0.7853981633972997312 ) ;
#3384=ORIENTED_EDGE ( 'NONE', *, *, #16929, .F. ) ;
#3389=CARTESIAN_POINT ( 'NONE',  ( -3.000000000000000000, 22.00000000000000000, 0.000000000000000000 ) ) ;
#3391=CARTESIAN_POINT ( 'NONE',  ( 0.6543697108982381438, 24.23333333333333073, 2.434931691670778608 ) ) ;
#3395=UNCERTAINTY_MEASURE_WITH_UNIT (LENGTH_MEASURE( 1.000000000000000082E-05 ), #4305, 'distance_accuracy_value', 'NONE');
#3398=CARTESIAN_POINT ( 'NONE',  ( -0.8605612368241999377, 30.29128581794000041, 1.971086656256000103 ) ) ;
#3401=AXIS2_PLACEMENT_3D ( 'NONE', #12949, #23506, #3178 ) ;
#3402=VERTEX_POINT ( 'NONE', #5890 ) ;
#3405=CARTESIAN_POINT ( 'NONE',  ( 0.3272492347489617259, 29.01666666666666572, 2.499999999999996447 ) ) ;
#3406=AXIS2_PLACEMENT_3D ( 'NONE', #84, #23949, #20675 ) ;
#3413=DIRECTION ( 'NONE',  ( 0.000000000000000000, 0.000000000000000000, -1.000000000000000000 ) ) ;
#3416=CARTESIAN_POINT ( 'NONE',  ( 2.431246278770999858, 25.97421836118000016, -0.3831752036581999588 ) ) ;
#3417=DIRECTION ( 'NONE',  ( 1.000000000000000000, 0.000000000000000000, 0.000000000000000000 ) ) ;
#3419=AXIS2_PLACEMENT_3D ( 'NONE', #14593, #6732, #12672 ) ;
#3422=CARTESIAN_POINT ( 'NONE',  ( 0.000000000000000000, 20.04999987253367877, 0.000000000000000000 ) ) ;
#3423=CARTESIAN_POINT ( 'NONE',  ( -2.251038631694548986, 23.88666666666668448, -0.9061425655839590032 ) ) ;
#3425=CARTESIAN_POINT ( 'NONE',  ( -0.1529142988638288181, 26.50000000000000355, -2.395123632968240823 ) ) ;
#3430=CARTESIAN_POINT ( 'NONE',  ( 0.01686421794022999882, 25.08949700035999797, -2.144542314183000009 ) ) ;
#3435=CARTESIAN_POINT ( 'NONE',  ( -1.875937833822000078, 30.94419248354000374, 0.8416011999412000844 ) ) ;
#3436=B_SPLINE_CURVE_WITH_KNOTS ( 'NONE', 3,
 ( #14345, #2723, #15900, #16016, #6467, #19803, #15654, #13976 ),
 .UNSPECIFIED., .F., .F.,
 ( 4, 2, 2, 4 ),
 ( 0.000000000000000000, 0.2499999999999999445, 0.4999999999999998890, 1.000000000000000000 ),
 .UNSPECIFIED. ) ;
#3439=ORIENTED_EDGE ( 'NONE', *, *, #3306, .F. ) ;
#3440=DIRECTION ( 'NONE',  ( 1.000000000000000000, 0.000000000000000000, 0.000000000000000000 ) ) ;
#3441=ORIENTED_EDGE ( 'NONE', *, *, #1584, .T. ) ;
#3442=CONICAL_SURFACE ( 'NONE', #15006, 2.849999993810000021, 0.7853981633972997312 ) ;
#3443=CARTESIAN_POINT ( 'NONE',  ( -0.3418248460082276563, 30.21683089135267508, -2.592948918868650754 ) ) ;
#3445=EDGE_CURVE ( 'NONE', #16168, #23400, #13162, .T. ) ;
#3447=AXIS2_PLACEMENT_3D ( 'NONE', #1825, #10807, #5233 ) ;
#3454=EDGE_LOOP ( 'NONE', ( #12677, #20314, #8681, #5924, #9418 ) ) ;
#3461=CARTESIAN_POINT ( 'NONE',  ( -0.3635937247009000117, 28.79408723144999627, 2.231225001579999923 ) ) ;
#3464=CARTESIAN_POINT ( 'NONE',  ( 2.067250320083055648, 29.84154813460735056, -0.6328137310853092501 ) ) ;
#3473=ORIENTED_EDGE ( 'NONE', *, *, #16950, .F. ) ;
#3474=CIRCLE ( 'NONE', #8903, 2.000000000000000000 ) ;
#3478=DIRECTION ( 'NONE',  ( 1.000000000000000000, 0.000000000000000000, 0.000000000000000000 ) ) ;
#3480=CARTESIAN_POINT ( 'NONE',  ( -0.6543697108981931798, 29.76666666666666217, 2.434931691670791043 ) ) ;
#3481=ORIENTED_EDGE ( 'NONE', *, *, #4962, .F. ) ;
#3489=CARTESIAN_POINT ( 'NONE',  ( 1.740441092190665895, 27.32044006443200601, 1.359758610450851446 ) ) ;
#3490=CARTESIAN_POINT ( 'NONE',  ( 1.182158213329999930, 29.12000240010000240, 2.320116128650000054 ) ) ;
#3491=CIRCLE ( 'NONE', #17003, 2.899999999999999911 ) ;
#3492=CARTESIAN_POINT ( 'NONE',  ( 2.021074183709790528, 30.64977378284504539, -0.7618599147945216421 ) ) ;
#3493=VERTEX_POINT ( 'NONE', #13517 ) ;
#3494=CARTESIAN_POINT ( 'NONE',  ( -1.839173991642404138, 26.50000000000000355, -3.556954554355651776 ) ) ;
#3495=DIRECTION ( 'NONE',  ( 0.000000000000000000, 1.000000000000000000, 0.000000000000000000 ) ) ;
#3496=CARTESIAN_POINT ( 'NONE',  ( 1.629375854237163912, 24.77111710846513404, 1.370482674755798769 ) ) ;
#3497=CARTESIAN_POINT ( 'NONE',  ( -1.800284464616000113, 27.67364211382000150, 1.419229835182000077 ) ) ;
#3498=EDGE_CURVE ( 'NONE', #14786, #2047, #2378, .T. ) ;
#3504=CARTESIAN_POINT ( 'NONE',  ( -0.6743924145742135057, 30.66853591686814440, -2.175867686628469855 ) ) ;
#3506=CARTESIAN_POINT ( 'NONE',  ( 0.000000000000000000, 9.000000000000000000, 0.000000000000000000 ) ) ;
#3511=ADVANCED_FACE ( 'NONE', ( #17034 ), #4827, .F. ) ;
#3513=CARTESIAN_POINT ( 'NONE',  ( 1.341975064934000095, 29.62948861319000216, 1.680729365189000069 ) ) ;
#3516=EDGE_LOOP ( 'NONE', ( #21764, #17810, #18464, #16532, #2678, #6284, #6194 ) ) ;
#3519=CARTESIAN_POINT ( 'NONE',  ( -3.100000000000000089, 15.00000000000000000, 0.000000000000000000 ) ) ;
#3523=CARTESIAN_POINT ( 'NONE',  ( -1.633064903454896966, 29.31302280117960990, -1.413517025400313321 ) ) ;
#3524=CARTESIAN_POINT ( 'NONE',  ( -1.767766952966000060, 30.50000000000000000, 1.767766952966000060 ) ) ;
#3525=EDGE_LOOP ( 'NONE', ( #17576, #3926, #8622, #8440, #2866, #17469, #7430 ) ) ;
#3526=ADVANCED_FACE ( 'NONE', ( #549 ), #14100, .F. ) ;
#3527=CARTESIAN_POINT ( 'NONE',  ( 2.099577540571663015, 23.85573745231591403, 1.106133451035238524 ) ) ;
#3528=VERTEX_POINT ( 'NONE', #2624 ) ;
#3529=CARTESIAN_POINT ( 'NONE',  ( -0.6391230356295000137, 23.90547497936000099, 2.064599356847000244 ) ) ;
#3537=CARTESIAN_POINT ( 'NONE',  ( 0.000000000000000000, 19.00000000000000000, 0.000000000000000000 ) ) ;
#3538=CARTESIAN_POINT ( 'NONE',  ( -4.000000000000000000, 24.50000000000000000, 0.000000000000000000 ) ) ;
#3541=CARTESIAN_POINT ( 'NONE',  ( -1.946458991525999993, 25.34566145796000214, 0.9003574723619000020 ) ) ;
#3547=CARTESIAN_POINT ( 'NONE',  ( -4.749999884653000493, 20.09999988465641252, 5.093549627072000020E-08 ) ) ;
#3554=CARTESIAN_POINT ( 'NONE',  ( 1.803851175814259244, 30.74302359554534192, -1.387995464745191310 ) ) ;
#3558=EDGE_CURVE ( 'NONE', #11075, #18791, #22953, .T. ) ;
#3559=CARTESIAN_POINT ( 'NONE',  ( 1.450871306011999984, 27.86506359723999893, 1.996953125041000199 ) ) ;
#3560=VERTEX_POINT ( 'NONE', #6499 ) ;
#3566=CARTESIAN_POINT ( 'NONE',  ( 4.724999999999999645, 14.90000000000000036, 0.000000000000000000 ) ) ;
#3570=CARTESIAN_POINT ( 'NONE',  ( -2.180465314960999823, 31.04811387923000154, 0.5967716603282000598 ) ) ;
#3572=CARTESIAN_POINT ( 'NONE',  ( 2.122511661976075548, 29.82749129234522556, -0.4006784551261859395 ) ) ;
#3573=ORIENTED_EDGE ( 'NONE', *, *, #18548, .F. ) ;
#3574=CARTESIAN_POINT ( 'NONE',  ( -1.613915809855000161, 25.52668260664000144, 1.467707619367000227 ) ) ;
#3576=CARTESIAN_POINT ( 'NONE',  ( -0.9863764412085774813, 23.62386489563331082, -1.881032207583069216 ) ) ;
#3577=CIRCLE ( 'NONE', #21362, 3.100000000000000089 ) ;
#3583=EDGE_CURVE ( 'NONE', #2909, #5518, #5506, .T. ) ;
#3589=CARTESIAN_POINT ( 'NONE',  ( 2.399999988617999680, 26.49999998861800066, 6.349992443878999481E-08 ) ) ;
#3597=CARTESIAN_POINT ( 'NONE',  ( 2.036279486417807316, 27.45294582375450787, -0.8150601855909705984 ) ) ;
#3599=CARTESIAN_POINT ( 'NONE',  ( 1.686548823153775745, 30.68970166146306511, -1.349673947955718711 ) ) ;
#3600=ORIENTED_EDGE ( 'NONE', *, *, #10443, .F. ) ;
#3605=CARTESIAN_POINT ( 'NONE',  ( 1.981708497821000226, 26.53437716036000182, 1.439795436514999860 ) ) ;
#3607=EDGE_LOOP ( 'NONE', ( #874, #13520, #23613, #5720, #6594, #11648 ) ) ;
#3611=CARTESIAN_POINT ( 'NONE',  ( -2.273481569363994925, 30.02225594647815043, -0.1432571156271773005 ) ) ;
#3615=LINE ( 'NONE', #14654, #10343 ) ;
#3619=CARTESIAN_POINT ( 'NONE',  ( 1.536366799937295413, 29.31753006952332896, 1.999167105995444338 ) ) ;
#3620=CARTESIAN_POINT ( 'NONE',  ( -0.7039221594073999944, 28.80840715711999778, 2.125142508213000436 ) ) ;
#3624=CIRCLE ( 'NONE', #5553, 3.000000000000000000 ) ;
#3629=DIRECTION ( 'NONE',  ( 1.000000000000000000, 0.000000000000000000, 0.000000000000000000 ) ) ;
#3631=CARTESIAN_POINT ( 'NONE',  ( -1.635465687292884773, 29.31323759626713255, -1.410743754062205646 ) ) ;
#3634=DIRECTION ( 'NONE',  ( 0.000000000000000000, 1.000000000000000000, 0.000000000000000000 ) ) ;
#3635=ORIENTED_EDGE ( 'NONE', *, *, #15775, .F. ) ;
#3637=DIRECTION ( 'NONE',  ( 0.000000000000000000, 0.000000000000000000, -1.000000000000000000 ) ) ;
#3640=CARTESIAN_POINT ( 'NONE',  ( -1.802851389305008434, 26.49891402983596222, 1.731858503842447217 ) ) ;
#3643=AXIS2_PLACEMENT_3D ( 'NONE', #10921, #14771, #7388 ) ;
#3648=ORIENTED_EDGE ( 'NONE', *, *, #12504, .F. ) ;
#3652=CARTESIAN_POINT ( 'NONE',  ( 2.246634820853000036, 25.60312647565999811, -0.3244181043566000122 ) ) ;
#3656=CARTESIAN_POINT ( 'NONE',  ( -2.214826247177999807, 30.81482155776999932, 0.5323604184908000692 ) ) ;
#3663=DIRECTION ( 'NONE',  ( 0.000000000000000000, -1.000000000000000000, 0.000000000000000000 ) ) ;
#3666=VECTOR ( 'NONE', #5384, 999.9999999999998863 ) ;
#3668=FACE_OUTER_BOUND ( 'NONE', #10223, .T. ) ;
#3669=CARTESIAN_POINT ( 'NONE',  ( 2.826365205286999860, 27.75169433610000169, 0.5047246425490000687 ) ) ;
#3670=ORIENTED_EDGE ( 'NONE', *, *, #9828, .F. ) ;
#3671=VECTOR ( 'NONE', #20716, 1000.000000000000114 ) ;
#3681=CARTESIAN_POINT ( 'NONE',  ( -1.090723536193999976, 30.35272267939000201, 2.073606040276000151 ) ) ;
#3684=CARTESIAN_POINT ( 'NONE',  ( 1.381408399707872992, 29.91531716123279239, -1.660698994484458346 ) ) ;
#3685=VERTEX_POINT ( 'NONE', #5285 ) ;
#3686=CARTESIAN_POINT ( 'NONE',  ( -1.854454310345000190, 24.53117208695000073, -1.420007133126999888 ) ) ;
#3688=CARTESIAN_POINT ( 'NONE',  ( -0.9472309125058132606, 23.62634780752645014, -1.903746509698968081 ) ) ;
#3695=VECTOR ( 'NONE', #7844, 1000.000000000000000 ) ;
#3697=SHAPE_DEFINITION_REPRESENTATION ( #11928, #16160 ) ;
#3699=ORIENTED_EDGE ( 'NONE', *, *, #8801, .F. ) ;
#3705=CARTESIAN_POINT ( 'NONE',  ( -4.000000000000000000, 26.20000000000000284, -2.309401076759000304 ) ) ;
#3710=CARTESIAN_POINT ( 'NONE',  ( 2.013323156743944686, 30.65106894508059199, -0.7821756420678627197 ) ) ;
#3712=B_SPLINE_CURVE_WITH_KNOTS ( 'NONE', 3,
 ( #13139, #3939, #16649, #7094, #55, #14484, #5286, #3480, #3820, #7440, #14820, #1648, #9038, #9386, #7559, #14937, #8927, #23799 ),
 .UNSPECIFIED., .F., .F.,
 ( 4, 2, 2, 2, 2, 2, 2, 2, 4 ),
 ( 0.000000000000000000, 0.1250000000000000000, 0.2500000000000000000, 0.3750000000000000000, 0.5000000000000000000, 0.6250000000000000000, 0.7500000000000000000, 0.8750000000000000000, 1.000000000000000000 ),
 .UNSPECIFIED. ) ;
#3717=CARTESIAN_POINT ( 'NONE',  ( -1.360883606431000148, 26.33937716036000154, 2.036706090186000129 ) ) ;
#3718=FACE_OUTER_BOUND ( 'NONE', #738, .T. ) ;
#3719=DIRECTION ( 'NONE',  ( 0.000000000000000000, -1.000000000000000000, 0.000000000000000000 ) ) ;
#3720=ORIENTED_EDGE ( 'NONE', *, *, #21985, .F. ) ;
#3722=EDGE_CURVE ( 'NONE', #5602, #23163, #22594, .T. ) ;
#3724=CARTESIAN_POINT ( 'NONE',  ( -0.8447332559524692863, 29.87863817527814803, -2.115577172688746455 ) ) ;
#3725=ORIENTED_EDGE ( 'NONE', *, *, #9118, .T. ) ;
#3728=CONICAL_SURFACE ( 'NONE', #4905, 4.649999926447000220, 0.7853981633972997312 ) ;
#3731=CARTESIAN_POINT ( 'NONE',  ( 0.6543697108982093891, 29.26753006952333536, 2.434931691670787490 ) ) ;
#3732=CARTESIAN_POINT ( 'NONE',  ( 2.140718310772999899, 30.55600469983999901, -0.2075533484111000138 ) ) ;
#3733=DIRECTION ( 'NONE',  ( 0.000000000000000000, -1.000000000000000000, 0.000000000000000000 ) ) ;
#3735=EDGE_LOOP ( 'NONE', ( #18257, #3233 ) ) ;
#3736=CARTESIAN_POINT ( 'NONE',  ( 0.000000000000000000, 9.000000000000000000, 0.000000000000000000 ) ) ;
#3739=CARTESIAN_POINT ( 'NONE',  ( 0.6543697108982240440, 29.03333333333333854, 2.434931691670783049 ) ) ;
#3745=CARTESIAN_POINT ( 'NONE',  ( 0.01500812129314476814, 29.20288496623757979, -2.161759760356441795 ) ) ;
#3746=CARTESIAN_POINT ( 'NONE',  ( 0.000000000000000000, 9.050044887908999414, 0.000000000000000000 ) ) ;
#3747=ORIENTED_EDGE ( 'NONE', *, *, #6285, .F. ) ;
#3751=CARTESIAN_POINT ( 'NONE',  ( 1.941085051938999939, 25.12563408233999951, -1.330354224329999946 ) ) ;
#3753=ADVANCED_FACE ( 'NONE', ( #21991 ), #14819, .T. ) ;
#3756=DIRECTION ( 'NONE',  ( 0.000000000000000000, 0.7071067811866525998, -0.7071067811864425456 ) ) ;
#3758=DIRECTION ( 'NONE',  ( 1.000000000000000000, 0.000000000000000000, 0.000000000000000000 ) ) ;
#3762=DIRECTION ( 'NONE',  ( 0.000000000000000000, 1.000000000000000000, 0.000000000000000000 ) ) ;
#3763=EDGE_CURVE ( 'NONE', #11168, #20706, #20819, .T. ) ;
#3765=ORIENTED_EDGE ( 'NONE', *, *, #16914, .T. ) ;
#3767=AXIS2_PLACEMENT_3D ( 'NONE', #3969, #9535, #16912 ) ;
#3768=CARTESIAN_POINT ( 'NONE',  ( -1.814669259075999852, 24.47173345458000071, 1.469565487754999955 ) ) ;
#3773=CARTESIAN_POINT ( 'NONE',  ( 2.512136363505000247, 30.30246990879999913, -0.4555555407424999870 ) ) ;
#3775=EDGE_CURVE ( 'NONE', #8097, #20600, #9153, .T. ) ;
#3780=DIRECTION ( 'NONE',  ( -2.317847129507103042E-07, 0.9999999999999731326, 0.000000000000000000 ) ) ;
#3785=ADVANCED_FACE ( 'NONE', ( #15536 ), #11802, .T. ) ;
#3790=CARTESIAN_POINT ( 'NONE',  ( -2.607696352436000176, 25.90712896666999754, 0.5721489135198000175 ) ) ;
#3795=ORIENTED_EDGE ( 'NONE', *, *, #16810, .F. ) ;
#3796=CARTESIAN_POINT ( 'NONE',  ( 1.699999999999999956, 9.029776626192267841, 0.9151613154069033751 ) ) ;
#3800=AXIS2_PLACEMENT_3D ( 'NONE', #16933, #6028, #11264 ) ;
#3802=CARTESIAN_POINT ( 'NONE',  ( -0.3395901671559999890, 28.81242903415000001, 2.083925050886000108 ) ) ;
#3805=CARTESIAN_POINT ( 'NONE',  ( -0.07097743868425297753, 29.59969681156075438, 2.158689068696717950 ) ) ;
#3806=ORIENTED_EDGE ( 'NONE', *, *, #4172, .T. ) ;
#3807=CARTESIAN_POINT ( 'NONE',  ( 0.5132826282582999555, 24.04258772846000269, 2.278587698102000125 ) ) ;
#3809=CARTESIAN_POINT ( 'NONE',  ( -0.8709342061498644982, 23.65006605176747456, -1.965773624965944100 ) ) ;
#3811=ORIENTED_EDGE ( 'NONE', *, *, #17878, .F. ) ;
#3815=AXIS2_PLACEMENT_3D ( 'NONE', #17667, #15474, #1064 ) ;
#3816=FACE_OUTER_BOUND ( 'NONE', #7547, .T. ) ;
#3820=CARTESIAN_POINT ( 'NONE',  ( -0.3272492347489287523, 29.78333333333333499, 2.500000000000001332 ) ) ;
#3822=ORIENTED_EDGE ( 'NONE', *, *, #4195, .F. ) ;
#3825=AXIS2_PLACEMENT_3D ( 'NONE', #9780, #18980, #2391 ) ;
#3828=DIRECTION ( 'NONE',  ( 0.000000000000000000, -1.000000000000000000, 0.000000000000000000 ) ) ;
#3834=CARTESIAN_POINT ( 'NONE',  ( 1.456462752601113353, 30.70952715242214381, -1.595930482832717434 ) ) ;
#3838=CIRCLE ( 'NONE', #9642, 2.270871215252209030 ) ;
#3840=CARTESIAN_POINT ( 'NONE',  ( 0.4021892318948999678, 26.45521896306000187, 2.252185756629999869 ) ) ;
#3851=PLANE ( 'NONE',  #14600 ) ;
#3855=LINE ( 'NONE', #5439, #11567 ) ;
#3856=CARTESIAN_POINT ( 'NONE',  ( -2.121370068014000410, 29.36476973129000001, 0.3543124420124999507 ) ) ;
#3859=AXIS2_PLACEMENT_3D ( 'NONE', #14426, #14540, #22274 ) ;
#3863=B_SPLINE_CURVE_WITH_KNOTS ( 'NONE', 3,
 ( #6865, #4573, #14257, #17531, #21655, #11965, #5068, #925 ),
 .UNSPECIFIED., .F., .F.,
 ( 4, 2, 2, 4 ),
 ( 0.000000000000000000, 0.2500000000000000000, 0.5000000000000000000, 1.000000000000000000 ),
 .UNSPECIFIED. ) ;
#3867=CARTESIAN_POINT ( 'NONE',  ( 3.000000000000000000, 15.00000000000000000, 0.000000000000000000 ) ) ;
#3869=CARTESIAN_POINT ( 'NONE',  ( -0.6469316270125009538, 29.24251007170759920, -2.063874927344320209 ) ) ;
#3871=ORIENTED_EDGE ( 'NONE', *, *, #22837, .T. ) ;
#3872=CARTESIAN_POINT ( 'NONE',  ( -0.01212694170664108638, 23.76765559877391354, 2.284373250672524058 ) ) ;
#3874=CARTESIAN_POINT ( 'NONE',  ( 2.064511051236999961, 25.76334910003999923, -0.3253761041896999773 ) ) ;
#3876=CARTESIAN_POINT ( 'NONE',  ( -2.256099604565999783, 27.67799822781000074, -0.2222064166828000287 ) ) ;
#3878=DIRECTION ( 'NONE',  ( 0.000000000000000000, -1.000000000000000000, 0.000000000000000000 ) ) ;
#3880=DIRECTION ( 'NONE',  ( 0.000000000000000000, -1.000000000000000000, 0.000000000000000000 ) ) ;
#3882=SHAPE_REPRESENTATION_RELATIONSHIP ( 'NONE' , 'NONE' ,  #16160, #982 ) ;
#3885=DIRECTION ( 'NONE',  ( 0.000000000000000000, -1.000000000000000000, 0.000000000000000000 ) ) ;
#3886=DIRECTION ( 'NONE',  ( -0.000000000000000000, -1.000000000000000000, -0.000000000000000000 ) ) ;
#3889=CARTESIAN_POINT ( 'NONE',  ( 2.229792775116000048, 24.02344565378000141, -0.6933047407275000351 ) ) ;
#3893=CARTESIAN_POINT ( 'NONE',  ( 0.6648189132885999886, 30.44608768000000154, -2.465032527426999742 ) ) ;
#3896=PLANE ( 'NONE',  #6122 ) ;
#3899=CARTESIAN_POINT ( 'NONE',  ( 1.800000000000000044, 13.00000000000000000, -1.081665382638999917 ) ) ;
#3907=DIRECTION ( 'NONE',  ( -1.000000000000000000, 0.000000000000000000, 2.810008490046999894E-14 ) ) ;
#3908=EDGE_CURVE ( 'NONE', #2909, #11168, #22263, .T. ) ;
#3909=CARTESIAN_POINT ( 'NONE',  ( 2.159851832628000068, 26.19962896667000152, 1.569224139466999901 ) ) ;
#3911=ORIENTED_EDGE ( 'NONE', *, *, #436, .T. ) ;
#3912=B_SPLINE_CURVE_WITH_KNOTS ( 'NONE', 3,
 ( #3067, #19651, #16358, #10452, #23514, #19776, #18305, #5005, #16245, #1708, #5120, #14541, #18073, #5346, #17839, #1234, #3303, #5235, #9097, #12502, #12619, #8624, #10809, #18201 ),
 .UNSPECIFIED., .F., .F.,
 ( 4, 2, 2, 2, 2, 2, 2, 2, 2, 2, 2, 4 ),
 ( 8.179270553615951679E-05, 0.0008436736815539817337, 0.001224614169562892978, 0.001605554657571804439, 0.002367435633589626710, 0.002748376121598538387, 0.002938846365602994226, 0.003034081487605222362, 0.003057890268105779071, 0.003069794658356057859, 0.003081699048606336214, 0.003129316609607453534 ),
 .UNSPECIFIED. ) ;
#3914=CARTESIAN_POINT ( 'NONE',  ( 0.000000000000000000, 18.50000000000000000, 0.000000000000000000 ) ) ;
#3922=CARTESIAN_POINT ( 'NONE',  ( -2.042928671780000371, 30.08837290161000055, 1.173968745881999842 ) ) ;
#3923=EDGE_CURVE ( 'NONE', #9876, #15019, #3277, .T. ) ;
#3925=CARTESIAN_POINT ( 'NONE',  ( 1.139808571972009021, 29.67456316804590699, 1.835980945443606238 ) ) ;
#3926=ORIENTED_EDGE ( 'NONE', *, *, #2587, .T. ) ;
#3927=CARTESIAN_POINT ( 'NONE',  ( -0.06876214361208000947, 24.82870495165000335, 2.180404198171999930 ) ) ;
#3928=LINE ( 'NONE', #11321, #4627 ) ;
#3934=EDGE_CURVE ( 'NONE', #11746, #4287, #16404, .T. ) ;
#3938=CARTESIAN_POINT ( 'NONE',  ( -1.536366799937273653, 28.35086340285666395, 1.999167105995461213 ) ) ;
#3939=CARTESIAN_POINT ( 'NONE',  ( -2.499999999999999556, 29.61666666666666714, 0.3272492347489423525 ) ) ;
#3940=CIRCLE ( 'NONE', #17477, 2.500000000000000000 ) ;
#3943=CARTESIAN_POINT ( 'NONE',  ( 1.768240990936880142, 24.49990546444021078, -1.767061324597003713 ) ) ;
#3949=ADVANCED_FACE ( 'NONE', ( #16137 ), #4037, .F. ) ;
#3950=DIRECTION ( 'NONE',  ( 1.000000000000000000, 0.000000000000000000, 0.000000000000000000 ) ) ;
#3952=SURFACE_SIDE_STYLE ('',( #20541 ) ) ;
#3953=PLANE ( 'NONE',  #6041 ) ;
#3954=CARTESIAN_POINT ( 'NONE',  ( 0.8670279822662322333, 30.45653399219317592, 1.978445612786488672 ) ) ;
#3956=DIRECTION ( 'NONE',  ( 1.000000000000000000, 0.000000000000000000, 0.000000000000000000 ) ) ;
#3957=CARTESIAN_POINT ( 'NONE',  ( 1.493398715743419869, 24.78022351799236489, 1.505750370948753414 ) ) ;
#3960=CARTESIAN_POINT ( 'NONE',  ( -1.273605814386999713, 26.11364211382000278, 1.906085653762000121 ) ) ;
#3961=CARTESIAN_POINT ( 'NONE',  ( -2.127716147605950514, 30.86060364257915367, 0.2232574844277085691 ) ) ;
#3963=DIRECTION ( 'NONE',  ( 0.000000000000000000, -1.000000000000000000, 0.000000000000000000 ) ) ;
#3964=VERTEX_POINT ( 'NONE', #3331 ) ;
#3969=CARTESIAN_POINT ( 'NONE',  ( 0.000000000000000000, 18.00000000000000000, 0.000000000000000000 ) ) ;
#3972=PLANE ( 'NONE',  #17357 ) ;
#3974=CARTESIAN_POINT ( 'NONE',  ( 1.236794719700695211, 24.50000548481460427, 2.172625763342098004 ) ) ;
#3975=AXIS2_PLACEMENT_3D ( 'NONE', #15262, #19146, #15385 ) ;
#3978=DIRECTION ( 'NONE',  ( 0.000000000000000000, 1.000000000000000000, 0.000000000000000000 ) ) ;
#3980=DIRECTION ( 'NONE',  ( 0.000000000000000000, 0.000000000000000000, 1.000000000000000000 ) ) ;
#3983=CARTESIAN_POINT ( 'NONE',  ( -1.569329342329819577, 29.30733016622408371, -1.486957734784279062 ) ) ;
#3988=CARTESIAN_POINT ( 'NONE',  ( -1.155917513699999954, 24.67184805413999982, 1.826172021010999957 ) ) ;
#3990=CARTESIAN_POINT ( 'NONE',  ( -0.2222064166829000043, 26.70299822781000287, -2.256099604565999783 ) ) ;
#3994=DIRECTION ( 'NONE',  ( 1.000000000000000000, 0.000000000000000000, 0.000000000000000000 ) ) ;
#3998=VERTEX_POINT ( 'NONE', #6591 ) ;
#4000=CARTESIAN_POINT ( 'NONE',  ( 1.751540416571000236, 23.98205213760000021, -1.819511229224000104 ) ) ;
#4002=DIRECTION ( 'NONE',  ( -0.7071067811864758523, 0.7071067811861759811, -7.917084064338729087E-07 ) ) ;
#4004=CARTESIAN_POINT ( 'NONE',  ( -2.360231394774000346, 29.18715348418999866, 0.03874416005483000136 ) ) ;
#4007=CARTESIAN_POINT ( 'NONE',  ( 0.000000000000000000, 9.000000000000000000, -1.899912543625706274 ) ) ;
#4011=CARTESIAN_POINT ( 'NONE',  ( -2.430432513736672906, 24.27082020183427247, 0.7153544994183682615 ) ) ;
#4012=CYLINDRICAL_SURFACE ( 'NONE', #4190, 4.750000000000000000 ) ;
#4015=CIRCLE ( 'NONE', #16389, 2.500000000000000000 ) ;
#4021=CARTESIAN_POINT ( 'NONE',  ( -2.254705796085000102, 27.45919433610000127, 1.777466727206999941 ) ) ;
#4022=EDGE_CURVE ( 'NONE', #14442, #18459, #4966, .T. ) ;
#4026=CARTESIAN_POINT ( 'NONE',  ( 1.536366799937286087, 27.15086340285666822, -1.999167105995451221 ) ) ;
#4028=CONICAL_SURFACE ( 'NONE', #4406, 2.949999959913000236, 0.7853981633972997312 ) ;
#4036=CARTESIAN_POINT ( 'NONE',  ( 0.4726444045413000228, 28.61631019869999903, 2.141105848461999805 ) ) ;
#4037=TOROIDAL_SURFACE ( 'NONE', #2889, 2.099999992707999752, 0.1000000000000000056 ) ;
#4039=EDGE_CURVE ( 'NONE', #18459, #2273, #17553, .T. ) ;
#4040=CARTESIAN_POINT ( 'NONE',  ( 0.7411338969787365505, 29.64842732084730770, 2.029636956427176120 ) ) ;
#4041=ORIENTED_EDGE ( 'NONE', *, *, #12836, .F. ) ;
#4042=CARTESIAN_POINT ( 'NONE',  ( -0.07362252012096999476, 24.81036314894999961, 2.334523671301000469 ) ) ;
#4047=CARTESIAN_POINT ( 'NONE',  ( 2.424643331163519964E-11, 24.52694564545263844, -2.373054354547839306 ) ) ;
#4048=CARTESIAN_POINT ( 'NONE',  ( 1.950358564618835500, 30.32279782412667402, -1.623347314877277459 ) ) ;
#4050=ADVANCED_FACE ( 'NONE', ( #21309 ), #4722, .T. ) ;
#4055=EDGE_LOOP ( 'NONE', ( #16683, #7350, #19085, #18273, #4428, #4436, #6358, #5880, #18247 ) ) ;
#4057=CARTESIAN_POINT ( 'NONE',  ( 0.000000000000000000, 24.50000000000000000, -2.400000000000455991 ) ) ;
#4060=ADVANCED_FACE ( 'NONE', ( #23823 ), #252, .T. ) ;
#4064=CARTESIAN_POINT ( 'NONE',  ( 1.735739373471972158, 26.42668463374644361, -1.556826290527684620 ) ) ;
#4066=CARTESIAN_POINT ( 'NONE',  ( -2.500000000000000000, 28.23419673618999681, 0.000000000000000000 ) ) ;
#4068=CARTESIAN_POINT ( 'NONE',  ( 1.154729593009722333, 30.47563926276945168, 1.826466678455010983 ) ) ;
#4075=CARTESIAN_POINT ( 'NONE',  ( -2.459101194521000178, 26.82946440325999760, 0.1450207862197999964 ) ) ;
#4076=CONICAL_SURFACE ( 'NONE', #23796, 2.249999993254999886, 0.7853981633972997312 ) ;
#4078=ORIENTED_EDGE ( 'NONE', *, *, #2707, .F. ) ;
#4082=ADVANCED_FACE ( 'NONE', ( #6766 ), #4967, .T. ) ;
#4083=CARTESIAN_POINT ( 'NONE',  ( 0.3345823118753548098, 28.21060522079947575, -2.176823781557687187 ) ) ;
#4092=FACE_OUTER_BOUND ( 'NONE', #22033, .T. ) ;
#4097=CARTESIAN_POINT ( 'NONE',  ( -2.804372049896000085, 26.48750240010000212, 0.6153010951427000386 ) ) ;
#4099=CARTESIAN_POINT ( 'NONE',  ( 2.109404096337074375, 29.03140909393173530, -0.4645879857137120150 ) ) ;
#4101=ORIENTED_EDGE ( 'NONE', *, *, #5500, .F. ) ;
#4102=CARTESIAN_POINT ( 'NONE',  ( 4.724999978625000097, 14.90000002138000035, 2.519183602109999904E-09 ) ) ;
#4106=CARTESIAN_POINT ( 'NONE',  ( 1.831974274068000064, 25.63049822781000131, 0.9334375154566999511 ) ) ;
#4107=CARTESIAN_POINT ( 'NONE',  ( 1.499999883624000052, 7.099999883624000141, -4.580366257796999989E-07 ) ) ;
#4108=TOROIDAL_SURFACE ( 'NONE', #20740, 2.500000000000000000, 0.5500000000000000444 ) ;
#4116=AXIS2_PLACEMENT_3D ( 'NONE', #6490, #8434, #13993 ) ;
#4117=CARTESIAN_POINT ( 'NONE',  ( 0.9856789269715999779, 25.22148090944999765, 2.530880771168000365 ) ) ;
#4121=CARTESIAN_POINT ( 'NONE',  ( 0.2669411416847999874, 28.86629219681999814, -2.539114488640000111 ) ) ;
#4124=AXIS2_PLACEMENT_3D ( 'NONE', #17488, #21246, #15648 ) ;
#4125=DIRECTION ( 'NONE',  ( 0.7071067811880967779, 0.7071067811849969242, -4.142944449020979899E-08 ) ) ;
#4126=CARTESIAN_POINT ( 'NONE',  ( 0.000000000000000000, 19.00000000000000000, 0.000000000000000000 ) ) ;
#4129=ORIENTED_EDGE ( 'NONE', *, *, #3199, .T. ) ;
#4130=CARTESIAN_POINT ( 'NONE',  ( 2.410494989090000040, 25.19716278443000235, 1.296714785155999916 ) ) ;
#4131=CARTESIAN_POINT ( 'NONE',  ( 0.000000000000000000, 23.50000000000000000, 0.000000000000000000 ) ) ;
#4133=ORIENTED_EDGE ( 'NONE', *, *, #18692, .T. ) ;
#4137=CARTESIAN_POINT ( 'NONE',  ( -2.329463490920999913, 28.34462896666999754, 1.304555153736000062 ) ) ;
#4139=VERTEX_POINT ( 'NONE', #14624 ) ;
#4140=CIRCLE ( 'NONE', #17694, 0.5500000000000001554 ) ;
#4145=EDGE_CURVE ( 'NONE', #4287, #17972, #21118, .T. ) ;
#4149=FACE_OUTER_BOUND ( 'NONE', #4950, .T. ) ;
#4152=CARTESIAN_POINT ( 'NONE',  ( 0.5506292728288999516, 30.59193204632999752, -2.290976999470999864 ) ) ;
#4153=AXIS2_PLACEMENT_3D ( 'NONE', #13039, #192, #15083 ) ;
#4157=CARTESIAN_POINT ( 'NONE',  ( -0.4240070336381018823, 29.57875158174377717, 2.118275460938266797 ) ) ;
#4158=ORIENTED_EDGE ( 'NONE', *, *, #2148, .F. ) ;
#4161=CARTESIAN_POINT ( 'NONE',  ( -2.047002538946999906, 25.14301022640000127, -0.7667419757990000528 ) ) ;
#4164=DIRECTION ( 'NONE',  ( 0.000000000000000000, 1.000000000000000000, 0.000000000000000000 ) ) ;
#4166=DIRECTION ( 'NONE',  ( 0.000000000000000000, -1.000000000000000000, 0.000000000000000000 ) ) ;
#4172=EDGE_CURVE ( 'NONE', #5160, #15484, #16476, .T. ) ;
#4182=CARTESIAN_POINT ( 'NONE',  ( 0.8545932710616224171, 26.39685207198635553, -4.125402498422513276 ) ) ;
#4183=CARTESIAN_POINT ( 'NONE',  ( 2.500000000000000000, 24.40000000000000213, 0.000000000000000000 ) ) ;
#4184=EDGE_CURVE ( 'NONE', #17924, #9190, #11514, .T. ) ;
#4185=CARTESIAN_POINT ( 'NONE',  ( 0.9032590285184615153, 30.45886934512990152, 1.961921808037713655 ) ) ;
#4190=AXIS2_PLACEMENT_3D ( 'NONE', #2188, #15374, #9701 ) ;
#4192=CARTESIAN_POINT ( 'NONE',  ( -1.287118485750000207, 28.29196440325999973, -2.100366574696000299 ) ) ;
#4193=CARTESIAN_POINT ( 'NONE',  ( 0.000000000000000000, 20.00000000000000000, 0.000000000000000000 ) ) ;
#4195=EDGE_CURVE ( 'NONE', #18500, #4867, #10744, .T. ) ;
#4199=AXIS2_PLACEMENT_3D ( 'NONE', #2510, #3978, #11372 ) ;
#4200=AXIS2_PLACEMENT_3D ( 'NONE', #21126, #19561, #6706 ) ;
#4201=DIRECTION ( 'NONE',  ( 0.000000000000000000, 1.000000000000000000, 0.000000000000000000 ) ) ;
#4202=ORIENTED_EDGE ( 'NONE', *, *, #17493, .T. ) ;
#4217=DIRECTION ( 'NONE',  ( -1.511005198495999796E-08, -0.9999999999999997780, -8.997177385936997916E-09 ) ) ;
#4220=CARTESIAN_POINT ( 'NONE',  ( 1.777466727206999941, 26.97500240009999928, -2.254705796085000102 ) ) ;
#4222=CARTESIAN_POINT ( 'NONE',  ( 2.122476591467600038, 29.02756187265872256, -0.4001553311762567899 ) ) ;
#4224=ORIENTED_EDGE ( 'NONE', *, *, #6447, .F. ) ;
#4225=CARTESIAN_POINT ( 'NONE',  ( 2.270871215252209030, 18.00000000000000000, 0.000000000000000000 ) ) ;
#4231=CARTESIAN_POINT ( 'NONE',  ( 1.107772814030999919, 25.82549822781000159, -1.978081431919000099 ) ) ;
#4235=AXIS2_PLACEMENT_3D ( 'NONE', #4193, #3963, #19205 ) ;
#4236=EDGE_CURVE ( 'NONE', #10806, #12888, #2328, .T. ) ;
#4239=AXIS2_PLACEMENT_3D ( 'NONE', #21688, #8487, #1457 ) ;
#4243=ORIENTED_EDGE ( 'NONE', *, *, #22670, .T. ) ;
#4244=CARTESIAN_POINT ( 'NONE',  ( -1.089863560591000091, 30.60758970965000003, 2.496295939784000328 ) ) ;
#4245=CARTESIAN_POINT ( 'NONE',  ( -2.393157034060999777, 24.23821659520999816, -0.8070405077446000108 ) ) ;
#4250=ADVANCED_FACE ( 'NONE', ( #18382 ), #3851, .T. ) ;
#4252=EDGE_CURVE ( 'NONE', #7057, #3560, #13819, .T. ) ;
#4254=CARTESIAN_POINT ( 'NONE',  ( 0.000000000000000000, 14.95000002005000006, 0.000000000000000000 ) ) ;
#4257=ORIENTED_EDGE ( 'NONE', *, *, #20883, .F. ) ;
#4259=VERTEX_POINT ( 'NONE', #5435 ) ;
#4262=CARTESIAN_POINT ( 'NONE',  ( -2.500000000000000000, 24.00000000000000000, 8.181116922990998136E-14 ) ) ;
#4264=LINE ( 'NONE', #8007, #18846 ) ;
#4265=AXIS2_PLACEMENT_3D ( 'NONE', #176, #17137, #7698 ) ;
#4269=VERTEX_POINT ( 'NONE', #20320 ) ;
#4273=DIRECTION ( 'NONE',  ( 0.000000000000000000, 1.000000000000000000, 0.000000000000000000 ) ) ;
#4280=CARTESIAN_POINT ( 'NONE',  ( -1.876762163929999838, 29.36394619264999761, -1.125344217945999814 ) ) ;
#4283=CARTESIAN_POINT ( 'NONE',  ( 1.512189683744231905, 29.70242366392465527, 1.543056007447467737 ) ) ;
#4285=CARTESIAN_POINT ( 'NONE',  ( -1.447949418204000027, 25.10653475033999982, -1.849518100036999790 ) ) ;
#4287=VERTEX_POINT ( 'NONE', #7356 ) ;
#4289=CARTESIAN_POINT ( 'NONE',  ( -2.500000000000000000, 27.43419673618999965, 0.000000000000000000 ) ) ;
#4296=CARTESIAN_POINT ( 'NONE',  ( 0.000000000000000000, 20.05000017415440183, -3.049999825846000157 ) ) ;
#4303=DIRECTION ( 'NONE',  ( 1.000000000000000000, 0.000000000000000000, 0.000000000000000000 ) ) ;
#4304=CARTESIAN_POINT ( 'NONE',  ( -4.724999978625000097, 14.90000002138000035, -2.519184009061999785E-09 ) ) ;
#4305=( LENGTH_UNIT ( ) NAMED_UNIT ( * ) SI_UNIT ( .MILLI., .METRE. ) );
#4307=CARTESIAN_POINT ( 'NONE',  ( 0.9439321425118507580, 30.46150519779229526, 1.942806962222955791 ) ) ;
#4314=CARTESIAN_POINT ( 'NONE',  ( 1.419229835182000077, 26.50364211381999979, -1.800284464616000113 ) ) ;
#4315=CARTESIAN_POINT ( 'NONE',  ( -3.824747491000654698, 24.75094615491947891, -2.410583160005970171 ) ) ;
#4316=ORIENTED_EDGE ( 'NONE', *, *, #21183, .T. ) ;
#4318=DIRECTION ( 'NONE',  ( 0.8500000000000165201, 0.000000000000000000, -0.5267826876426102700 ) ) ;
#4319=CARTESIAN_POINT ( 'NONE',  ( 0.000000000000000000, 20.05000017415440183, 0.000000000000000000 ) ) ;
#4320=APPLICATION_CONTEXT ( 'automotive_design' ) ;
#4330=CARTESIAN_POINT ( 'NONE',  ( -0.6543697108981785249, 28.96666666666666501, 2.434931691670795484 ) ) ;
#4333=CARTESIAN_POINT ( 'NONE',  ( -2.381850618623087001, 26.58949608044243718, -0.8771401830057823368 ) ) ;
#4334=ORIENTED_EDGE ( 'NONE', *, *, #10576, .T. ) ;
#4336=CARTESIAN_POINT ( 'NONE',  ( 2.554499528901000183, 25.99206776952000197, -0.7744564004552999537 ) ) ;
#4338=CARTESIAN_POINT ( 'NONE',  ( 2.050298679598668183, 28.96300717529661028, 0.6792431909432838921 ) ) ;
#4344=CARTESIAN_POINT ( 'NONE',  ( 0.000000000000000000, -1.550000000000000044, 0.000000000000000000 ) ) ;
#4345=CARTESIAN_POINT ( 'NONE',  ( 0.5271288625574210851, 26.26111511314614688, 2.095841999210956264 ) ) ;
#4354=CARTESIAN_POINT ( 'NONE',  ( 0.000000000000000000, 20.00000000000000000, 0.000000000000000000 ) ) ;
#4355=ORIENTED_EDGE ( 'NONE', *, *, #14435, .T. ) ;
#4356=CARTESIAN_POINT ( 'NONE',  ( 1.600110441081000090, 30.73994915060000110, 2.204300939401000026 ) ) ;
#4357=CARTESIAN_POINT ( 'NONE',  ( -1.707744019578999906, 24.17417548081000334, -1.860678729632000206 ) ) ;
#4361=CARTESIAN_POINT ( 'NONE',  ( 1.600279783570000003, 30.05341750703000159, 2.231095953505000118 ) ) ;
#4362=CARTESIAN_POINT ( 'NONE',  ( -3.100000000000000089, 20.00000000000000000, 0.000000000000000000 ) ) ;
#4363=CARTESIAN_POINT ( 'NONE',  ( 0.000000000000000000, 21.89999999999999858, 0.000000000000000000 ) ) ;
#4367=CARTESIAN_POINT ( 'NONE',  ( 2.500000000000000000, 29.45086340285666537, -0.3272492347489373565 ) ) ;
#4369=EDGE_CURVE ( 'NONE', #2983, #20057, #11894, .T. ) ;
#4374=B_SPLINE_SURFACE_WITH_KNOTS ( 'NONE', 3, 3, ( 
 ( #3490, #16770, #14722, #10870, #179, #18255, #7570, #1657, #18365, #22119, #9046, #21773, #7217, #19955, #3374, #10753, #1550, #1776, #10153, #20810, #17539, #447, #934, #4220, #7970, #15341, #13769, #22614, #4097, #19228, #8332, #15699, #8099, #816, #11612 ),
 ( #15466, #2394, #2768, #18983, #23088, #563, #2513, #22852, #9783, #6265, #22731, #8216, #11849, #2642, #6513, #17049, #20688, #17169, #11493, #7850, #18870, #6145, #13534, #20930, #21171, #6023, #2275, #10037, #9668, #15217, #13649, #15583, #4336, #13409, #11728 ),
 ( #17422, #21046, #4458, #19362, #19102, #9904, #17291, #693, #22970, #6386, #4583, #11974, #1433, #19481, #8941, #4953, #12097, #16065, #12459, #16190, #23591, #21778, #12338, #4829, #19842, #23701, #12572, #23337, #6995, #14384, #19730, #21664, #1059, #8582, #15943 ),
 ( #6633, #3141, #18027, #2891, #5190, #8460, #19960, #5077, #8700, #21414, #6752, #14145, #21540, #3379, #10760, #3012, #10525, #23462, #10271, #12214, #17908, #8828, #21299, #19604, #1312, #15827, #18153, #1557, #6874, #10399, #17791, #14266, #3255, #14023, #16309 ) ),
 .UNSPECIFIED., .F., .F., .F.,
 ( 4, 4 ),
 ( 4, 1, 1, 1, 1, 1, 1, 1, 1, 1, 1, 1, 1, 1, 1, 1, 1, 1, 1, 1, 1, 1, 1, 1, 1, 1, 1, 1, 1, 1, 1, 1, 4 ),
 ( -0.3056682515952000023, 1.305668251594999996 ),
 ( -0.02000000000000000042, 0.01250000000000000069, 0.04499999999999999833, 0.07749999999999999944, 0.1100000000000000006, 0.1424999999999999878, 0.1749999999999999889, 0.2074999999999999900, 0.2399999999999999911, 0.2725000000000000200, 0.3049999999999999933, 0.3375000000000000222, 0.3699999999999999956, 0.4025000000000000244, 0.4349999999999999978, 0.4675000000000000266, 0.5000000000000000000, 0.5324999999999999734, 0.5649999999999999467, 0.5975000000000000311, 0.6300000000000000044, 0.6624999999999999778, 0.6949999999999999512, 0.7275000000000000355, 0.7600000000000000089, 0.7924999999999999822, 0.8249999999999999556, 0.8575000000000000400, 0.8900000000000000133, 0.9224999999999999867, 0.9549999999999999600, 0.9875000000000000444, 1.020000000000000018 ),
 .UNSPECIFIED. ) ;
#4377=CARTESIAN_POINT ( 'NONE',  ( 0.4070492355296851938, 24.37989684473771845, -2.155747726877813797 ) ) ;
#4380=DIRECTION ( 'NONE',  ( -0.000000000000000000, 1.000000000000000000, 0.000000000000000000 ) ) ;
#4382=ADVANCED_FACE ( 'NONE', ( #10259 ), #1461, .T. ) ;
#4383=EDGE_LOOP ( 'NONE', ( #20928, #11277, #12848, #3911 ) ) ;
#4384=ORIENTED_EDGE ( 'NONE', *, *, #10887, .F. ) ;
#4390=AXIS2_PLACEMENT_3D ( 'NONE', #8983, #23856, #3758 ) ;
#4395=CARTESIAN_POINT ( 'NONE',  ( 1.835060406389813270, 24.49999999999984368, 3.559329533908949461 ) ) ;
#4400=CARTESIAN_POINT ( 'NONE',  ( -1.507258510594286616, 29.50557409157621436, 1.546987692870358089 ) ) ;
#4406=AXIS2_PLACEMENT_3D ( 'NONE', #22894, #12018, #21336 ) ;
#4410=CARTESIAN_POINT ( 'NONE',  ( 0.6543697108981982868, 26.96666666666666501, -2.434931691670790155 ) ) ;
#4412=ORIENTED_EDGE ( 'NONE', *, *, #12950, .T. ) ;
#4414=CARTESIAN_POINT ( 'NONE',  ( -1.670832290882946713, 24.71086476070425419, 1.427778279994880606 ) ) ;
#4418=CARTESIAN_POINT ( 'NONE',  ( 0.000000000000000000, 19.00000000000000000, 0.000000000000000000 ) ) ;
#4424=DIRECTION ( 'NONE',  ( 0.000000000000000000, -1.000000000000000000, 0.000000000000000000 ) ) ;
#4425=CARTESIAN_POINT ( 'NONE',  ( 2.500000000000000000, 28.63419673618999894, 0.000000000000000000 ) ) ;
#4427=CARTESIAN_POINT ( 'NONE',  ( -0.6004538078361787434, 30.36805637628708610, 2.074802447086620649 ) ) ;
#4428=ORIENTED_EDGE ( 'NONE', *, *, #5244, .F. ) ;
#4433=DIRECTION ( 'NONE',  ( 0.000000000000000000, 1.000000000000000000, 0.000000000000000000 ) ) ;
#4434=CARTESIAN_POINT ( 'NONE',  ( 1.992911166421000191, 26.34196440326000044, 1.447934651311999943 ) ) ;
#4436=ORIENTED_EDGE ( 'NONE', *, *, #8654, .F. ) ;
#4439=AXIS2_PLACEMENT_3D ( 'NONE', #5223, #16097, #21921 ) ;
#4440=CARTESIAN_POINT ( 'NONE',  ( 2.059621423746683888, 27.98870470916865472, 0.6859841289820139965 ) ) ;
#4455=CARTESIAN_POINT ( 'NONE',  ( -1.940710640446570823, 26.54479542469487185, -1.635918543245983070 ) ) ;
#4458=CARTESIAN_POINT ( 'NONE',  ( -0.7160459369171999766, 28.81163313895000044, 2.361836001938000251 ) ) ;
#4459=AXIS2_PLACEMENT_3D ( 'NONE', #23240, #17930, #15965 ) ;
#4461=CARTESIAN_POINT ( 'NONE',  ( 2.009434425284166714, 29.05181478867270783, -0.7974684545092869392 ) ) ;
#4469=LINE ( 'NONE', #6035, #16884 ) ;
#4479=CARTESIAN_POINT ( 'NONE',  ( 2.083590786046000343, 25.28552202384999958, 1.742323173877000198 ) ) ;
#4484=CARTESIAN_POINT ( 'NONE',  ( -2.000000000000000000, 18.89999999999999858, 0.000000000000000000 ) ) ;
#4489=EDGE_CURVE ( 'NONE', #903, #10311, #9568, .T. ) ;
#4495=CARTESIAN_POINT ( 'NONE',  ( -1.401027947687027320, 24.49235475105247772, -1.687018025696104040 ) ) ;
#4502=ORIENTED_EDGE ( 'NONE', *, *, #2004, .T. ) ;
#4503=ORIENTED_EDGE ( 'NONE', *, *, #15315, .F. ) ;
#4505=CARTESIAN_POINT ( 'NONE',  ( 2.649379677055639259, 24.52555747447238588, 3.089210087447479491 ) ) ;
#4508=ORIENTED_EDGE ( 'NONE', *, *, #17535, .T. ) ;
#4510=CARTESIAN_POINT ( 'NONE',  ( 3.099999999996331468, 15.00000000000000000, 5.570939913765761767E-07 ) ) ;
#4511=AXIS2_PLACEMENT_3D ( 'NONE', #18991, #13657, #8108 ) ;
#4512=LINE ( 'NONE', #11903, #993 ) ;
#4516=CARTESIAN_POINT ( 'NONE',  ( 0.3502059142680099546, 24.70197603011302334, 4.416610674642952539 ) ) ;
#4518=DIRECTION ( 'NONE',  ( 1.000000000000000000, 0.000000000000000000, 0.000000000000000000 ) ) ;
#4519=CARTESIAN_POINT ( 'NONE',  ( -1.819570094927574155, 29.47616403948960695, 1.164058689780290035 ) ) ;
#4521=ORIENTED_EDGE ( 'NONE', *, *, #15001, .F. ) ;
#4523=CARTESIAN_POINT ( 'NONE',  ( 0.5161842332063000249, 23.85017497135000042, 2.291468635377000407 ) ) ;
#4525=VECTOR ( 'NONE', #4201, 1000.000000000000000 ) ;
#4529=AXIS2_PLACEMENT_3D ( 'NONE', #12413, #1506, #14216 ) ;
#4535=DIRECTION ( 'NONE',  ( 0.000000000000000000, 0.000000000000000000, -1.000000000000000000 ) ) ;
#4537=CARTESIAN_POINT ( 'NONE',  ( 4.000000000000000000, 26.41693820796410108, -1.184172465503444904 ) ) ;
#4546=AXIS2_PLACEMENT_3D ( 'NONE', #10652, #7233, #21902 ) ;
#4547=CARTESIAN_POINT ( 'NONE',  ( 2.273493636278927976, 26.37349363267965074, -0.1540032442819480318 ) ) ;
#4551=CARTESIAN_POINT ( 'NONE',  ( -2.146022825185431859, 30.18926127037506646, -0.2447506456446620349 ) ) ;
#4552=EDGE_CURVE ( 'NONE', #23163, #11582, #6373, .T. ) ;
#4557=CARTESIAN_POINT ( 'NONE',  ( -2.434931691670788378, 27.46753006952333109, 0.6543697108982053923 ) ) ;
#4560=CIRCLE ( 'NONE', #3419, 3.000000000000000000 ) ;
#4561=AXIS2_PLACEMENT_3D ( 'NONE', #21253, #9359, #7177 ) ;
#4563=ORIENTED_EDGE ( 'NONE', *, *, #14508, .T. ) ;
#4564=DIRECTION ( 'NONE',  ( 0.000000000000000000, 1.000000000000000000, 0.000000000000000000 ) ) ;
#4565=CARTESIAN_POINT ( 'NONE',  ( 0.5551539414043799026, 26.26248452079970619, 2.089084675604010233 ) ) ;
#4566=CARTESIAN_POINT ( 'NONE',  ( -0.2092130522973276729, 28.61742282545599281, 2.160054418272680632 ) ) ;
#4567=ORIENTED_EDGE ( 'NONE', *, *, #11737, .T. ) ;
#4573=CARTESIAN_POINT ( 'NONE',  ( -0.1752525090037950484, 24.75094615491814665, 4.517620070267612142 ) ) ;
#4575=CARTESIAN_POINT ( 'NONE',  ( -1.606544753322670216, 28.69849995987307523, 1.460805988974954728 ) ) ;
#4576=AXIS2_PLACEMENT_3D ( 'NONE', #10584, #1374, #16127 ) ;
#4577=CARTESIAN_POINT ( 'NONE',  ( -0.3272492347489284192, 26.81753006952333251, 2.500000000000001332 ) ) ;
#4578=DIRECTION ( 'NONE',  ( 0.000000000000000000, -1.000000000000000000, 0.000000000000000000 ) ) ;
#4583=CARTESIAN_POINT ( 'NONE',  ( -0.3381971108622000011, 28.03163313894999931, 2.445091418594000032 ) ) ;
#4585=CARTESIAN_POINT ( 'NONE',  ( 0.9799592777482039052, 28.86341118070886225, 1.932436292759031726 ) ) ;
#4587=AXIS2_PLACEMENT_3D ( 'NONE', #15698, #23087, #21539 ) ;
#4590=AXIS2_PLACEMENT_3D ( 'NONE', #19971, #14510, #21903 ) ;
#4599=CARTESIAN_POINT ( 'NONE',  ( 1.999167105995449445, 27.11753006952333322, -1.536366799937288530 ) ) ;
#4603=CIRCLE ( 'NONE', #20848, 3.100000000000000089 ) ;
#4604=ORIENTED_EDGE ( 'NONE', *, *, #14673, .F. ) ;
#4606=CARTESIAN_POINT ( 'NONE',  ( -1.031996076613000080, 31.00953293605000027, -2.230181950283000258 ) ) ;
#4607=DIRECTION ( 'NONE',  ( -0.000000000000000000, 1.000000000000000000, -0.000000000000000000 ) ) ;
#4622=AXIS2_PLACEMENT_3D ( 'NONE', #13448, #6057, #20850 ) ;
#4624=CARTESIAN_POINT ( 'NONE',  ( 0.7194182799258999061, 25.89386557969000080, 2.640899101350000056 ) ) ;
#4625=CARTESIAN_POINT ( 'NONE',  ( -0.3561344694547327050, 24.42488000727052011, -2.163805914283786880 ) ) ;
#4627=VECTOR ( 'NONE', #21697, 1000.000000000000227 ) ;
#4631=CARTESIAN_POINT ( 'NONE',  ( 2.747163055864000114, 25.41169433610000183, -0.8328668639933000106 ) ) ;
#4632=EDGE_LOOP ( 'NONE', ( #10454, #8516 ) ) ;
#4633=ORIENTED_EDGE ( 'NONE', *, *, #20520, .F. ) ;
#4638=EDGE_CURVE ( 'NONE', #12888, #2273, #980, .T. ) ;
#4643=CONICAL_SURFACE ( 'NONE', #14307, 2.849999992212000066, 0.7853981633972997312 ) ;
#4649=CARTESIAN_POINT ( 'NONE',  ( -1.913666731007989785, 29.46549386981544316, 1.007641490493420777 ) ) ;
#4651=CARTESIAN_POINT ( 'NONE',  ( -1.347470520100000124, 25.07321246089999889, -1.721172773618999896 ) ) ;
#4653=CONICAL_SURFACE ( 'NONE', #18200, 3.049999825846000157, 0.7853981633972997312 ) ;
#4664=CARTESIAN_POINT ( 'NONE',  ( 2.500000000000000000, 26.81666666666667354, -0.3272492347489370235 ) ) ;
#4677=DIRECTION ( 'NONE',  ( 1.000000000000000000, 0.000000000000000000, 0.000000000000000000 ) ) ;
#4679=CARTESIAN_POINT ( 'NONE',  ( -2.144040404256133847, 30.18827354168691812, -0.2615996283942206291 ) ) ;
#4684=CARTESIAN_POINT ( 'NONE',  ( -1.976671150083846973, 23.62257745056772862, -0.7977860612064010537 ) ) ;
#4686=CARTESIAN_POINT ( 'NONE',  ( 0.2604860018441254588, 24.64510472144360165, 2.238162498141799794 ) ) ;
#4690=ORIENTED_EDGE ( 'NONE', *, *, #2225, .F. ) ;
#4697=ORIENTED_EDGE ( 'NONE', *, *, #3215, .F. ) ;
#4698=EDGE_CURVE ( 'NONE', #1429, #23795, #19020, .T. ) ;
#4706=CARTESIAN_POINT ( 'NONE',  ( -3.999999999999998224, 26.44682129341587640, -0.9440428258622635127 ) ) ;
#4709=CARTESIAN_POINT ( 'NONE',  ( 0.000000000000000000, 24.65000000000000213, 0.000000000000000000 ) ) ;
#4710=VERTEX_POINT ( 'NONE', #4938 ) ;
#4712=CARTESIAN_POINT ( 'NONE',  ( -0.8137643771028287842, 24.74949622857204901, 2.006896345404644233 ) ) ;
#4713=DIRECTION ( 'NONE',  ( 1.000000000000000000, 0.000000000000000000, 0.000000000000000000 ) ) ;
#4715=DIRECTION ( 'NONE',  ( 0.000000000000000000, 1.000000000000000000, 0.000000000000000000 ) ) ;
#4722=CYLINDRICAL_SURFACE ( 'NONE', #14841, 2.500000000000000000 ) ;
#4729=CARTESIAN_POINT ( 'NONE',  ( 0.5028989451434000557, 28.98002150817000100, 2.482341192449999845 ) ) ;
#4731=CARTESIAN_POINT ( 'NONE',  ( -2.629981577853999664, 23.38563562995999945, 0.2328718829719999828 ) ) ;
#4735=DIRECTION ( 'NONE',  ( 0.000000000000000000, -1.000000000000000000, 0.000000000000000000 ) ) ;
#4736=CARTESIAN_POINT ( 'NONE',  ( -1.018158653951999781, 29.62256419343999880, -2.549909324983000047 ) ) ;
#4739=FACE_OUTER_BOUND ( 'NONE', #14733, .T. ) ;
#4740=CIRCLE ( 'NONE', #12085, 3.100000000000000089 ) ;
#4741=CARTESIAN_POINT ( 'NONE',  ( 0.000000000000000000, 20.00000000000000000, -3.100000000000386002 ) ) ;
#4744=DIRECTION ( 'NONE',  ( 0.000000000000000000, 0.7071067811866525998, -0.7071067811864425456 ) ) ;
#4747=CARTESIAN_POINT ( 'NONE',  ( 2.600121693191999928, 24.50045998918000123, -0.8551739725367000222 ) ) ;
#4753=CARTESIAN_POINT ( 'NONE',  ( -1.595084814687000030, 25.89919433610000254, 2.387212940976999764 ) ) ;
#4754=ORIENTED_EDGE ( 'NONE', *, *, #7620, .T. ) ;
#4757=DIRECTION ( 'NONE',  ( 0.000000000000000000, 0.000000000000000000, -1.000000000000000000 ) ) ;
#4761=DIRECTION ( 'NONE',  ( 0.000000000000000000, 0.000000000000000000, -1.000000000000000000 ) ) ;
#4770=CARTESIAN_POINT ( 'NONE',  ( -1.854515264472811786, 29.47225744612200060, 1.107362145631518136 ) ) ;
#4772=DIRECTION ( 'NONE',  ( 1.000000000000000000, 0.000000000000000000, 0.000000000000000000 ) ) ;
#4785=DIRECTION ( 'NONE',  ( 0.000000000000000000, 0.000000000000000000, -1.000000000000000000 ) ) ;
#4786=EDGE_LOOP ( 'NONE', ( #9976, #17842, #12505 ) ) ;
#4788=DIRECTION ( 'NONE',  ( -1.000000000000000000, 0.000000000000000000, 0.000000000000000000 ) ) ;
#4791=AXIS2_PLACEMENT_3D ( 'NONE', #17101, #2562, #7900 ) ;
#4797=CARTESIAN_POINT ( 'NONE',  ( -1.931946195963927915, 30.14479945992585641, -0.9657778908081225966 ) ) ;
#4802=CARTESIAN_POINT ( 'NONE',  ( -1.999167105995446780, 27.51753006952333180, 1.536366799937292305 ) ) ;
#4804=CARTESIAN_POINT ( 'NONE',  ( 2.151661648330430943, 24.06873469183733860, -0.6690115951027478802 ) ) ;
#4806=EDGE_CURVE ( 'NONE', #15484, #18419, #18327, .T. ) ;
#4810=CARTESIAN_POINT ( 'NONE',  ( -4.000000142211483478, 24.55137445130720053, -0.9449696197475782045 ) ) ;
#4811=CARTESIAN_POINT ( 'NONE',  ( -1.250502274040745654, 26.95316898822477114, 1.812620555901804265 ) ) ;
#4812=EDGE_CURVE ( 'NONE', #6384, #12389, #7691, .T. ) ;
#4818=EDGE_CURVE ( 'NONE', #18419, #23934, #3940, .T. ) ;
#4827=CONICAL_SURFACE ( 'NONE', #19523, 2.249999993254999886, 0.7853981633972997312 ) ;
#4829=CARTESIAN_POINT ( 'NONE',  ( 1.528152797339000113, 26.76413313895000101, -1.938452583514000072 ) ) ;
#4838=DIRECTION ( 'NONE',  ( 0.000000000000000000, 1.000000000000000000, 0.000000000000000000 ) ) ;
#4840=DIRECTION ( 'NONE',  ( 0.000000000000000000, 0.000000000000000000, -1.000000000000000000 ) ) ;
#4844=CARTESIAN_POINT ( 'NONE',  ( -1.235289751754999887, 30.50000000000000000, -2.173490103315000255 ) ) ;
#4848=VERTEX_POINT ( 'NONE', #22459 ) ;
#4850=CARTESIAN_POINT ( 'NONE',  ( -2.498205606922999866, 29.57563899243999828, 0.4172517292406999756 ) ) ;
#4851=FACE_OUTER_BOUND ( 'NONE', #6824, .T. ) ;
#4853=AXIS2_PLACEMENT_3D ( 'NONE', #960, #6412, #13796 ) ;
#4854=ORIENTED_EDGE ( 'NONE', *, *, #4252, .F. ) ;
#4855=CARTESIAN_POINT ( 'NONE',  ( -0.1529142988638288181, 26.50000000000000355, -2.395123632968240823 ) ) ;
#4856=DIRECTION ( 'NONE',  ( 0.000000000000000000, 0.000000000000000000, 1.000000000000000000 ) ) ;
#4858=DIRECTION ( 'NONE',  ( 0.000000000000000000, -1.000000000000000000, 0.000000000000000000 ) ) ;
#4860=FACE_OUTER_BOUND ( 'NONE', #5036, .T. ) ;
#4862=FACE_OUTER_BOUND ( 'NONE', #4888, .T. ) ;
#4863=EDGE_LOOP ( 'NONE', ( #5248, #105, #4224, #7535 ) ) ;
#4865=CARTESIAN_POINT ( 'NONE',  ( 0.000000000000000000, 26.35000000000000142, 0.000000000000000000 ) ) ;
#4867=VERTEX_POINT ( 'NONE', #4057 ) ;
#4868=CARTESIAN_POINT ( 'NONE',  ( -2.694750659793999858, 24.08243831202999985, 0.4798224739857999688 ) ) ;
#4873=CARTESIAN_POINT ( 'NONE',  ( -1.999167105995452998, 27.91666666666667140, -1.536366799937284089 ) ) ;
#4874=DIRECTION ( 'NONE',  ( 0.000000000000000000, -0.7071067811866525998, -0.7071067811864425456 ) ) ;
#4878=CARTESIAN_POINT ( 'NONE',  ( -4.000000000000000000, 24.80000000000000426, 2.309401076759000304 ) ) ;
#4884=AXIS2_PLACEMENT_3D ( 'NONE', #1117, #23642, #15992 ) ;
#4885=CARTESIAN_POINT ( 'NONE',  ( 2.000000000000000000, 24.50000000000000000, 3.464101615137999968 ) ) ;
#4888=EDGE_LOOP ( 'NONE', ( #4355, #18232, #17096 ) ) ;
#4891=CARTESIAN_POINT ( 'NONE',  ( -1.653388338670852109, 29.31485580340598318, -1.389752403157769045 ) ) ;
#4892=ORIENTED_EDGE ( 'NONE', *, *, #12504, .T. ) ;
#4895=EDGE_LOOP ( 'NONE', ( #20024, #22602, #8193, #8635, #18617, #17609 ) ) ;
#4902=AXIS2_PLACEMENT_3D ( 'NONE', #9585, #3663, #20498 ) ;
#4905=AXIS2_PLACEMENT_3D ( 'NONE', #6681, #6929, #4761 ) ;
#4917=CARTESIAN_POINT ( 'NONE',  ( -2.015675766250876855, 30.15706052976086937, -0.7768981003585021528 ) ) ;
#4918=ORIENTED_EDGE ( 'NONE', *, *, #16011, .T. ) ;
#4923=CARTESIAN_POINT ( 'NONE',  ( -1.709420958921680223, 23.61501560995045779, -1.257455528530935229 ) ) ;
#4928=EDGE_LOOP ( 'NONE', ( #20763, #18486, #18303, #13809 ) ) ;
#4932=EDGE_LOOP ( 'NONE', ( #16729, #5253, #1972, #10010 ) ) ;
#4934=CARTESIAN_POINT ( 'NONE',  ( 1.154873175401071261, 27.10110266264532797, 1.837081552305992016 ) ) ;
#4938=CARTESIAN_POINT ( 'NONE',  ( 0.000000000000000000, 26.20000000000000284, -4.618802153517000519 ) ) ;
#4945=B_SPLINE_CURVE_WITH_KNOTS ( 'NONE', 3,
 ( #769, #4664, #11927, #6592, #1012, #8414, #15899, #4410, #2590, #9979, #8169, #22924, #10104, #17491, #15653, #23044, #19558, #12049 ),
 .UNSPECIFIED., .F., .F.,
 ( 4, 2, 2, 2, 2, 2, 2, 2, 4 ),
 ( 0.000000000000000000, 0.1250000000000000555, 0.2500000000000001110, 0.3750000000000000555, 0.5000000000000000000, 0.6249999999999998890, 0.7499999999999998890, 0.8749999999999998890, 1.000000000000000000 ),
 .UNSPECIFIED. ) ;
#4947=DIRECTION ( 'NONE',  ( 0.000000000000000000, -1.000000000000000000, 0.000000000000000000 ) ) ;
#4950=EDGE_LOOP ( 'NONE', ( #3188, #298, #4521, #2106 ) ) ;
#4953=CARTESIAN_POINT ( 'NONE',  ( 1.812579491195999815, 27.54413313894999860, -1.675531247043999805 ) ) ;
#4954=CIRCLE ( 'NONE', #18810, 1.399999999999999911 ) ;
#4960=EDGE_LOOP ( 'NONE', ( #21615, #395, #5428 ) ) ;
#4962=EDGE_CURVE ( 'NONE', #953, #18033, #19418, .T. ) ;
#4965=CARTESIAN_POINT ( 'NONE',  ( 2.111585849641928192, 30.38130037447719900, 0.8546615592128204986 ) ) ;
#4966=B_SPLINE_CURVE_WITH_KNOTS ( 'NONE', 3,
 ( #18681, #5949, #15840, #20616, #1073, #16853, #6642, #13783, #256, #11303, #7661, #21184, #4026, #4599, #19373, #10168, #11421, #18793 ),
 .UNSPECIFIED., .F., .F.,
 ( 4, 2, 2, 2, 2, 2, 2, 2, 4 ),
 ( 0.000000000000000000, 0.1250000000000000555, 0.2500000000000000555, 0.3750000000000000555, 0.5000000000000000000, 0.6249999999999998890, 0.7499999999999998890, 0.8749999999999998890, 1.000000000000000000 ),
 .UNSPECIFIED. ) ;
#4967=CYLINDRICAL_SURFACE ( 'NONE', #4546, 3.000000000000000000 ) ;
#4975=CARTESIAN_POINT ( 'NONE',  ( 0.5408282081481999848, 29.08545613873999969, 2.669562448062999582 ) ) ;
#4980=DIRECTION ( 'NONE',  ( 0.000000000000000000, -1.000000000000000000, 0.000000000000000000 ) ) ;
#4982=CYLINDRICAL_SURFACE ( 'NONE', #17378, 2.500000000000000000 ) ;
#4988=VERTEX_POINT ( 'NONE', #2475 ) ;
#4989=DIRECTION ( 'NONE',  ( 0.000000000000000000, 0.000000000000000000, 1.000000000000000000 ) ) ;
#4990=CARTESIAN_POINT ( 'NONE',  ( 1.712379611124581258, 12.94862384910287467, 1.057050596558879452 ) ) ;
#4993=CARTESIAN_POINT ( 'NONE',  ( 2.665416330148000057, 24.43078970964999996, 0.6225038595752000470 ) ) ;
#4995=CARTESIAN_POINT ( 'NONE',  ( 0.3272492347489618925, 28.45086340285666182, 2.499999999999996447 ) ) ;
#4997=EDGE_CURVE ( 'NONE', #15990, #3964, #5497, .T. ) ;
#5002=ORIENTED_EDGE ( 'NONE', *, *, #10609, .F. ) ;
#5004=CARTESIAN_POINT ( 'NONE',  ( -2.434931691670788378, 29.86753006952333678, 0.6543697108982053923 ) ) ;
#5005=CARTESIAN_POINT ( 'NONE',  ( -1.212947244561992655, 26.21668223261122677, 1.752979114926064508 ) ) ;
#5010=DIRECTION ( 'NONE',  ( 0.7071067811823850136, -0.7071067811898851252, 1.080116765722976056E-06 ) ) ;
#5012=AXIS2_PLACEMENT_3D ( 'NONE', #8164, #9294, #11108 ) ;
#5014=CARTESIAN_POINT ( 'NONE',  ( -0.8966937801068000091, 29.43620588595999976, 1.973860271291999702 ) ) ;
#5017=ORIENTED_EDGE ( 'NONE', *, *, #23568, .F. ) ;
#5018=CARTESIAN_POINT ( 'NONE',  ( -1.074254588831038193, 26.46059486951026685, 2.123687106836487981 ) ) ;
#5020=CARTESIAN_POINT ( 'NONE',  ( -1.503657042384516807, 29.30187328459274809, -1.552941005774420180 ) ) ;
#5021=VERTEX_POINT ( 'NONE', #6470 ) ;
#5022=CARTESIAN_POINT ( 'NONE',  ( 1.536366799937286087, 29.31666666666665932, -1.999167105995451665 ) ) ;
#5026=DIRECTION ( 'NONE',  ( 1.000000000000000000, 0.000000000000000000, 0.000000000000000000 ) ) ;
#5027=CARTESIAN_POINT ( 'NONE',  ( 0.000000000000000000, 18.50000000000000000, 0.000000000000000000 ) ) ;
#5031=ORIENTED_EDGE ( 'NONE', *, *, #464, .T. ) ;
#5035=CIRCLE ( 'NONE', #4235, 4.649999999999999467 ) ;
#5036=EDGE_LOOP ( 'NONE', ( #10406, #21931, #8886, #14195, #20613 ) ) ;
#5044=CARTESIAN_POINT ( 'NONE',  ( -2.036516393111000411, 31.06645568193000173, 0.5573742727589000578 ) ) ;
#5048=CARTESIAN_POINT ( 'NONE',  ( -0.02483573736219273770, 30.00522634882376849, -2.170826557311644756 ) ) ;
#5052=CARTESIAN_POINT ( 'NONE',  ( -1.445575777915792948, 23.61402273486993053, -1.544386912436334747 ) ) ;
#5059=ORIENTED_EDGE ( 'NONE', *, *, #21937, .F. ) ;
#5060=AXIS2_PLACEMENT_3D ( 'NONE', #20775, #9512, #15304 ) ;
#5062=DIRECTION ( 'NONE',  ( 1.000000000000000000, 0.000000000000000000, 0.000000000000000000 ) ) ;
#5068=CARTESIAN_POINT ( 'NONE',  ( -1.670409819853669209, 24.49999999999984368, 3.654390594367815215 ) ) ;
#5070=CARTESIAN_POINT ( 'NONE',  ( -0.1402836262634008790, 27.99621943665322021, 2.168309435604789392 ) ) ;
#5077=CARTESIAN_POINT ( 'NONE',  ( 1.884954223019000175, 28.21869850838000104, -1.259486242684000112 ) ) ;
#5078=DIRECTION ( 'NONE',  ( 0.000000000000000000, 1.000000000000000000, 0.000000000000000000 ) ) ;
#5079=CARTESIAN_POINT ( 'NONE',  ( -0.3356153332444000159, 27.99687716036000396, 2.426425728984999974 ) ) ;
#5087=VERTEX_POINT ( 'NONE', #12295 ) ;
#5088=CARTESIAN_POINT ( 'NONE',  ( -2.184465970885610009, 24.06666666666666643, 1.259047450927307521 ) ) ;
#5093=CARTESIAN_POINT ( 'NONE',  ( 2.184465970885645092, 28.46666666666667922, -1.259047450927249123 ) ) ;
#5094=CARTESIAN_POINT ( 'NONE',  ( -2.686623376377999861, 29.68107362301000052, 0.4487213728548000158 ) ) ;
#5095=CARTESIAN_POINT ( 'NONE',  ( 0.9652172239566000345, 23.62045304942999735, 2.538761913251999847 ) ) ;
#5100=ADVANCED_FACE ( 'NONE', ( #19683 ), #23667, .T. ) ;
#5109=CARTESIAN_POINT ( 'NONE',  ( -4.000000000000000000, 26.47444252552741872, 0.7494995952805646455 ) ) ;
#5111=CARTESIAN_POINT ( 'NONE',  ( 1.651019514586000048, 24.46469563812999937, -1.937031240432999901 ) ) ;
#5118=ORIENTED_EDGE ( 'NONE', *, *, #11029, .F. ) ;
#5120=CARTESIAN_POINT ( 'NONE',  ( -1.740327722686464851, 26.21338436845917741, 1.205708594814126844 ) ) ;
#5121=CARTESIAN_POINT ( 'NONE',  ( 1.699999999999999956, 9.000014419210808470, 0.2828404724695334771 ) ) ;
#5126=DIRECTION ( 'NONE',  ( -0.5000000000000169864, 0.000000000000000000, 0.8660254037844288266 ) ) ;
#5128=EDGE_CURVE ( 'NONE', #20342, #14322, #3017, .T. ) ;
#5129=CARTESIAN_POINT ( 'NONE',  ( -1.143608723645000103, 30.12066899698000100, 2.065030851670000001 ) ) ;
#5133=ORIENTED_EDGE ( 'NONE', *, *, #18366, .F. ) ;
#5134=LINE ( 'NONE', #16484, #14493 ) ;
#5137=AXIS2_PLACEMENT_3D ( 'NONE', #3094, #17865, #1264 ) ;
#5138=CYLINDRICAL_SURFACE ( 'NONE', #18490, 3.000000000000000000 ) ;
#5140=CARTESIAN_POINT ( 'NONE',  ( -2.596700060712746172, 30.41537005277800887, 0.3120530614487230237 ) ) ;
#5141=CARTESIAN_POINT ( 'NONE',  ( 2.228577735068977717, 30.71132486706381926, -0.6003337536057592461 ) ) ;
#5146=ORIENTED_EDGE ( 'NONE', *, *, #3353, .F. ) ;
#5150=ORIENTED_EDGE ( 'NONE', *, *, #18394, .T. ) ;
#5157=CARTESIAN_POINT ( 'NONE',  ( -1.997236045835000251, 31.07209288612999742, 0.9729124824121000437 ) ) ;
#5159=CARTESIAN_POINT ( 'NONE',  ( 1.479086741115911874, 29.90763722216965448, -1.574257872583303408 ) ) ;
#5160=VERTEX_POINT ( 'NONE', #4262 ) ;
#5167=DIRECTION ( 'NONE',  ( 0.000000000000000000, 0.000000000000000000, -1.000000000000000000 ) ) ;
#5170=ORIENTED_EDGE ( 'NONE', *, *, #2920, .T. ) ;
#5172=ORIENTED_EDGE ( 'NONE', *, *, #14008, .T. ) ;
#5184=CARTESIAN_POINT ( 'NONE',  ( -1.090060885945051128, 26.86992048250327514, -1.916741099986829955 ) ) ;
#5190=CARTESIAN_POINT ( 'NONE',  ( -2.193530619437999984, 28.51119850838000147, -0.5724186824819998964 ) ) ;
#5191=CONICAL_SURFACE ( 'NONE', #18706, 2.249999941723000330, 0.7853981633972997312 ) ;
#5193=CARTESIAN_POINT ( 'NONE',  ( 0.4710401059126000378, 28.61614211382000050, 2.093446882794999908 ) ) ;
#5198=CARTESIAN_POINT ( 'NONE',  ( -1.733098085964022372, 30.74034480246814738, -1.478422619745301869 ) ) ;
#5199=VECTOR ( 'NONE', #22427, 1000.000000000000000 ) ;
#5200=ORIENTED_EDGE ( 'NONE', *, *, #11048, .F. ) ;
#5202=CARTESIAN_POINT ( 'NONE',  ( -1.999167105995410365, 24.08333333333333570, 1.536366799937339156 ) ) ;
#5210=AXIS2_PLACEMENT_3D ( 'NONE', #166, #12789, #21875 ) ;
#5215=DIRECTION ( 'NONE',  ( -1.000000000000000000, 0.000000000000000000, 0.000000000000000000 ) ) ;
#5217=FACE_OUTER_BOUND ( 'NONE', #14177, .T. ) ;
#5219=CARTESIAN_POINT ( 'NONE',  ( -3.316314694148182696, 24.62756664670257933, 2.704122461039521141 ) ) ;
#5220=CARTESIAN_POINT ( 'NONE',  ( 0.000000000000000000, 24.29999999999999716, 0.000000000000000000 ) ) ;
#5223=CARTESIAN_POINT ( 'NONE',  ( -2.500000000000000000, 18.50000000000000000, 0.000000000000000000 ) ) ;
#5224=CARTESIAN_POINT ( 'NONE',  ( 1.670409819843222898, 24.49999999999985079, -3.654390594373847723 ) ) ;
#5225=ORIENTED_EDGE ( 'NONE', *, *, #8833, .F. ) ;
#5226=CARTESIAN_POINT ( 'NONE',  ( 1.286819792229999981, 25.02205787433999973, 2.195916730907999881 ) ) ;
#5227=CARTESIAN_POINT ( 'NONE',  ( 2.504532394112000003E-14, 28.43419673618999965, 2.500000000000000000 ) ) ;
#5230=CARTESIAN_POINT ( 'NONE',  ( -1.259047450927251566, 27.86666666666666714, -2.184465970885643316 ) ) ;
#5231=EDGE_CURVE ( 'NONE', #367, #5021, #17730, .T. ) ;
#5232=EDGE_LOOP ( 'NONE', ( #15308, #1682, #11181 ) ) ;
#5233=DIRECTION ( 'NONE',  ( 0.000000000000000000, 0.000000000000000000, -1.000000000000000000 ) ) ;
#5235=CARTESIAN_POINT ( 'NONE',  ( -1.972625189811084478, 26.24262259178813395, 0.8364124223001996317 ) ) ;
#5239=CARTESIAN_POINT ( 'NONE',  ( 0.7782965750743000566, 25.53778480117000171, 1.998394996811000190 ) ) ;
#5243=CARTESIAN_POINT ( 'NONE',  ( -0.6418273050434999405, 30.72876582673999835, -2.070799230921999801 ) ) ;
#5244=EDGE_CURVE ( 'NONE', #5087, #11168, #11673, .T. ) ;
#5247=CARTESIAN_POINT ( 'NONE',  ( -1.704938782513197637, 26.34374313124272504, 1.466284411147575462 ) ) ;
#5248=ORIENTED_EDGE ( 'NONE', *, *, #7422, .F. ) ;
#5249=CARTESIAN_POINT ( 'NONE',  ( 0.6634078306992999829, 24.00000000000000000, -2.410371351092000403 ) ) ;
#5251=FACE_OUTER_BOUND ( 'NONE', #19995, .T. ) ;
#5253=ORIENTED_EDGE ( 'NONE', *, *, #22531, .T. ) ;
#5258=ADVANCED_FACE ( 'NONE', ( #10559 ), #3055, .T. ) ;
#5268=CARTESIAN_POINT ( 'NONE',  ( 0.5475340434131998890, 30.78434480342999890, -2.278098825807999717 ) ) ;
#5271=CARTESIAN_POINT ( 'NONE',  ( 1.905473965356794031, 29.86637024958199760, -1.018015044609141162 ) ) ;
#5278=CYLINDRICAL_SURFACE ( 'NONE', #13885, 2.000000000000000000 ) ;
#5282=EDGE_CURVE ( 'NONE', #19347, #10715, #6210, .T. ) ;
#5284=ORIENTED_EDGE ( 'NONE', *, *, #14256, .T. ) ;
#5285=CARTESIAN_POINT ( 'NONE',  ( 4.625000000000000000, 13.00000000000000000, 0.000000000000000000 ) ) ;
#5286=CARTESIAN_POINT ( 'NONE',  ( -1.259047450927242462, 29.73333333333333783, 2.184465970885648201 ) ) ;
#5292=EDGE_CURVE ( 'NONE', #2748, #8374, #2753, .T. ) ;
#5295=CARTESIAN_POINT ( 'NONE',  ( -0.6568252240428453792, 26.36639859639442562, 2.105786140651809468 ) ) ;
#5296=AXIS2_PLACEMENT_3D ( 'NONE', #21670, #4838, #23224 ) ;
#5297=CARTESIAN_POINT ( 'NONE',  ( 0.000000000000000000, 22.19999999999999574, 0.000000000000000000 ) ) ;
#5304=CARTESIAN_POINT ( 'NONE',  ( -0.5776703561810999643, 26.06521896306000130, -2.213655236985999863 ) ) ;
#5314=CARTESIAN_POINT ( 'NONE',  ( 0.000000000000000000, -1.550000000000000044, 0.000000000000000000 ) ) ;
#5320=CARTESIAN_POINT ( 'NONE',  ( 0.8151085262080000060, 29.89420749509000075, -1.990313132251999795 ) ) ;
#5323=AXIS2_PLACEMENT_3D ( 'NONE', #6555, #23374, #6669 ) ;
#5324=ORIENTED_EDGE ( 'NONE', *, *, #13348, .T. ) ;
#5328=CARTESIAN_POINT ( 'NONE',  ( 2.000000000000000000, 23.50000000000000000, 0.000000000000000000 ) ) ;
#5334=DIRECTION ( 'NONE',  ( 0.7071067811823850136, -0.7071067811898851252, 1.080116765722976056E-06 ) ) ;
#5335=EDGE_LOOP ( 'NONE', ( #14982, #22305, #23844, #22797 ) ) ;
#5337=ORIENTED_EDGE ( 'NONE', *, *, #2920, .F. ) ;
#5338=CARTESIAN_POINT ( 'NONE',  ( 2.104624887614000350, 24.11448581793999679, 0.4915318859118999462 ) ) ;
#5346=CARTESIAN_POINT ( 'NONE',  ( -1.922299668730066635, 26.22581021936841594, 0.9082030837895462838 ) ) ;
#5348=VERTEX_POINT ( 'NONE', #12839 ) ;
#5350=CARTESIAN_POINT ( 'NONE',  ( 1.791338785401000111, 25.49639128499999785, 1.497938606261000061 ) ) ;
#5359=ADVANCED_FACE ( 'NONE', ( #13068 ), #1601, .T. ) ;
#5365=AXIS2_PLACEMENT_3D ( 'NONE', #16481, #12856, #18211 ) ;
#5367=CARTESIAN_POINT ( 'NONE',  ( 2.309807618587000011, 30.69019238141000017, -7.292675330123999428E-08 ) ) ;
#5370=CONICAL_SURFACE ( 'NONE', #13083, 2.154903751016000069, 0.7853981633972997312 ) ;
#5373=EDGE_CURVE ( 'NONE', #13184, #13716, #20890, .T. ) ;
#5374=EDGE_LOOP ( 'NONE', ( #1008, #10067, #4041, #13334, #22335, #15780 ) ) ;
#5384=DIRECTION ( 'NONE',  ( -6.465317295295811501E-08, 0.9999999999999703570, -2.351119575178930673E-07 ) ) ;
#5386=CARTESIAN_POINT ( 'NONE',  ( 2.192736427680999967, 30.56853374141000046, 0.8254858857236999636 ) ) ;
#5390=CARTESIAN_POINT ( 'NONE',  ( 1.543414968236286988, 29.90237403121793491, -1.511123829192336343 ) ) ;
#5391=VERTEX_POINT ( 'NONE', #20820 ) ;
#5392=CARTESIAN_POINT ( 'NONE',  ( 0.9136931036111000104, 25.17769377914000017, -1.980922918787000109 ) ) ;
#5394=CARTESIAN_POINT ( 'NONE',  ( -1.959792349063410599, 26.25942009138634603, 0.9068320924654740267 ) ) ;
#5397=DIRECTION ( 'NONE',  ( 0.000000000000000000, -0.7071067811866525998, -0.7071067811864425456 ) ) ;
#5403=DIRECTION ( 'NONE',  ( 0.000000000000000000, 0.7071230553199298052, -0.7070905066786058457 ) ) ;
#5405=VECTOR ( 'NONE', #18721, 1000.000000000000114 ) ;
#5407=AXIS2_PLACEMENT_3D ( 'NONE', #1805, #209, #7132 ) ;
#5415=CARTESIAN_POINT ( 'NONE',  ( 0.5334682286136585017, 28.03597116440634807, 2.139201694519461849 ) ) ;
#5416=LINE ( 'NONE', #11101, #1537 ) ;
#5417=EDGE_CURVE ( 'NONE', #7680, #1412, #16548, .T. ) ;
#5418=CARTESIAN_POINT ( 'NONE',  ( 0.6642235200064005030, 30.76429554769410402, -2.063723317057710727 ) ) ;
#5425=CARTESIAN_POINT ( 'NONE',  ( 1.344743706340999934, 28.11271896306000073, 1.850881008969999852 ) ) ;
#5428=ORIENTED_EDGE ( 'NONE', *, *, #16011, .F. ) ;
#5431=DIRECTION ( 'NONE',  ( 0.000000000000000000, 1.000000000000000000, 0.000000000000000000 ) ) ;
#5432=EDGE_CURVE ( 'NONE', #13113, #12315, #12427, .T. ) ;
#5435=CARTESIAN_POINT ( 'NONE',  ( 0.1526552725783049125, 24.50000000000000000, 2.395140156181688074 ) ) ;
#5439=CARTESIAN_POINT ( 'NONE',  ( 0.000000000000000000, 24.39999999221199900, -2.849999992212000066 ) ) ;
#5440=CARTESIAN_POINT ( 'NONE',  ( 2.177130415331999913, 29.80110296423999827, 0.8625838095880999923 ) ) ;
#5443=ORIENTED_EDGE ( 'NONE', *, *, #3558, .T. ) ;
#5448=DIRECTION ( 'NONE',  ( 0.000000000000000000, 0.000000000000000000, -1.000000000000000000 ) ) ;
#5449=DIRECTION ( 'NONE',  ( -1.000000000000000000, 0.000000000000000000, 0.000000000000000000 ) ) ;
#5450=CARTESIAN_POINT ( 'NONE',  ( -0.7774759188957669487, 29.25062229162126570, -2.015113548211680872 ) ) ;
#5453=CARTESIAN_POINT ( 'NONE',  ( 2.385098070162194883, 23.88509807016325226, 0.2903665702034990415 ) ) ;
#5455=CARTESIAN_POINT ( 'NONE',  ( -1.312395939795999888, 23.62679386126000125, -1.717109324558000027 ) ) ;
#5464=CARTESIAN_POINT ( 'NONE',  ( -2.750000000000000000, 22.19999999999999574, 0.000000000000000000 ) ) ;
#5466=VERTEX_POINT ( 'NONE', #22861 ) ;
#5468=CARTESIAN_POINT ( 'NONE',  ( -2.110827410376000302, 24.51312697075000102, 0.3791487629745999843 ) ) ;
#5470=CARTESIAN_POINT ( 'NONE',  ( 2.500000000000000000, 27.59999999999999787, 0.000000000000000000 ) ) ;
#5472=FACE_OUTER_BOUND ( 'NONE', #4055, .T. ) ;
#5481=CARTESIAN_POINT ( 'NONE',  ( 1.373052545766183741, 30.76415608119967615, -1.788908248115641531 ) ) ;
#5486=CARTESIAN_POINT ( 'NONE',  ( -1.500144717171000064, 28.04419433609999857, -2.447990496630999768 ) ) ;
#5494=CARTESIAN_POINT ( 'NONE',  ( 0.000000000000000000, 22.19999999999999574, 0.000000000000000000 ) ) ;
#5497=CIRCLE ( 'NONE', #2002, 2.899999999999999911 ) ;
#5498=CARTESIAN_POINT ( 'NONE',  ( 1.651614159710000029, 28.91398226591000054, 1.661872489819000043 ) ) ;
#5500=EDGE_CURVE ( 'NONE', #5602, #23303, #2776, .T. ) ;
#5501=CARTESIAN_POINT ( 'NONE',  ( 2.155981317445319512, 29.81398103993711857, -0.1719232382127588998 ) ) ;
#5503=CARTESIAN_POINT ( 'NONE',  ( -2.310215611903000177, 23.83319443196000265, 0.3439361960344000102 ) ) ;
#5506=B_SPLINE_CURVE_WITH_KNOTS ( 'NONE', 3,
 ( #6006, #4566, #19210, #13881, #18853, #6369, #9886, #15203, #6248, #15682, #11477, #11597, #18969, #13631, #17275, #8082, #4083, #2259, #15449, #8198, #22600, #9652, #21027, #4440, #13393, #11830, #9767, #17153, #7954, #15324, #6127, #10016, #17405, #15566, #13752, #21152, #11957, #22716, #2752, #19344, #10133, #17522, #916, #8316, #15810, #12556, #1174, #3240, #23319, #23203, #18132, #14003, #10381, #6734, #17772, #4934, #8807, #16048, #2871, #16169, #15926, #4811, #8926, #1413, #6617, #8443, #3124, #8566, #23686, #23440, #7093, #23572, #21284, #12080, #19942, #3362, #14126, #10255, #21397, #12198, #10741, #14368, #16292, #8682, #19587 ),
 .UNSPECIFIED., .F., .F.,
 ( 4, 2, 2, 2, 2, 2, 2, 2, 2, 2, 2, 2, 2, 2, 2, 2, 2, 1, 2, 2, 2, 2, 2, 1, 2, 2, 2, 2, 2, 1, 2, 2, 2, 2, 2, 2, 2, 2, 2, 2, 2, 2, 2, 4 ),
 ( 0.000000000000000000, 0.01232754932072391285, 0.02465509864144782570, 0.04931019728289567222, 0.07396529592434351874, 0.09862039456579137220, 0.1109479438865152712, 0.1232754932072391979, 0.1479305918486870375, 0.1725856904901348909, 0.1972407891315827444, 0.2095683384523066572, 0.2218958877730305423, 0.2465509864144784513, 0.2712060850559263048, 0.2958611836973741305, 0.3081887330180980711, 0.3205162823388220117, 0.3328438316595459523, 0.3451713809802698374, 0.3698264796217177186, 0.3944815782631655443, 0.4068091275838894849, 0.4191366769046134255, 0.4314642262253373661, 0.4437917755460611957, 0.4684468741875091324, 0.4931019728289570692, 0.5054295221496809543, 0.5177570714704048394, 0.5300846207911287244, 0.5424121701118527206, 0.5670672687533004908, 0.5917223673947482609, 0.6163774660361961422, 0.6287050153569201383, 0.6410325646776440234, 0.6656876633190919046, 0.6903427619605397858, 0.7149978606019877780, 0.7273254099227116631, 0.7396529592434355482, 0.7643080578848834294, 0.7889631565263313107 ),
 .UNSPECIFIED. ) ;
#5507=ORIENTED_EDGE ( 'NONE', *, *, #1371, .F. ) ;
#5509=CARTESIAN_POINT ( 'NONE',  ( 0.000000000000000000, -1.550000000000000044, 0.000000000000000000 ) ) ;
#5511=EDGE_LOOP ( 'NONE', ( #19915, #3439, #877, #4892 ) ) ;
#5516=CARTESIAN_POINT ( 'NONE',  ( 2.000000000000000000, 18.89999999999999858, 5.041407240605999832E-11 ) ) ;
#5517=EDGE_CURVE ( 'NONE', #21669, #11307, #15488, .T. ) ;
#5518=VERTEX_POINT ( 'NONE', #8224 ) ;
#5524=CARTESIAN_POINT ( 'NONE',  ( 0.6162257440955131171, 27.24093660882355650, 2.118443747156355084 ) ) ;
#5528=CARTESIAN_POINT ( 'NONE',  ( 2.137480853478654019, 30.62211454086312656, -0.3111734527053177657 ) ) ;
#5530=DIRECTION ( 'NONE',  ( 0.000000000000000000, -1.000000000000000000, 0.000000000000000000 ) ) ;
#5534=CARTESIAN_POINT ( 'NONE',  ( 2.236906829057999868, 25.78687716036000310, 0.5033195914047999819 ) ) ;
#5537=ADVANCED_FACE ( 'NONE', ( #2401 ), #9709, .T. ) ;
#5543=EDGE_CURVE ( 'NONE', #13895, #23303, #8161, .T. ) ;
#5545=CARTESIAN_POINT ( 'NONE',  ( -0.6543697108981931798, 28.16666666666667140, 2.434931691670791043 ) ) ;
#5549=CARTESIAN_POINT ( 'NONE',  ( -1.502772323173000135, 29.33784492091999851, -1.796001945673999955 ) ) ;
#5553=AXIS2_PLACEMENT_3D ( 'NONE', #9012, #22193, #11186 ) ;
#5559=ADVANCED_FACE ( 'NONE', ( #18850 ), #16276, .T. ) ;
#5561=CARTESIAN_POINT ( 'NONE',  ( 0.000000000000000000, 24.65000000674550051, 0.000000000000000000 ) ) ;
#5563=CARTESIAN_POINT ( 'NONE',  ( -0.7577245197952828804, 29.24939092660360629, -2.022592451772749378 ) ) ;
#5565=ORIENTED_EDGE ( 'NONE', *, *, #5244, .T. ) ;
#5566=CARTESIAN_POINT ( 'NONE',  ( 0.000000000000000000, 18.10000000000000142, 0.000000000000000000 ) ) ;
#5569=CARTESIAN_POINT ( 'NONE',  ( 2.113544220839000065, 25.71690224701999838, 0.4514181673775000125 ) ) ;
#5572=CARTESIAN_POINT ( 'NONE',  ( 0.000000000000000000, 20.00000000000000000, 0.000000000000000000 ) ) ;
#5575=CONICAL_SURFACE ( 'NONE', #12915, 3.049999825846000157, 0.7853981633972997312 ) ;
#5578=DIRECTION ( 'NONE',  ( 0.000000000000000000, 1.000000000000000000, 0.000000000000000000 ) ) ;
#5581=CARTESIAN_POINT ( 'NONE',  ( 2.063368671964000090, 25.70856110624000124, -0.2979541432074999663 ) ) ;
#5585=CARTESIAN_POINT ( 'NONE',  ( 0.5079312758524999749, 28.61268239940000058, 2.305192271312999974 ) ) ;
#5586=ADVANCED_FACE ( 'NONE', ( #5888 ), #13965, .T. ) ;
#5591=ORIENTED_EDGE ( 'NONE', *, *, #4369, .F. ) ;
#5594=ORIENTED_EDGE ( 'NONE', *, *, #23599, .T. ) ;
#5595=CARTESIAN_POINT ( 'NONE',  ( -2.121106334292000017, 30.87889366360999688, 6.284935476095000148E-07 ) ) ;
#5601=CARTESIAN_POINT ( 'NONE',  ( 1.099251314038999894, 28.53962896666999782, 2.157402177123000087 ) ) ;
#5602=VERTEX_POINT ( 'NONE', #6004 ) ;
#5603=AXIS2_PLACEMENT_3D ( 'NONE', #13440, #17199, #7998 ) ;
#5607=ORIENTED_EDGE ( 'NONE', *, *, #23001, .T. ) ;
#5613=CARTESIAN_POINT ( 'NONE',  ( -1.901161826014999834, 30.05505061217000318, 1.092502442907999916 ) ) ;
#5616=CARTESIAN_POINT ( 'NONE',  ( 1.797367992752552990, 29.72859529399798006, 1.204889009139612055 ) ) ;
#5618=CARTESIAN_POINT ( 'NONE',  ( 2.133148737088000235, 25.80587366863000298, 0.4564637253469999711 ) ) ;
#5623=CARTESIAN_POINT ( 'NONE',  ( 2.500000000000000444, 30.25634700817417766, -0.4349195733711135325 ) ) ;
#5636=FACE_OUTER_BOUND ( 'NONE', #6420, .T. ) ;
#5639=CARTESIAN_POINT ( 'NONE',  ( 1.399078845269212223, 30.71403437281561111, -1.645507438231223363 ) ) ;
#5642=CARTESIAN_POINT ( 'NONE',  ( 0.000000000000000000, 22.00000000000000000, 0.000000000000000000 ) ) ;
#5643=LINE ( 'NONE', #22350, #5405 ) ;
#5647=CARTESIAN_POINT ( 'NONE',  ( -1.950678319476999878, 26.16271896306000144, -1.195388535980999922 ) ) ;
#5650=VERTEX_POINT ( 'NONE', #15807 ) ;
#5653=CARTESIAN_POINT ( 'NONE',  ( -1.844810972989856968, 29.95044706087815456, -1.336380754565594797 ) ) ;
#5657=CIRCLE ( 'NONE', #4511, 4.625000000000000000 ) ;
#5662=CARTESIAN_POINT ( 'NONE',  ( -1.725915770149999862, 30.22510609745999943, 1.283340576838000180 ) ) ;
#5665=ORIENTED_EDGE ( 'NONE', *, *, #5500, .T. ) ;
#5667=CARTESIAN_POINT ( 'NONE',  ( -2.499999999999999556, 28.81666666666666643, 0.3272492347489436848 ) ) ;
#5675=CARTESIAN_POINT ( 'NONE',  ( -0.7657973753844729004, 29.24989338039968700, -2.019557259306400177 ) ) ;
#5681=CARTESIAN_POINT ( 'NONE',  ( -0.5998269938833999948, 25.50789140844999991, 2.076358161442000139 ) ) ;
#5687=DIRECTION ( 'NONE',  ( 0.000000000000000000, -1.000000000000000000, 0.000000000000000000 ) ) ;
#5696=CARTESIAN_POINT ( 'NONE',  ( 0.6079502603517000781, 24.15152788257999816, -2.254560651513999758 ) ) ;
#5701=CARTESIAN_POINT ( 'NONE',  ( -0.3657044282044999428, 28.56480980899999977, 2.248360111627000002 ) ) ;
#5707=ORIENTED_EDGE ( 'NONE', *, *, #18366, .T. ) ;
#5708=EDGE_CURVE ( 'NONE', #6198, #6330, #11258, .T. ) ;
#5709=CARTESIAN_POINT ( 'NONE',  ( 2.403644530880252539, 23.90364453088029961, -0.2598880820672725966 ) ) ;
#5712=ORIENTED_EDGE ( 'NONE', *, *, #7026, .T. ) ;
#5713=B_SPLINE_SURFACE_WITH_KNOTS ( 'NONE', 3, 3, ( 
 ( #20468, #7618, #11269, #6031, #22505, #2052, #22392, #14880, #5915, #6158, #17059, #16816, #3876, #13543, #14994, #15110, #11385, #22267, #13187, #7859, #5805, #13299, #3990, #9679, #18756, #2166, #9559, #18879, #13420, #341, #20698, #4231, #7743, #2287, #4106 ),
 ( #11505, #457, #22623, #11624, #18993, #2402, #9793, #18101, #20151, #3559, #23286, #14091, #14218, #1259, #8647, #3208, #10592, #17978, #1380, #8772, #14685, #9241, #14909, #14792, #5718, #1851, #18443, #18677, #5945, #20731, #22188, #16727, #1736, #20503, #9353 ),
 ( #5601, #1970, #11180, #4137, #7411, #20612, #137, #13332, #2083, #11535, #23887, #16618, #7776, #12982, #9123, #16496, #18566, #22428, #9473, #12866, #22078, #16976, #11057, #27, #2199, #3909, #20382, #15143, #3790, #22540, #7528, #22303, #13105, #11300, #16850 ),
 ( #253, #7293, #7658, #11417, #15030, #5486, #20266, #18789, #3669, #5835, #13219, #4021, #9591, #377, #21337, #17333, #10195, #13695, #979, #9711, #13454, #22895, #17462, #23135, #737, #10076, #609, #4753, #18914, #17094, #856, #6310, #4631, #20857, #17212 ) ),
 .UNSPECIFIED., .F., .F., .F.,
 ( 4, 4 ),
 ( 4, 1, 1, 1, 1, 1, 1, 1, 1, 1, 1, 1, 1, 1, 1, 1, 1, 1, 1, 1, 1, 1, 1, 1, 1, 1, 1, 1, 1, 1, 1, 1, 4 ),
 ( -0.3056682515952000023, 1.305668251594999996 ),
 ( -0.02000000000000000042, 0.01250000000000000069, 0.04499999999999999833, 0.07749999999999999944, 0.1100000000000000006, 0.1424999999999999878, 0.1749999999999999889, 0.2074999999999999900, 0.2399999999999999911, 0.2725000000000000200, 0.3049999999999999933, 0.3375000000000000222, 0.3699999999999999956, 0.4025000000000000244, 0.4349999999999999978, 0.4675000000000000266, 0.5000000000000000000, 0.5324999999999999734, 0.5649999999999999467, 0.5975000000000000311, 0.6300000000000000044, 0.6624999999999999778, 0.6949999999999999512, 0.7275000000000000355, 0.7600000000000000089, 0.7924999999999999822, 0.8249999999999999556, 0.8575000000000000400, 0.8900000000000000133, 0.9224999999999999867, 0.9549999999999999600, 0.9875000000000000444, 1.020000000000000018 ),
 .UNSPECIFIED. ) ;
#5718=CARTESIAN_POINT ( 'NONE',  ( 2.445091418594000032, 26.40256359724000035, -0.3381971108622000011 ) ) ;
#5720=ORIENTED_EDGE ( 'NONE', *, *, #14420, .T. ) ;
#5722=EDGE_CURVE ( 'NONE', #15990, #23046, #23831, .T. ) ;
#5726=ORIENTED_EDGE ( 'NONE', *, *, #6268, .T. ) ;
#5729=LINE ( 'NONE', #10950, #19579 ) ;
#5731=CIRCLE ( 'NONE', #6116, 0.1000000000000003525 ) ;
#5733=CARTESIAN_POINT ( 'NONE',  ( 1.542578681836999976, 28.93232406860999717, 1.552159782388999876 ) ) ;
#5735=STYLED_ITEM ( 'NONE', ( #16892 ), #8659 ) ;
#5736=CARTESIAN_POINT ( 'NONE',  ( 0.2039437053001954547, 29.61575808220096206, 2.150321007061429146 ) ) ;
#5737=EDGE_LOOP ( 'NONE', ( #10070, #11047, #20859, #21558 ) ) ;
#5738=CARTESIAN_POINT ( 'NONE',  ( -0.2525366025761000000, 25.24749154463999901, -2.166821629601999977 ) ) ;
#5744=DIRECTION ( 'NONE',  ( 0.000000000000000000, 1.000000000000000000, 0.000000000000000000 ) ) ;
#5750=ORIENTED_EDGE ( 'NONE', *, *, #13248, .F. ) ;
#5755=B_SPLINE_CURVE_WITH_KNOTS ( 'NONE', 3,
 ( #11098, #13262, #20653, #18482, #1895, #4064, #11458, #16659, #18833, #2239, #63, #6480, #4547, #10116 ),
 .UNSPECIFIED., .F., .F.,
 ( 4, 2, 2, 2, 2, 2, 4 ),
 ( 0.0001520356277385664402, 0.001067258118390845053, 0.001982480609043124099, 0.002440091854369263839, 0.002897703099695404013, 0.003355314345021543319, 0.003812925590347683059 ),
 .UNSPECIFIED. ) ;
#5759=CLOSED_SHELL ( 'NONE', ( #23018, #16518, #20058, #1427, #7554, #9242, #8346 ) ) ;
#5761=CARTESIAN_POINT ( 'NONE',  ( 2.500000000000000000, 26.80000000000000071, 0.000000000000000000 ) ) ;
#5762=AXIS2_PLACEMENT_3D ( 'NONE', #3746, #102, #7487 ) ;
#5764=CARTESIAN_POINT ( 'NONE',  ( 1.999167105995449445, 27.91753006952333749, -1.536366799937288530 ) ) ;
#5765=CARTESIAN_POINT ( 'NONE',  ( 1.380771013157804372, 30.49197061622366078, 1.664552687405546960 ) ) ;
#5770=AXIS2_PLACEMENT_3D ( 'NONE', #6708, #21371, #4788 ) ;
#5772=CARTESIAN_POINT ( 'NONE',  ( -0.2246974795679000103, 26.60114211381999993, -2.281391790424999844 ) ) ;
#5773=CARTESIAN_POINT ( 'NONE',  ( -2.121106334292000017, 30.87889366360999688, 6.284935476095000148E-07 ) ) ;
#5778=VECTOR ( 'NONE', #15171, 1000.000000000000000 ) ;
#5780=ORIENTED_EDGE ( 'NONE', *, *, #514, .T. ) ;
#5781=DIRECTION ( 'NONE',  ( 1.000000000000000000, 0.000000000000000000, 0.000000000000000000 ) ) ;
#5783=EDGE_CURVE ( 'NONE', #16380, #20998, #15100, .T. ) ;
#5785=FACE_OUTER_BOUND ( 'NONE', #22347, .T. ) ;
#5787=CARTESIAN_POINT ( 'NONE',  ( 0.1526552725783049125, 24.50000000000000000, 2.395140156181688074 ) ) ;
#5789=FACE_OUTER_BOUND ( 'NONE', #8706, .T. ) ;
#5792=ORIENTED_EDGE ( 'NONE', *, *, #21364, .F. ) ;
#5794=DIRECTION ( 'NONE',  ( 0.000000000000000000, 1.000000000000000000, 0.000000000000000000 ) ) ;
#5795=AXIS2_PLACEMENT_3D ( 'NONE', #23832, #23956, #16215 ) ;
#5797=CARTESIAN_POINT ( 'NONE',  ( -0.9120910450028335559, 29.25920337588331321, -1.958506303686876393 ) ) ;
#5803=CARTESIAN_POINT ( 'NONE',  ( 0.5680559541153000769, 25.57756168797000029, 2.085265971965999832 ) ) ;
#5804=CARTESIAN_POINT ( 'NONE',  ( -2.434931691670787934, 28.03333333333334210, 0.6543697108982051702 ) ) ;
#5805=CARTESIAN_POINT ( 'NONE',  ( -2.263084017374999757, 26.89799822780999961, 0.1334610483750000021 ) ) ;
#5811=CARTESIAN_POINT ( 'NONE',  ( -2.500000000000000000, 28.80000000000000071, 0.000000000000000000 ) ) ;
#5816=CARTESIAN_POINT ( 'NONE',  ( 2.305541151813000234, 24.64511087984000071, -1.435767851291000152 ) ) ;
#5820=CARTESIAN_POINT ( 'NONE',  ( 2.435082195634000080, 29.44076328160999978, 0.7672906025640999772 ) ) ;
#5823=DIRECTION ( 'NONE',  ( 0.000000000000000000, 0.000000000000000000, -1.000000000000000000 ) ) ;
#5828=CARTESIAN_POINT ( 'NONE',  ( 1.792728101376139804, 23.95620205949097326, -1.699880397723725789 ) ) ;
#5829=ORIENTED_EDGE ( 'NONE', *, *, #6087, .T. ) ;
#5833=AXIS2_PLACEMENT_3D ( 'NONE', #2494, #2255, #9764 ) ;
#5835=CARTESIAN_POINT ( 'NONE',  ( 1.687576972922000040, 27.65419433610000155, 2.322750540216000026 ) ) ;
#5836=ORIENTED_EDGE ( 'NONE', *, *, #10757, .F. ) ;
#5840=DIRECTION ( 'NONE',  ( 0.000000000000000000, -1.000000000000000000, 0.000000000000000000 ) ) ;
#5850=CARTESIAN_POINT ( 'NONE',  ( 2.111381028812000515, 29.62342848812999918, -0.5916485676189999765 ) ) ;
#5852=CARTESIAN_POINT ( 'NONE',  ( 1.089341972983306261, 29.67115983959759618, 1.865512284885492145 ) ) ;
#5855=CARTESIAN_POINT ( 'NONE',  ( 1.153787575258000020, 24.88016091445000200, 2.030811482765999987 ) ) ;
#5877=CARTESIAN_POINT ( 'NONE',  ( 0.1784790855350541494, 26.24995697614779644, -4.515757205439222766 ) ) ;
#5879=CARTESIAN_POINT ( 'NONE',  ( -1.015987791502897419, 30.34136096126319515, 1.906676889270033426 ) ) ;
#5880=ORIENTED_EDGE ( 'NONE', *, *, #11499, .F. ) ;
#5885=CARTESIAN_POINT ( 'NONE',  ( 2.093446882794999908, 25.56114211382000079, 0.4710401059125000067 ) ) ;
#5888=FACE_OUTER_BOUND ( 'NONE', #10189, .T. ) ;
#5890=CARTESIAN_POINT ( 'NONE',  ( -4.000000000000000000, 26.20000000000000284, -2.309401076759000304 ) ) ;
#5897=CARTESIAN_POINT ( 'NONE',  ( -2.121106334292000017, 30.87889366360999688, 6.284935476095000148E-07 ) ) ;
#5901=CARTESIAN_POINT ( 'NONE',  ( 0.000000000000000000, 22.00000000000000000, 0.000000000000000000 ) ) ;
#5902=ORIENTED_EDGE ( 'NONE', *, *, #6904, .F. ) ;
#5906=CARTESIAN_POINT ( 'NONE',  ( 2.154709788952736460, 28.99504473153596251, 0.1496538372950146079 ) ) ;
#5914=CARTESIAN_POINT ( 'NONE',  ( 0.6543697108982093891, 28.23333333333333428, 2.434931691670787046 ) ) ;
#5915=CARTESIAN_POINT ( 'NONE',  ( 2.231710853292999897, 28.06799822781000131, 0.3985328791175999918 ) ) ;
#5916=DIRECTION ( 'NONE',  ( 1.000000000000000000, 0.000000000000000000, 0.000000000000000000 ) ) ;
#5917=CYLINDRICAL_SURFACE ( 'NONE', #21154, 4.724999999999999645 ) ;
#5922=AXIS2_PLACEMENT_3D ( 'NONE', #19405, #6800, #4757 ) ;
#5924=ORIENTED_EDGE ( 'NONE', *, *, #9875, .T. ) ;
#5926=CARTESIAN_POINT ( 'NONE',  ( -2.127181242815999962, 23.63919896736999604, 0.9631217529048999859 ) ) ;
#5930=CARTESIAN_POINT ( 'NONE',  ( -1.236897034087000025, 30.01523436640999876, 2.233482906277000080 ) ) ;
#5934=CARTESIAN_POINT ( 'NONE',  ( -1.536366799937290084, 29.71753006952332399, -1.999167105995447669 ) ) ;
#5936=CARTESIAN_POINT ( 'NONE',  ( 1.600000000000000089, 8.900000000000000355, -1.856657105836000120E-09 ) ) ;
#5938=EDGE_CURVE ( 'NONE', #4848, #22927, #11669, .T. ) ;
#5939=CARTESIAN_POINT ( 'NONE',  ( 1.123018145447999938, 25.40617362301000171, -2.496154155557999577 ) ) ;
#5945=CARTESIAN_POINT ( 'NONE',  ( -2.411020654974999733, 26.01256359723999978, 0.5289967318968999965 ) ) ;
#5946=ORIENTED_EDGE ( 'NONE', *, *, #16379, .T. ) ;
#5949=CARTESIAN_POINT ( 'NONE',  ( -2.500000000000000888, 27.41753006952333749, -0.3272492347489316944 ) ) ;
#5950=CARTESIAN_POINT ( 'NONE',  ( 4.649999849441000421, 19.99999984944626874, -6.648422669304000250E-08 ) ) ;
#5951=CONICAL_SURFACE ( 'NONE', #9440, 4.699999872533999756, 0.7853981633972997312 ) ;
#5960=CARTESIAN_POINT ( 'NONE',  ( -1.799241820176000095, 29.91117657083000125, -1.253278400384999935 ) ) ;
#5961=VECTOR ( 'NONE', #6528, 1000.000000000000000 ) ;
#5964=CARTESIAN_POINT ( 'NONE',  ( -0.06398334756564613701, 29.60010643587459711, 2.158911828703185432 ) ) ;
#5965=ORIENTED_EDGE ( 'NONE', *, *, #5292, .T. ) ;
#5966=CARTESIAN_POINT ( 'NONE',  ( -2.335877486882000031, 24.40855709534999818, -0.2468828260556999998 ) ) ;
#5973=AXIS2_PLACEMENT_3D ( 'NONE', #998, #23031, #6689 ) ;
#5987=DIRECTION ( 'NONE',  ( 1.000000000000000000, 0.000000000000000000, 0.000000000000000000 ) ) ;
#5992=CARTESIAN_POINT ( 'NONE',  ( 0.5486518589655812184, 30.43653985558582420, 2.089137083840504783 ) ) ;
#5993=ORIENTED_EDGE ( 'NONE', *, *, #22539, .F. ) ;
#5996=DIRECTION ( 'NONE',  ( 0.000000000000000000, 1.000000000000000000, 0.000000000000000000 ) ) ;
#5999=FACE_OUTER_BOUND ( 'NONE', #19790, .T. ) ;
#6001=AXIS2_PLACEMENT_3D ( 'NONE', #1923, #12713, #7245 ) ;
#6004=CARTESIAN_POINT ( 'NONE',  ( 2.750000000000000000, 22.19999999999999574, 0.000000000000000000 ) ) ;
#6006=CARTESIAN_POINT ( 'NONE',  ( 2.053005267516999902E-14, 28.63049582772000079, 2.160000000000000142 ) ) ;
#6008=VERTEX_POINT ( 'NONE', #17963 ) ;
#6009=ORIENTED_EDGE ( 'NONE', *, *, #6285, .T. ) ;
#6011=DIRECTION ( 'NONE',  ( 0.000000000000000000, 0.000000000000000000, -1.000000000000000000 ) ) ;
#6013=CIRCLE ( 'NONE', #15288, 0.5500000000000001554 ) ;
#6018=DIRECTION ( 'NONE',  ( 0.000000000000000000, 0.000000000000000000, -1.000000000000000000 ) ) ;
#6023=CARTESIAN_POINT ( 'NONE',  ( 2.159851832628000068, 26.67456776951999942, 1.569224139466999901 ) ) ;
#6028=DIRECTION ( 'NONE',  ( 0.000000000000000000, 1.000000000000000000, 0.000000000000000000 ) ) ;
#6029=ORIENTED_EDGE ( 'NONE', *, *, #6558, .T. ) ;
#6031=CARTESIAN_POINT ( 'NONE',  ( -1.978081431919000099, 28.55549822781000202, 1.107772814030999919 ) ) ;
#6033=AXIS2_PLACEMENT_3D ( 'NONE', #8136, #13572, #22768 ) ;
#6035=CARTESIAN_POINT ( 'NONE',  ( 0.000000000000000000, 13.04999996922999905, -4.674999969225999585 ) ) ;
#6041=AXIS2_PLACEMENT_3D ( 'NONE', #17386, #9997, #2362 ) ;
#6042=CARTESIAN_POINT ( 'NONE',  ( -1.836544194422999876, 24.06874085023000021, -2.001013430241999735 ) ) ;
#6047=CARTESIAN_POINT ( 'NONE',  ( -0.8128465029875000525, 30.41246193502999873, -2.622577599952000238 ) ) ;
#6050=CARTESIAN_POINT ( 'NONE',  ( 0.000000000000000000, 13.10000000000000142, 0.000000000000000000 ) ) ;
#6054=DIRECTION ( 'NONE',  ( 0.000000000000000000, -1.000000000000000000, 0.000000000000000000 ) ) ;
#6055=VERTEX_POINT ( 'NONE', #4362 ) ;
#6057=DIRECTION ( 'NONE',  ( 0.000000000000000000, 1.000000000000000000, 0.000000000000000000 ) ) ;
#6058=CARTESIAN_POINT ( 'NONE',  ( -2.181221257712567141, 23.81760731231018369, 0.2322847663867408652 ) ) ;
#6069=CARTESIAN_POINT ( 'NONE',  ( 0.000000000000000000, 15.00000000000000000, 0.000000000000000000 ) ) ;
#6073=DIRECTION ( 'NONE',  ( 0.000000000000000000, -1.000000000000000000, 0.000000000000000000 ) ) ;
#6077=CARTESIAN_POINT ( 'NONE',  ( -1.880548603011000131, 29.11986934341000222, -1.127614642727999827 ) ) ;
#6080=CARTESIAN_POINT ( 'NONE',  ( 1.210944093517519971, 29.67954644253612884, 1.788468199683581172 ) ) ;
#6081=ORIENTED_EDGE ( 'NONE', *, *, #5543, .T. ) ;
#6083=CARTESIAN_POINT ( 'NONE',  ( -2.013021446580000262, 23.53766161991999795, -0.8520286084860999587 ) ) ;
#6085=ORIENTED_EDGE ( 'NONE', *, *, #5708, .T. ) ;
#6087=EDGE_CURVE ( 'NONE', #18500, #18102, #23244, .T. ) ;
#6091=ORIENTED_EDGE ( 'NONE', *, *, #23433, .T. ) ;
#6092=AXIS2_PLACEMENT_3D ( 'NONE', #15113, #3880, #3994 ) ;
#6093=DIRECTION ( 'NONE',  ( -0.7071067811865474617, -0.7071067811865474617, 0.000000000000000000 ) ) ;
#6100=CARTESIAN_POINT ( 'NONE',  ( 4.000000000000000000, 26.46241504948189416, 0.8002143650531878816 ) ) ;
#6106=CARTESIAN_POINT ( 'NONE',  ( 2.500000000000000000, 28.63419673618999894, 0.000000000000000000 ) ) ;
#6110=CARTESIAN_POINT ( 'NONE',  ( -0.06504580400199751200, 30.39993742280512734, 2.159169369958346518 ) ) ;
#6116=AXIS2_PLACEMENT_3D ( 'NONE', #5936, #2313, #3780 ) ;
#6118=CARTESIAN_POINT ( 'NONE',  ( 2.270811333173000435, 26.40614211381999965, -0.3140912549739999782 ) ) ;
#6120=DIRECTION ( 'NONE',  ( 1.000000000000000000, 0.000000000000000000, 0.000000000000000000 ) ) ;
#6122=AXIS2_PLACEMENT_3D ( 'NONE', #1838, #11163, #12747 ) ;
#6124=CARTESIAN_POINT ( 'NONE',  ( -3.999702431747993003, 24.50639765414745241, -0.3779811684369214220 ) ) ;
#6126=CIRCLE ( 'NONE', #4590, 4.000000000000000000 ) ;
#6127=CARTESIAN_POINT ( 'NONE',  ( -1.047143917943662350, 27.76680419753780527, 1.933088563971394613 ) ) ;
#6129=ORIENTED_EDGE ( 'NONE', *, *, #14833, .T. ) ;
#6135=DIRECTION ( 'NONE',  ( -0.000000000000000000, 1.000000000000000000, 0.000000000000000000 ) ) ;
#6136=EDGE_CURVE ( 'NONE', #16360, #11502, #1539, .T. ) ;
#6141=VECTOR ( 'NONE', #13930, 1000.000000000000000 ) ;
#6142=CARTESIAN_POINT ( 'NONE',  ( 3.999895459877826465, 24.70780860099995380, -1.909390889640790512 ) ) ;
#6143=VERTEX_POINT ( 'NONE', #23362 ) ;
#6145=CARTESIAN_POINT ( 'NONE',  ( -2.030073792688000367, 27.06456776951999998, -1.733846816783999989 ) ) ;
#6146=TOROIDAL_SURFACE ( 'NONE', #20853, 3.000000000000000000, 1.000000000000000000 ) ;
#6148=CARTESIAN_POINT ( 'NONE',  ( 2.095699401784793192, 28.97244882208192607, 0.5250962896352469045 ) ) ;
#6151=ADVANCED_FACE ( 'NONE', ( #23617, #2919 ), #17820, .T. ) ;
#6155=ORIENTED_EDGE ( 'NONE', *, *, #14821, .F. ) ;
#6158=CARTESIAN_POINT ( 'NONE',  ( 1.332518472557000067, 27.97049822781000117, 1.834054417453000019 ) ) ;
#6164=CIRCLE ( 'NONE', #19731, 2.000000000000000000 ) ;
#6169=CARTESIAN_POINT ( 'NONE',  ( -2.704380769729999745, 30.47523026870999985, 0.3249933680386999924 ) ) ;
#6171=CARTESIAN_POINT ( 'NONE',  ( -2.573651909687999950, 24.13278196464000303, -0.8679085051213999424 ) ) ;
#6173=ORIENTED_EDGE ( 'NONE', *, *, #19301, .F. ) ;
#6176=CARTESIAN_POINT ( 'NONE',  ( -2.296046026427999820, 29.04809310863999627, 1.505608598421000144 ) ) ;
#6179=DIRECTION ( 'NONE',  ( 0.000000000000000000, -1.000000000000000000, 0.000000000000000000 ) ) ;
#6187=CARTESIAN_POINT ( 'NONE',  ( 2.500000000000001776, 28.61753006952332967, 0.3272492347489252551 ) ) ;
#6193=VERTEX_POINT ( 'NONE', #10180 ) ;
#6194=ORIENTED_EDGE ( 'NONE', *, *, #15472, .T. ) ;
#6198=VERTEX_POINT ( 'NONE', #6780 ) ;
#6199=CARTESIAN_POINT ( 'NONE',  ( 1.764297223473136000, 13.00000000000000000, -1.071763214071401515 ) ) ;
#6206=CARTESIAN_POINT ( 'NONE',  ( -1.099135848509952051, 29.53578701925532357, 1.859266377551254346 ) ) ;
#6208=CARTESIAN_POINT ( 'NONE',  ( 1.453244340366000031, 24.09604374391000192, -1.632848260547999919 ) ) ;
#6210=CIRCLE ( 'NONE', #19775, 2.949999999999999734 ) ;
#6217=ADVANCED_FACE ( 'NONE', ( #19757 ), #4982, .T. ) ;
#6219=VERTEX_POINT ( 'NONE', #1091 ) ;
#6223=ORIENTED_EDGE ( 'NONE', *, *, #81, .F. ) ;
#6225=DIRECTION ( 'NONE',  ( -1.000000000000000000, 0.000000000000000000, 0.000000000000000000 ) ) ;
#6234=CARTESIAN_POINT ( 'NONE',  ( -2.500000000000000888, 29.01753006952332825, -0.3272492347489316944 ) ) ;
#6235=DIRECTION ( 'NONE',  ( 0.000000000000000000, 1.000000000000000000, 0.000000000000000000 ) ) ;
#6236=CARTESIAN_POINT ( 'NONE',  ( 2.140330047059040730, 30.58679688062958846, 0.2894183440755233039 ) ) ;
#6242=CARTESIAN_POINT ( 'NONE',  ( 1.120191590154000050, 25.72364211381999866, -2.000256872718999990 ) ) ;
#6243=CARTESIAN_POINT ( 'NONE',  ( 0.000000000000000000, 18.00000000000000000, 0.000000000000000000 ) ) ;
#6244=VERTEX_POINT ( 'NONE', #21690 ) ;
#6247=CARTESIAN_POINT ( 'NONE',  ( -4.000000000000115463, 24.49999999999976197, -0.1904558375376560198 ) ) ;
#6248=CARTESIAN_POINT ( 'NONE',  ( -2.199358294017834670, 28.43250573243029322, 0.04245723217612143441 ) ) ;
#6251=DIRECTION ( 'NONE',  ( 0.000000000000000000, -1.000000000000000000, 0.000000000000000000 ) ) ;
#6258=CARTESIAN_POINT ( 'NONE',  ( -1.928881730073939371, 28.53949304903204265, -1.071374732005587527 ) ) ;
#6262=CARTESIAN_POINT ( 'NONE',  ( -1.618278083580495963, 26.52244509682108742, -1.955444531118598173 ) ) ;
#6265=CARTESIAN_POINT ( 'NONE',  ( 1.569224139466999901, 28.23456776952000169, 2.159851832628000068 ) ) ;
#6266=CIRCLE ( 'NONE', #23295, 3.000000000000000000 ) ;
#6268=EDGE_CURVE ( 'NONE', #6055, #6143, #18181, .T. ) ;
#6269=CARTESIAN_POINT ( 'NONE',  ( 2.063594504837999888E-14, 28.80370090847999975, 2.160000000000000142 ) ) ;
#6274=ADVANCED_FACE ( 'NONE', ( #5217 ), #8507, .T. ) ;
#6279=DIRECTION ( 'NONE',  ( -1.000000000000000000, 0.000000000000000000, 0.000000000000000000 ) ) ;
#6284=ORIENTED_EDGE ( 'NONE', *, *, #20319, .F. ) ;
#6285=EDGE_CURVE ( 'NONE', #17341, #23303, #15829, .T. ) ;
#6288=EDGE_CURVE ( 'NONE', #2693, #13406, #14637, .T. ) ;
#6289=CARTESIAN_POINT ( 'NONE',  ( -0.3515821444375999971, 23.66184656560000121, 2.500975805065000390 ) ) ;
#6290=CARTESIAN_POINT ( 'NONE',  ( 0.000000000000000000, 15.00000000000000000, -2.704938617610999654E-14 ) ) ;
#6294=DIRECTION ( 'NONE',  ( 0.000000000000000000, 1.000000000000000000, 0.000000000000000000 ) ) ;
#6298=CARTESIAN_POINT ( 'NONE',  ( 0.3272492347489341924, 29.61753006952334033, -2.500000000000000888 ) ) ;
#6300=DIRECTION ( 'NONE',  ( 0.000000000000000000, 0.7071067811866525998, -0.7071067811864425456 ) ) ;
#6308=DIRECTION ( 'NONE',  ( 0.000000000000000000, 0.000000000000000000, 1.000000000000000000 ) ) ;
#6310=CARTESIAN_POINT ( 'NONE',  ( 1.402946323589000066, 25.50919433610000198, -2.505154520421000175 ) ) ;
#6311=ORIENTED_EDGE ( 'NONE', *, *, #3356, .T. ) ;
#6314=CARTESIAN_POINT ( 'NONE',  ( 4.000000000000000000, 24.80000000000000426, 2.309401076759000304 ) ) ;
#6315=FACE_OUTER_BOUND ( 'NONE', #6551, .T. ) ;
#6317=EDGE_CURVE ( 'NONE', #2821, #19900, #14874, .T. ) ;
#6319=CARTESIAN_POINT ( 'NONE',  ( 1.727213515435479740, 12.96860573960580254, -1.061287104562887551 ) ) ;
#6326=VECTOR ( 'NONE', #10861, 1000.000000000000000 ) ;
#6329=CARTESIAN_POINT ( 'NONE',  ( -1.856047877541181279, 29.47208282624109543, 1.104794950165609801 ) ) ;
#6330=VERTEX_POINT ( 'NONE', #10901 ) ;
#6331=CARTESIAN_POINT ( 'NONE',  ( -1.735522259956000068, 24.30543704041000197, -1.328937561357000030 ) ) ;
#6334=CARTESIAN_POINT ( 'NONE',  ( -4.724999978625000097, 14.90000002138000035, -2.519184009061999785E-09 ) ) ;
#6337=CYLINDRICAL_SURFACE ( 'NONE', #4124, 2.750000000000000000 ) ;
#6343=CARTESIAN_POINT ( 'NONE',  ( 0.000000000000000000, 15.00000000000000000, 0.000000000000000000 ) ) ;
#6344=ORIENTED_EDGE ( 'NONE', *, *, #18262, .F. ) ;
#6356=ADVANCED_FACE ( 'NONE', ( #14751 ), #8966, .T. ) ;
#6357=CARTESIAN_POINT ( 'NONE',  ( -2.061598702545497375, 30.16504885856303630, -0.6499987980253106867 ) ) ;
#6358=ORIENTED_EDGE ( 'NONE', *, *, #9766, .F. ) ;
#6361=CARTESIAN_POINT ( 'NONE',  ( -2.500000000000000000, 27.43419673618999965, 0.000000000000000000 ) ) ;
#6369=CARTESIAN_POINT ( 'NONE',  ( -1.533592183623019967, 28.53112818204400725, 1.575162359379769006 ) ) ;
#6371=DIRECTION ( 'NONE',  ( -1.000000000000000000, 0.000000000000000000, 0.000000000000000000 ) ) ;
#6373=LINE ( 'NONE', #23075, #2218 ) ;
#6379=CARTESIAN_POINT ( 'NONE',  ( 0.000000000000000000, 21.95000012746600149, -2.704938617610999654E-14 ) ) ;
#6382=EDGE_CURVE ( 'NONE', #20600, #13895, #12934, .T. ) ;
#6384=VERTEX_POINT ( 'NONE', #3519 ) ;
#6386=CARTESIAN_POINT ( 'NONE',  ( 1.450871306011999984, 28.12913313894999945, 1.996953125041000199 ) ) ;
#6389=CARTESIAN_POINT ( 'NONE',  ( 1.912977839466240892, 28.94241077574801579, 1.003607546239349890 ) ) ;
#6391=FACE_OUTER_BOUND ( 'NONE', #14306, .T. ) ;
#6399=DIRECTION ( 'NONE',  ( 1.000000000000000000, 0.000000000000000000, 0.000000000000000000 ) ) ;
#6402=B_SPLINE_CURVE_WITH_KNOTS ( 'NONE', 3,
 ( #19870, #3286, #10668, #8491, #23619, #5219, #19987, #15857 ),
 .UNSPECIFIED., .F., .F.,
 ( 4, 2, 2, 4 ),
 ( 0.000000000000000000, 0.2499999999999997224, 0.4999999999999994449, 1.000000000000000000 ),
 .UNSPECIFIED. ) ;
#6404=EDGE_CURVE ( 'NONE', #12389, #21355, #7967, .T. ) ;
#6408=CARTESIAN_POINT ( 'NONE',  ( -0.3559997375695000410, 30.27669110727999779, -2.700474074450999851 ) ) ;
#6412=DIRECTION ( 'NONE',  ( 0.000000000000000000, 1.000000000000000000, 0.000000000000000000 ) ) ;
#6413=DIRECTION ( 'NONE',  ( 0.000000000000000000, -1.000000000000000000, 0.000000000000000000 ) ) ;
#6415=CARTESIAN_POINT ( 'NONE',  ( -2.500000000000000000, 28.23419673618999681, 0.000000000000000000 ) ) ;
#6420=EDGE_LOOP ( 'NONE', ( #20614, #1738, #7835, #6811 ) ) ;
#6426=CARTESIAN_POINT ( 'NONE',  ( 0.7864549106799859635, 24.35740526346785018, -2.047056573199967033 ) ) ;
#6432=FACE_OUTER_BOUND ( 'NONE', #11699, .T. ) ;
#6433=EDGE_LOOP ( 'NONE', ( #6785, #9100, #15901, #17717, #21724, #5993 ) ) ;
#6444=ADVANCED_FACE ( 'NONE', ( #17046 ), #10403, .F. ) ;
#6447=EDGE_CURVE ( 'NONE', #3305, #11676, #11176, .T. ) ;
#6448=DIRECTION ( 'NONE',  ( -0.000000000000000000, 1.000000000000000000, 0.000000000000000000 ) ) ;
#6449=CARTESIAN_POINT ( 'NONE',  ( -1.485745231353044371, 29.50735104790518903, 1.567784488697564038 ) ) ;
#6450=ORIENTED_EDGE ( 'NONE', *, *, #13348, .F. ) ;
#6452=CARTESIAN_POINT ( 'NONE',  ( -2.163129499999000060, 23.57098390934999799, -0.9155631307312001033 ) ) ;
#6465=CARTESIAN_POINT ( 'NONE',  ( 0.000000000000000000, 12.90000000000000036, 0.000000000000000000 ) ) ;
#6467=CARTESIAN_POINT ( 'NONE',  ( 2.818367767609802232, 24.55137445130672091, -2.991616928423186383 ) ) ;
#6469=CARTESIAN_POINT ( 'NONE',  ( 2.399999999999999911, 26.50000000000000355, 0.000000000000000000 ) ) ;
#6470=CARTESIAN_POINT ( 'NONE',  ( -2.143277222256999792, 23.64327722226000006, 4.118360636503000477E-13 ) ) ;
#6474=CIRCLE ( 'NONE', #8008, 4.649999999999999467 ) ;
#6475=LINE ( 'NONE', #11691, #13714 ) ;
#6479=AXIS2_PLACEMENT_3D ( 'NONE', #21157, #6251, #2876 ) ;
#6480=CARTESIAN_POINT ( 'NONE',  ( 2.263491887170372419, 26.37901421991915640, -0.3060186196293296357 ) ) ;
#6485=CARTESIAN_POINT ( 'NONE',  ( -2.148122869378203958, 30.19035462121604496, -0.2261009145559444433 ) ) ;
#6490=CARTESIAN_POINT ( 'NONE',  ( 0.000000000000000000, -1.550000000000000044, 0.000000000000000000 ) ) ;
#6494=CIRCLE ( 'NONE', #4561, 2.948682383037074750 ) ;
#6499=CARTESIAN_POINT ( 'NONE',  ( 4.649999999999999467, 22.00000000000000000, 0.000000000000000000 ) ) ;
#6501=CARTESIAN_POINT ( 'NONE',  ( 4.749999920006001020, 24.30000007999099765, 4.227385663729999829E-08 ) ) ;
#6513=CARTESIAN_POINT ( 'NONE',  ( 0.1571687770951999963, 27.74706776952000098, -2.665093312283999705 ) ) ;
#6516=CIRCLE ( 'NONE', #8462, 1.500000000000000000 ) ;
#6523=B_SPLINE_CURVE_WITH_KNOTS ( 'NONE', 3,
 ( #19408, #19156, #13584, #21345, #20980, #8268, #21097, #22783, #6319, #2822, #6199, #21226 ),
 .UNSPECIFIED., .F., .F.,
 ( 4, 2, 2, 2, 2, 4 ),
 ( 0.000000000000000000, 0.2500000000000285882, 0.3750000000000284217, 0.4375000000000150435, 0.5000000000000016653, 1.000000000000000000 ),
 .UNSPECIFIED. ) ;
#6526=FACE_OUTER_BOUND ( 'NONE', #11006, .T. ) ;
#6527=EDGE_CURVE ( 'NONE', #8499, #15019, #9394, .T. ) ;
#6528=DIRECTION ( 'NONE',  ( 0.000000000000000000, -1.000000000000000000, 1.177781335444000003E-14 ) ) ;
#6532=AXIS2_PLACEMENT_3D ( 'NONE', #10552, #18184, #19871 ) ;
#6533=ORIENTED_EDGE ( 'NONE', *, *, #9983, .T. ) ;
#6535=CARTESIAN_POINT ( 'NONE',  ( 2.507121665491000240, 29.97271731528999794, -0.3598210903258999838 ) ) ;
#6539=DIRECTION ( 'NONE',  ( -1.000000000000000000, 0.000000000000000000, 0.000000000000000000 ) ) ;
#6542=ADVANCED_FACE ( 'NONE', ( #20564 ), #813, .T. ) ;
#6543=CARTESIAN_POINT ( 'NONE',  ( 0.2668645045036935337, 24.51773570851615602, -2.370970244263094440 ) ) ;
#6545=CARTESIAN_POINT ( 'NONE',  ( 0.000000000000000000, 7.100000000000000533, -1.499999999999985345 ) ) ;
#6546=CARTESIAN_POINT ( 'NONE',  ( -2.999999956181000016, 17.90000004382000043, 2.609181505839000138E-08 ) ) ;
#6551=EDGE_LOOP ( 'NONE', ( #18522, #9888, #18744, #21924 ) ) ;
#6553=CARTESIAN_POINT ( 'NONE',  ( 0.6185100627188000466, 25.68299631853999898, 2.270477015093999906 ) ) ;
#6554=CARTESIAN_POINT ( 'NONE',  ( -0.9242717917835999719, 23.66000000000000014, -1.952260652400999996 ) ) ;
#6555=CARTESIAN_POINT ( 'NONE',  ( 0.000000000000000000, 26.35000000000000142, 0.000000000000000000 ) ) ;
#6557=FACE_OUTER_BOUND ( 'NONE', #18307, .T. ) ;
#6558=EDGE_CURVE ( 'NONE', #8533, #10983, #12581, .T. ) ;
#6562=CARTESIAN_POINT ( 'NONE',  ( 0.000000000000000000, 20.05000017415440183, 0.000000000000000000 ) ) ;
#6565=ORIENTED_EDGE ( 'NONE', *, *, #18126, .F. ) ;
#6571=FACE_OUTER_BOUND ( 'NONE', #15737, .T. ) ;
#6572=EDGE_CURVE ( 'NONE', #12128, #2115, #17355, .T. ) ;
#6575=FACE_OUTER_BOUND ( 'NONE', #182, .T. ) ;
#6576=CARTESIAN_POINT ( 'NONE',  ( -1.679626819221629264, 29.31726910860015067, -1.358118087700189269 ) ) ;
#6582=ORIENTED_EDGE ( 'NONE', *, *, #3218, .F. ) ;
#6589=ADVANCED_FACE ( 'NONE', ( #19838 ), #20454, .T. ) ;
#6590=VERTEX_POINT ( 'NONE', #1056 ) ;
#6591=CARTESIAN_POINT ( 'NONE',  ( -4.549999999999999822, 22.00000000000000000, 0.000000000000000000 ) ) ;
#6592=CARTESIAN_POINT ( 'NONE',  ( 2.184465970885645092, 26.86666666666667780, -1.259047450927249123 ) ) ;
#6594=ORIENTED_EDGE ( 'NONE', *, *, #12899, .T. ) ;
#6605=DIRECTION ( 'NONE',  ( 1.000000000000000000, 0.000000000000000000, 0.000000000000000000 ) ) ;
#6606=CARTESIAN_POINT ( 'NONE',  ( -2.144556769453566769, 30.18852709384431066, -0.2572742967693883442 ) ) ;
#6611=CARTESIAN_POINT ( 'NONE',  ( 0.5866479046345639548, 24.19681692063821288, -2.175561667358837603 ) ) ;
#6614=ORIENTED_EDGE ( 'NONE', *, *, #15594, .F. ) ;
#6617=CARTESIAN_POINT ( 'NONE',  ( -2.202320941319727776, 26.82989092620764993, 0.008350029242332654075 ) ) ;
#6621=EDGE_LOOP ( 'NONE', ( #20888, #21696, #13595, #7715 ) ) ;
#6622=CARTESIAN_POINT ( 'NONE',  ( 2.500000000000000000, 26.80000000000000071, 0.000000000000000000 ) ) ;
#6633=CARTESIAN_POINT ( 'NONE',  ( 0.9334375154566999511, 28.80369850838000190, 1.831974274068000064 ) ) ;
#6636=VERTEX_POINT ( 'NONE', #15824 ) ;
#6640=DIRECTION ( 'NONE',  ( 0.000000000000000000, -1.000000000000000000, 0.000000000000000000 ) ) ;
#6642=CARTESIAN_POINT ( 'NONE',  ( -1.259047450927251788, 27.30086340285666680, -2.184465970885643316 ) ) ;
#6648=CARTESIAN_POINT ( 'NONE',  ( -1.536366799937290084, 28.68333333333333002, -1.999167105995448113 ) ) ;
#6649=CARTESIAN_POINT ( 'NONE',  ( 1.997291889306999968, 30.03889703575999803, -1.557547871342000123 ) ) ;
#6650=DIRECTION ( 'NONE',  ( 0.000000000000000000, 1.000000000000000000, 0.000000000000000000 ) ) ;
#6653=CARTESIAN_POINT ( 'NONE',  ( 0.000000000000000000, 20.00000000000000000, 0.000000000000000000 ) ) ;
#6656=PLANE ( 'NONE',  #17734 ) ;
#6660=DIRECTION ( 'NONE',  ( -1.000000000000000000, 0.000000000000000000, 0.000000000000000000 ) ) ;
#6661=EDGE_CURVE ( 'NONE', #13113, #10909, #713, .T. ) ;
#6664=DIRECTION ( 'NONE',  ( 0.000000000000000000, -1.000000000000000000, 9.414779719719000361E-11 ) ) ;
#6667=CARTESIAN_POINT ( 'NONE',  ( 2.241442604181999698, 25.09172815385999655, 1.205773825739000049 ) ) ;
#6669=DIRECTION ( 'NONE',  ( 0.000000000000000000, 0.000000000000000000, 1.000000000000000000 ) ) ;
#6671=FACE_OUTER_BOUND ( 'NONE', #14067, .T. ) ;
#6674=EDGE_CURVE ( 'NONE', #11959, #6143, #23552, .T. ) ;
#6675=VERTEX_POINT ( 'NONE', #21660 ) ;
#6677=CARTESIAN_POINT ( 'NONE',  ( 0.000000000000000000, 20.10000000000000142, 0.000000000000000000 ) ) ;
#6679=ORIENTED_EDGE ( 'NONE', *, *, #16355, .T. ) ;
#6681=CARTESIAN_POINT ( 'NONE',  ( 0.000000000000000000, 24.40000007355299871, 0.000000000000000000 ) ) ;
#6684=CARTESIAN_POINT ( 'NONE',  ( 0.3498527751141999875, 29.44093971554000078, 2.330099399188000131 ) ) ;
#6687=EDGE_LOOP ( 'NONE', ( #19506, #7006, #16542, #6344, #21546, #12671 ) ) ;
#6689=DIRECTION ( 'NONE',  ( -1.000000000000000000, 0.000000000000000000, 0.000000000000000000 ) ) ;
#6690=ADVANCED_FACE ( 'NONE', ( #23085 ), #13101, .T. ) ;
#6691=CARTESIAN_POINT ( 'NONE',  ( -1.768277280319097811, 29.48163746745662905, 1.241304826943840256 ) ) ;
#6695=CARTESIAN_POINT ( 'NONE',  ( 2.500060036629733418, 30.00618913924456876, -0.1188157828604838595 ) ) ;
#6703=LINE ( 'NONE', #21490, #22697 ) ;
#6706=DIRECTION ( 'NONE',  ( 0.000000000000000000, 0.000000000000000000, 1.000000000000000000 ) ) ;
#6708=CARTESIAN_POINT ( 'NONE',  ( 0.000000000000000000, 24.29999999999999716, 0.000000000000000000 ) ) ;
#6715=CARTESIAN_POINT ( 'NONE',  ( 1.099193499486128101, 26.43562577624027199, 3.984182490697167900 ) ) ;
#6716=DIRECTION ( 'NONE',  ( 0.000000000000000000, -1.000000000000000000, 0.000000000000000000 ) ) ;
#6718=CARTESIAN_POINT ( 'NONE',  ( -2.159896986047187273, 30.20407674326398251, 0.006713223370198041426 ) ) ;
#6721=CARTESIAN_POINT ( 'NONE',  ( 0.6085180536320998756, 25.64793633493999891, 2.255015312327000032 ) ) ;
#6724=CARTESIAN_POINT ( 'NONE',  ( 1.536366799937295413, 27.71753006952333465, 1.999167105995444338 ) ) ;
#6725=ORIENTED_EDGE ( 'NONE', *, *, #18144, .T. ) ;
#6726=DIRECTION ( 'NONE',  ( 0.000000000000000000, -1.000000000000000000, 0.000000000000000000 ) ) ;
#6732=DIRECTION ( 'NONE',  ( 0.000000000000000000, 1.000000000000000000, 0.000000000000000000 ) ) ;
#6734=CARTESIAN_POINT ( 'NONE',  ( 1.633102778084561724, 27.13808608125045296, 1.430956311882127352 ) ) ;
#6736=ORIENTED_EDGE ( 'NONE', *, *, #7310, .F. ) ;
#6743=CARTESIAN_POINT ( 'NONE',  ( -4.000000000000000000, 26.20000000000000284, -2.309401076759000304 ) ) ;
#6748=EDGE_CURVE ( 'NONE', #6244, #19945, #12704, .T. ) ;
#6749=AXIS2_PLACEMENT_3D ( 'NONE', #19557, #10596, #15651 ) ;
#6752=CARTESIAN_POINT ( 'NONE',  ( -0.3106091461881000382, 27.92619850838000062, 2.245636445400999825 ) ) ;
#6758=VERTEX_POINT ( 'NONE', #18872 ) ;
#6764=AXIS2_PLACEMENT_3D ( 'NONE', #14108, #21269, #4677 ) ;
#6766=FACE_OUTER_BOUND ( 'NONE', #4863, .T. ) ;
#6772=CARTESIAN_POINT ( 'NONE',  ( 0.4178678117584000429, 29.87961278443000168, 2.691594793395000185 ) ) ;
#6777=CARTESIAN_POINT ( 'NONE',  ( -1.067140290979515571, 26.49999999999999645, -2.247699653298786515 ) ) ;
#6780=CARTESIAN_POINT ( 'NONE',  ( -4.724999999999999645, 13.10000000000000142, 0.000000000000000000 ) ) ;
#6785=ORIENTED_EDGE ( 'NONE', *, *, #21266, .F. ) ;
#6786=DIRECTION ( 'NONE',  ( -1.000000000000000000, 0.000000000000000000, 0.000000000000000000 ) ) ;
#6789=CARTESIAN_POINT ( 'NONE',  ( -2.203461932915999899, 24.77914110727999741, -1.623795195417000015 ) ) ;
#6790=CARTESIAN_POINT ( 'NONE',  ( 0.000000000000000000, 24.49999999999999645, 0.000000000000000000 ) ) ;
#6791=FACE_OUTER_BOUND ( 'NONE', #20218, .T. ) ;
#6794=CARTESIAN_POINT ( 'NONE',  ( -0.3272492347489393549, 27.81666666666668064, -2.499999999999999556 ) ) ;
#6797=CARTESIAN_POINT ( 'NONE',  ( -2.184465970885641983, 29.90086340285667177, 1.259047450927253564 ) ) ;
#6800=DIRECTION ( 'NONE',  ( 0.000000000000000000, -1.000000000000000000, 0.000000000000000000 ) ) ;
#6806=CARTESIAN_POINT ( 'NONE',  ( 3.999702431745993270, 24.50639765414744531, 0.3779811684581091957 ) ) ;
#6808=CARTESIAN_POINT ( 'NONE',  ( -2.167698761436000154, 29.29258811475999735, 0.03558365842844000287 ) ) ;
#6811=ORIENTED_EDGE ( 'NONE', *, *, #9715, .T. ) ;
#6812=AXIS2_PLACEMENT_3D ( 'NONE', #9265, #15170, #9378 ) ;
#6813=DIRECTION ( 'NONE',  ( 1.000000000000000000, 0.000000000000000000, 0.000000000000000000 ) ) ;
#6814=CARTESIAN_POINT ( 'NONE',  ( -0.8021525768333287454, 29.25217003084671674, -2.005518083782086514 ) ) ;
#6816=DIRECTION ( 'NONE',  ( 1.000000000000000000, 0.000000000000000000, 0.000000000000000000 ) ) ;
#6824=EDGE_LOOP ( 'NONE', ( #20240, #6679, #5712, #11672, #15964, #15144 ) ) ;
#6830=ORIENTED_EDGE ( 'NONE', *, *, #464, .F. ) ;
#6839=CARTESIAN_POINT ( 'NONE',  ( -1.215228304390323144, 30.08000406326414478, -1.785700434939019532 ) ) ;
#6840=ORIENTED_EDGE ( 'NONE', *, *, #9240, .T. ) ;
#6841=CARTESIAN_POINT ( 'NONE',  ( 1.694552266659000050, 25.71773410043999775, 1.607489577807000192 ) ) ;
#6843=CARTESIAN_POINT ( 'NONE',  ( -2.326721815211127023E-16, 9.000000000000000000, 1.899912543625706274 ) ) ;
#6845=CYLINDRICAL_SURFACE ( 'NONE', #4116, 2.500000000000000000 ) ;
#6852=ORIENTED_EDGE ( 'NONE', *, *, #12229, .F. ) ;
#6863=CIRCLE ( 'NONE', #11371, 2.949999999999999734 ) ;
#6865=CARTESIAN_POINT ( 'NONE',  ( 0.000000000000000000, 24.80000000000000426, 4.618802153517000519 ) ) ;
#6867=CARTESIAN_POINT ( 'NONE',  ( 2.064425410739836764, 26.64466069140416593, -0.6742583458788029560 ) ) ;
#6871=EDGE_LOOP ( 'NONE', ( #9259, #6922, #10095, #8467 ) ) ;
#6874=CARTESIAN_POINT ( 'NONE',  ( -2.214344957515000267, 26.17119850838000161, 0.4858445502740000310 ) ) ;
#6875=VECTOR ( 'NONE', #5403, 1000.000000000000000 ) ;
#6877=B_SPLINE_CURVE_WITH_KNOTS ( 'NONE', 3,
 ( #7045, #5121, #8875, #20005 ),
 .UNSPECIFIED., .F., .F.,
 ( 4, 4 ),
 ( 0.000000000000000000, 1.000000000000000000 ),
 .UNSPECIFIED. ) ;
#6886=EDGE_CURVE ( 'NONE', #4269, #8374, #23162, .T. ) ;
#6889=VECTOR ( 'NONE', #21789, 1000.000000000000114 ) ;
#6894=CARTESIAN_POINT ( 'NONE',  ( 2.135264558818000147, 30.59525960993000027, 0.9615570694947999097 ) ) ;
#6897=EDGE_LOOP ( 'NONE', ( #14042, #18703, #5594, #23800 ) ) ;
#6902=ADVANCED_FACE ( 'NONE', ( #15830 ), #8081, .T. ) ;
#6904=EDGE_CURVE ( 'NONE', #5348, #3528, #8701, .T. ) ;
#6907=CONICAL_SURFACE ( 'NONE', #17338, 2.949999944334000368, 0.7853981633972997312 ) ;
#6911=CARTESIAN_POINT ( 'NONE',  ( 2.309807618587000011, 30.69019238141000017, -7.292675330123999428E-08 ) ) ;
#6913=AXIS2_PLACEMENT_3D ( 'NONE', #15138, #606, #11769 ) ;
#6915=CARTESIAN_POINT ( 'NONE',  ( 0.6691735853424000124, 24.29144915060000187, 2.654084007310999915 ) ) ;
#6922=ORIENTED_EDGE ( 'NONE', *, *, #28, .F. ) ;
#6924=AXIS2_PLACEMENT_3D ( 'NONE', #10749, #19950, #7337 ) ;
#6926=CARTESIAN_POINT ( 'NONE',  ( -4.000024251878889991, 24.52555747447230416, 0.7498250608958048069 ) ) ;
#6927=ORIENTED_EDGE ( 'NONE', *, *, #13514, .F. ) ;
#6929=DIRECTION ( 'NONE',  ( 0.000000000000000000, -1.000000000000000000, 0.000000000000000000 ) ) ;
#6932=CARTESIAN_POINT ( 'NONE',  ( 4.000000142207500886, 24.55137445130360518, 0.9449696197344532589 ) ) ;
#6934=CARTESIAN_POINT ( 'NONE',  ( 0.4664974798648000021, 28.71811702996999927, 2.117149378852999586 ) ) ;
#6939=CIRCLE ( 'NONE', #6532, 4.750000000000000000 ) ;
#6940=ORIENTED_EDGE ( 'NONE', *, *, #18141, .F. ) ;
#6946=CARTESIAN_POINT ( 'NONE',  ( 0.9911964488588560496, 30.15065117088173707, -2.420280545933024552 ) ) ;
#6951=EDGE_LOOP ( 'NONE', ( #16374, #20619, #12309 ) ) ;
#6954=AXIS2_PLACEMENT_3D ( 'NONE', #8074, #544, #6120 ) ;
#6958=CARTESIAN_POINT ( 'NONE',  ( 1.699986466736000068, 9.100024030970999434, -1.053574575520999757 ) ) ;
#6961=CARTESIAN_POINT ( 'NONE',  ( 1.566978647078999920, 29.92110055533999713, -1.741866172968000059 ) ) ;
#6963=CARTESIAN_POINT ( 'NONE',  ( -0.5809343010167346000, 30.03825264969940179, -2.087773477905597641 ) ) ;
#6970=EDGE_LOOP ( 'NONE', ( #739, #19055, #11218, #16402 ) ) ;
#6972=CARTESIAN_POINT ( 'NONE',  ( -1.042632460611140788, 24.73976796275902146, 1.891962004173780576 ) ) ;
#6980=DIRECTION ( 'NONE',  ( 0.000000000000000000, -1.000000000000000000, 0.000000000000000000 ) ) ;
#6989=CARTESIAN_POINT ( 'NONE',  ( 1.805717673759776210, 27.47944697561501570, -1.207647802767778167 ) ) ;
#6991=CARTESIAN_POINT ( 'NONE',  ( 2.146186176612843610, 30.61809763272861318, -0.2430268685427999509 ) ) ;
#6993=DIRECTION ( 'NONE',  ( -1.000000000000000000, 0.000000000000000000, 0.000000000000000000 ) ) ;
#6995=CARTESIAN_POINT ( 'NONE',  ( -2.411020654974999733, 26.27663313894999675, 0.5289967318968999965 ) ) ;
#6998=CARTESIAN_POINT ( 'NONE',  ( -1.862634475845999837, 26.92437716036000239, -1.590840130251000017 ) ) ;
#6999=AXIS2_PLACEMENT_3D ( 'NONE', #19997, #1472, #17831 ) ;
#7001=ORIENTED_EDGE ( 'NONE', *, *, #18501, .T. ) ;
#7006=ORIENTED_EDGE ( 'NONE', *, *, #6886, .T. ) ;
#7008=CARTESIAN_POINT ( 'NONE',  ( -1.978156802582415441, 30.64141917833904927, -1.302609384799360503 ) ) ;
#7014=CARTESIAN_POINT ( 'NONE',  ( 1.417687315775000068, 28.83533196750000016, 1.617399067864000006 ) ) ;
#7015=DIRECTION ( 'NONE',  ( 0.000000000000000000, -0.7071067811866525998, -0.7071067811864425456 ) ) ;
#7017=EDGE_LOOP ( 'NONE', ( #5836, #2576, #19183, #15290 ) ) ;
#7020=CARTESIAN_POINT ( 'NONE',  ( 0.000000000000000000, 22.10000000618969906, -2.849999993810000021 ) ) ;
#7023=CARTESIAN_POINT ( 'NONE',  ( 0.000000000000000000, 26.50000000000000355, 0.000000000000000000 ) ) ;
#7026=EDGE_CURVE ( 'NONE', #2748, #4269, #9564, .T. ) ;
#7027=CARTESIAN_POINT ( 'NONE',  ( 3.000000000000000000, 22.00000000000000000, 0.000000000000000000 ) ) ;
#7031=FACE_OUTER_BOUND ( 'NONE', #5511, .T. ) ;
#7033=CARTESIAN_POINT ( 'NONE',  ( -2.496851939000000353, 25.57942011053999920, 0.4936453752708000464 ) ) ;
#7037=CARTESIAN_POINT ( 'NONE',  ( 0.000000000000000000, 20.04999987253367877, -4.699999872533999756 ) ) ;
#7045=CARTESIAN_POINT ( 'NONE',  ( 1.699986747157999911, 9.000014340785000400, 0.8485215224771999187 ) ) ;
#7048=CARTESIAN_POINT ( 'NONE',  ( 0.8298323553694000321, 23.83132231056999828, 2.182665959441000059 ) ) ;
#7050=AXIS2_PLACEMENT_3D ( 'NONE', #22628, #3886, #19000 ) ;
#7051=FACE_OUTER_BOUND ( 'NONE', #12119, .T. ) ;
#7053=CARTESIAN_POINT ( 'NONE',  ( 1.399243530816999925, 29.57982365715999862, 1.655989627749000048 ) ) ;
#7057=VERTEX_POINT ( 'NONE', #9866 ) ;
#7059=CIRCLE ( 'NONE', #19043, 2.000000000000000000 ) ;
#7060=DIRECTION ( 'NONE',  ( 0.000000000000000000, -1.000000000000000000, 0.000000000000000000 ) ) ;
#7075=CARTESIAN_POINT ( 'NONE',  ( -2.900806500513820829, 26.43562577624027199, 2.944020739578862234 ) ) ;
#7078=CARTESIAN_POINT ( 'NONE',  ( 0.3650451777216000004, 30.01137937871000005, -2.157632473909999682 ) ) ;
#7080=CARTESIAN_POINT ( 'NONE',  ( 1.951256826536600819, 29.86029468836431278, -0.9263714941426136606 ) ) ;
#7084=CARTESIAN_POINT ( 'NONE',  ( -0.9283276469500318928, 23.62785179069575037, -1.914674717947229654 ) ) ;
#7093=CARTESIAN_POINT ( 'NONE',  ( -0.8814048238219360787, 26.68195725178709310, -2.014038470394164726 ) ) ;
#7094=CARTESIAN_POINT ( 'NONE',  ( -2.184465970885641539, 29.66666666666666075, 1.259047450927253120 ) ) ;
#7102=CARTESIAN_POINT ( 'NONE',  ( -0.5748490789388736033, 27.63845388675433767, -2.129056650025603403 ) ) ;
#7104=CARTESIAN_POINT ( 'NONE',  ( 1.990833611345558474, 30.65463416023253984, -0.8378372468001260565 ) ) ;
#7106=CARTESIAN_POINT ( 'NONE',  ( -2.399999999999999911, 24.50000000000000000, 0.000000000000000000 ) ) ;
#7108=CARTESIAN_POINT ( 'NONE',  ( 1.657421040685276070, 24.74463929172237542, 1.377955417119847370 ) ) ;
#7110=CARTESIAN_POINT ( 'NONE',  ( 0.4912911496346000217, 28.16114211382000221, -2.239169049547999890 ) ) ;
#7113=ORIENTED_EDGE ( 'NONE', *, *, #5708, .F. ) ;
#7116=CARTESIAN_POINT ( 'NONE',  ( 1.327700301679965333, 30.30949148887719957, 1.851068045074677926 ) ) ;
#7119=CARTESIAN_POINT ( 'NONE',  ( 0.3272492347489778242, 24.21666666666666856, 2.499999999999994671 ) ) ;
#7125=CARTESIAN_POINT ( 'NONE',  ( -0.3060659231994000140, 30.06582184614000042, -2.321695786394999850 ) ) ;
#7129=ORIENTED_EDGE ( 'NONE', *, *, #20589, .T. ) ;
#7132=DIRECTION ( 'NONE',  ( 0.000000000000000000, 0.000000000000000000, 1.000000000000000000 ) ) ;
#7135=AXIS2_PLACEMENT_3D ( 'NONE', #4865, #1590, #4989 ) ;
#7139=ORIENTED_EDGE ( 'NONE', *, *, #2363, .F. ) ;
#7141=CARTESIAN_POINT ( 'NONE',  ( -4.000000000000000000, 26.20000000000000284, 2.309401076759000304 ) ) ;
#7142=ORIENTED_EDGE ( 'NONE', *, *, #12622, .T. ) ;
#7145=CARTESIAN_POINT ( 'NONE',  ( -2.184465970885646424, 27.93333333333333712, -1.259047450927245126 ) ) ;
#7146=EDGE_CURVE ( 'NONE', #12189, #13776, #23722, .T. ) ;
#7151=CARTESIAN_POINT ( 'NONE',  ( -4.000000000000117240, 24.49999999999976907, 0.3805779584833384743 ) ) ;
#7153=EDGE_LOOP ( 'NONE', ( #21700, #17851, #19296, #16433 ) ) ;
#7155=CARTESIAN_POINT ( 'NONE',  ( -2.049853467200000168, 23.68059248353999990, -0.1598001849699000054 ) ) ;
#7161=CARTESIAN_POINT ( 'NONE',  ( 0.000000000000000000, 24.49999999999999645, -2.949999999999969091 ) ) ;
#7177=DIRECTION ( 'NONE',  ( 0.000000000000000000, 0.000000000000000000, 1.000000000000000000 ) ) ;
#7180=ORIENTED_EDGE ( 'NONE', *, *, #21504, .F. ) ;
#7188=CARTESIAN_POINT ( 'NONE',  ( 1.444497674103000007, 29.12979332792999898, -1.844707417364999991 ) ) ;
#7190=CARTESIAN_POINT ( 'NONE',  ( 1.230364976846351821, 29.92667673716075427, -1.776183484651385758 ) ) ;
#7191=EDGE_CURVE ( 'NONE', #6055, #4848, #23431, .T. ) ;
#7192=VERTEX_POINT ( 'NONE', #6958 ) ;
#7194=EDGE_CURVE ( 'NONE', #14748, #21798, #5729, .T. ) ;
#7196=CARTESIAN_POINT ( 'NONE',  ( -0.8631307901486540146, 23.64762543080364310, -1.966548252814039000 ) ) ;
#7198=CARTESIAN_POINT ( 'NONE',  ( -1.350411050691750381, 23.74852911982829085, 1.803795205562840787 ) ) ;
#7203=DIRECTION ( 'NONE',  ( 0.000000000000000000, -1.000000000000000000, 0.000000000000000000 ) ) ;
#7206=LINE ( 'NONE', #3589, #17946 ) ;
#7208=VECTOR ( 'NONE', #3114, 1000.000000000000000 ) ;
#7216=CIRCLE ( 'NONE', #638, 0.5500000000000001554 ) ;
#7217=CARTESIAN_POINT ( 'NONE',  ( -2.857252503208999705, 28.04750240010000084, -0.2814148094396999866 ) ) ;
#7220=CARTESIAN_POINT ( 'NONE',  ( 6.356497079780072168E-07, 30.81706029784504963, -2.183072574220335849 ) ) ;
#7222=CARTESIAN_POINT ( 'NONE',  ( 4.749999920006001020, 24.30000007999099765, 4.227385663729999829E-08 ) ) ;
#7223=CARTESIAN_POINT ( 'NONE',  ( -2.283846754818999791, 27.04021896306000272, 0.1346854910758999990 ) ) ;
#7226=ORIENTED_EDGE ( 'NONE', *, *, #190, .F. ) ;
#7229=FACE_OUTER_BOUND ( 'NONE', #7331, .T. ) ;
#7233=DIRECTION ( 'NONE',  ( 0.000000000000000000, 1.000000000000000000, 0.000000000000000000 ) ) ;
#7234=B_SPLINE_CURVE_WITH_KNOTS ( 'NONE', 3,
 ( #20720, #2312, #2843, #13603, #15417, #17743, #11803, #19181 ),
 .UNSPECIFIED., .F., .F.,
 ( 4, 2, 2, 4 ),
 ( 0.000000000000000000, 0.2499999999999999445, 0.4999999999999998890, 1.000000000000000000 ),
 .UNSPECIFIED. ) ;
#7240=CARTESIAN_POINT ( 'NONE',  ( -0.3083377756936999670, 28.72503243337000001, 2.063798408617000035 ) ) ;
#7245=DIRECTION ( 'NONE',  ( -1.000000000000000000, 0.000000000000000000, 0.000000000000000000 ) ) ;
#7247=CARTESIAN_POINT ( 'NONE',  ( -3.099999776787000005, 20.00000022320933013, -5.570936493763999179E-07 ) ) ;
#7249=DIRECTION ( 'NONE',  ( 0.000000000000000000, 0.000000000000000000, -1.000000000000000000 ) ) ;
#7252=CARTESIAN_POINT ( 'NONE',  ( -0.8751670430457477723, 29.25681791730888293, -1.975049169652319581 ) ) ;
#7254=ORIENTED_EDGE ( 'NONE', *, *, #10548, .T. ) ;
#7264=ORIENTED_EDGE ( 'NONE', *, *, #12758, .T. ) ;
#7266=CARTESIAN_POINT ( 'NONE',  ( 2.948682383037186217, 22.00131761696259503, 0.000000000000000000 ) ) ;
#7267=VECTOR ( 'NONE', #15880, 1000.000000000000000 ) ;
#7272=CARTESIAN_POINT ( 'NONE',  ( -0.2813946553678000062, 25.47374368677000334, 2.126068569715000134 ) ) ;
#7276=CARTESIAN_POINT ( 'NONE',  ( -1.050320413202000092, 30.22610362754999969, 1.896578797062999922 ) ) ;
#7283=CARTESIAN_POINT ( 'NONE',  ( -2.000000000000000000, 26.50000000000000355, -3.464101615137999968 ) ) ;
#7286=CARTESIAN_POINT ( 'NONE',  ( -2.388006305967797732E-16, 9.050044887908999414, 1.949955127985000258 ) ) ;
#7287=CARTESIAN_POINT ( 'NONE',  ( 0.000000000000000000, 24.49999999999999645, 0.000000000000000000 ) ) ;
#7288=CARTESIAN_POINT ( 'NONE',  ( 0.000000000000000000, 20.10000000000000142, 0.000000000000000000 ) ) ;
#7290=AXIS2_PLACEMENT_3D ( 'NONE', #18040, #1446, #8842 ) ;
#7293=CARTESIAN_POINT ( 'NONE',  ( 0.5899383557787000187, 28.40169433610000027, 2.621867217767999581 ) ) ;
#7304=B_SPLINE_CURVE_WITH_KNOTS ( 'NONE', 3,
 ( #5773, #17234, #18373, #187, #7579, #1784, #15531, #75, #23940, #7460, #14842, #19175, #15411, #764, #14958, #3961, #22127, #22355, #17361, #7347, #22918, #19052, #2463 ),
 .UNSPECIFIED., .F., .F.,
 ( 4, 2, 2, 2, 2, 1, 2, 2, 2, 2, 2, 4 ),
 ( 0.000000000000000000, 0.2499999999999582556, 0.3749999999999373834, 0.4374999999999283906, 0.4999999999999193978, 0.5624999999999104050, 0.5937499999999095168, 0.6249999999999086286, 0.6874999999998993028, 0.7187499999999114042, 0.7499999999999235056, 1.000000000000000000 ),
 .UNSPECIFIED. ) ;
#7306=TOROIDAL_SURFACE ( 'NONE', #13119, 2.500000000000000000, 0.5500000000000000444 ) ;
#7307=CARTESIAN_POINT ( 'NONE',  ( -0.7572660196559000134, 30.85628182409999809, -2.217212191475999905 ) ) ;
#7308=CIRCLE ( 'NONE', #6924, 3.000000000000000000 ) ;
#7310=EDGE_CURVE ( 'NONE', #12379, #14207, #7419, .T. ) ;
#7311=CARTESIAN_POINT ( 'NONE',  ( 0.8715030722649804718, 29.95105470813893334, -1.976208964316035210 ) ) ;
#7313=CARTESIAN_POINT ( 'NONE',  ( -0.1534377328957000075, 23.64214293815999923, -2.069255304278999841 ) ) ;
#7315=CARTESIAN_POINT ( 'NONE',  ( -0.9242717917835999719, 23.66000000000000014, -1.952260652400999996 ) ) ;
#7316=EDGE_LOOP ( 'NONE', ( #6155, #4202, #2804 ) ) ;
#7318=CARTESIAN_POINT ( 'NONE',  ( -0.5949149593206247699, 24.54751201496592472, -2.281015981353338162 ) ) ;
#7319=FACE_OUTER_BOUND ( 'NONE', #3607, .T. ) ;
#7323=AXIS2_PLACEMENT_3D ( 'NONE', #7287, #14339, #23766 ) ;
#7325=ORIENTED_EDGE ( 'NONE', *, *, #4638, .T. ) ;
#7327=CARTESIAN_POINT ( 'NONE',  ( 2.394884942776999814, 23.89488494277999919, 0.000000000000000000 ) ) ;
#7331=EDGE_LOOP ( 'NONE', ( #2207, #4129, #14901, #7325, #12945, #1478, #8697 ) ) ;
#7332=EDGE_CURVE ( 'NONE', #11498, #14519, #18407, .T. ) ;
#7337=DIRECTION ( 'NONE',  ( -1.000000000000000000, 0.000000000000000000, 0.000000000000000000 ) ) ;
#7339=CARTESIAN_POINT ( 'NONE',  ( -0.3658598526173800214, 27.98296886073505618, 2.142157184475797393 ) ) ;
#7342=VERTEX_POINT ( 'NONE', #3566 ) ;
#7346=CARTESIAN_POINT ( 'NONE',  ( -0.6650079486839999277, 28.55114211381999922, 2.193490157264000207 ) ) ;
#7347=CARTESIAN_POINT ( 'NONE',  ( -2.136277960958246513, 30.85236464670898471, 0.2205790306774752796 ) ) ;
#7349=CARTESIAN_POINT ( 'NONE',  ( -2.000000000000000000, 18.89999999999999858, -5.041390465489999878E-11 ) ) ;
#7350=ORIENTED_EDGE ( 'NONE', *, *, #4145, .T. ) ;
#7356=CARTESIAN_POINT ( 'NONE',  ( -1.235289751754999887, 30.50000000000000000, -2.173490103315000255 ) ) ;
#7359=CARTESIAN_POINT ( 'NONE',  ( -2.434931691670788378, 29.06753006952332896, 0.6543697108982053923 ) ) ;
#7360=CARTESIAN_POINT ( 'NONE',  ( 2.318031435825999687, 29.86728268470999836, -0.3326829368231999928 ) ) ;
#7361=DIRECTION ( 'NONE',  ( 0.000000000000000000, -1.000000000000000000, 0.000000000000000000 ) ) ;
#7364=CARTESIAN_POINT ( 'NONE',  ( -1.999167105995442562, 28.88333333333333641, 1.536366799937298300 ) ) ;
#7366=CARTESIAN_POINT ( 'NONE',  ( 2.500000000000001776, 29.18333333333333357, 0.3272492347489251441 ) ) ;
#7367=ORIENTED_EDGE ( 'NONE', *, *, #20031, .T. ) ;
#7372=CARTESIAN_POINT ( 'NONE',  ( -0.2449543915955024187, 29.21838483711510293, -2.145887526803566647 ) ) ;
#7377=EDGE_LOOP ( 'NONE', ( #11864, #14543, #1249 ) ) ;
#7378=CARTESIAN_POINT ( 'NONE',  ( -0.2920304106900999952, 25.26497464138999760, -2.335031432767999959 ) ) ;
#7379=CARTESIAN_POINT ( 'NONE',  ( -0.3272492347489287523, 28.18333333333333357, 2.500000000000001332 ) ) ;
#7381=DIRECTION ( 'NONE',  ( -0.7071067811868960717, 0.7071067811861969643, -5.329912173642970297E-08 ) ) ;
#7388=DIRECTION ( 'NONE',  ( 1.000000000000000000, 0.000000000000000000, 0.000000000000000000 ) ) ;
#7391=CARTESIAN_POINT ( 'NONE',  ( 1.982157587870999826, 24.85598014098999897, -1.234381845068999839 ) ) ;
#7396=CARTESIAN_POINT ( 'NONE',  ( 0.4321025471916000171, 29.76162456898000030, -2.320663853759999729 ) ) ;
#7401=ORIENTED_EDGE ( 'NONE', *, *, #3763, .T. ) ;
#7402=CARTESIAN_POINT ( 'NONE',  ( -4.750000000000000000, 15.09999999999999964, 0.000000000000000000 ) ) ;
#7404=ORIENTED_EDGE ( 'NONE', *, *, #6268, .F. ) ;
#7405=FACE_OUTER_BOUND ( 'NONE', #17091, .T. ) ;
#7406=FACE_OUTER_BOUND ( 'NONE', #1003, .T. ) ;
#7407=ADVANCED_FACE ( 'NONE', ( #4149 ), #7959, .T. ) ;
#7411=CARTESIAN_POINT ( 'NONE',  ( -2.583184600869000036, 28.24712896667000095, -0.6741018852137000694 ) ) ;
#7419=LINE ( 'NONE', #9132, #11443 ) ;
#7422=EDGE_CURVE ( 'NONE', #3528, #5391, #20346, .T. ) ;
#7423=CARTESIAN_POINT ( 'NONE',  ( 1.417967650155999904, 30.30418396362999900, 1.881788475004999794 ) ) ;
#7425=CARTESIAN_POINT ( 'NONE',  ( 1.173990260879828496, 29.93071037106722798, -1.813501616305194686 ) ) ;
#7427=CARTESIAN_POINT ( 'NONE',  ( -0.6137755221146999896, 25.35240352290000132, 2.097951008038000165 ) ) ;
#7430=ORIENTED_EDGE ( 'NONE', *, *, #15315, .T. ) ;
#7434=DIRECTION ( 'NONE',  ( 1.000000000000000000, 0.000000000000000000, 0.000000000000000000 ) ) ;
#7437=CIRCLE ( 'NONE', #21759, 3.050000000000000266 ) ;
#7439=EDGE_CURVE ( 'NONE', #6219, #16646, #4512, .T. ) ;
#7440=CARTESIAN_POINT ( 'NONE',  ( 0.3272492347489455167, 29.81666666666667709, 2.499999999999998668 ) ) ;
#7441=EDGE_LOOP ( 'NONE', ( #15373, #7264, #14822, #1211, #11103, #5507 ) ) ;
#7442=DIRECTION ( 'NONE',  ( -0.000000000000000000, -1.000000000000000000, -0.000000000000000000 ) ) ;
#7445=ADVANCED_FACE ( 'NONE', ( #13464 ), #12611, .T. ) ;
#7449=CARTESIAN_POINT ( 'NONE',  ( 0.000000000000000000, 26.50000000000000355, 0.000000000000000000 ) ) ;
#7456=CONICAL_SURFACE ( 'NONE', #3975, 4.309401076758999416, 1.119376321708719590 ) ;
#7458=CARTESIAN_POINT ( 'NONE',  ( -2.445277951317000209, 27.02187716036000253, 0.1442055869096000031 ) ) ;
#7460=CARTESIAN_POINT ( 'NONE',  ( -2.124284333938379898, 30.86714579923354407, 0.1911072213488915206 ) ) ;
#7462=EDGE_LOOP ( 'NONE', ( #16813, #3441 ) ) ;
#7464=CARTESIAN_POINT ( 'NONE',  ( -0.9242717917835999719, 23.66000000000000014, -1.952260652400999996 ) ) ;
#7465=CARTESIAN_POINT ( 'NONE',  ( 0.4169900196955230176, 29.80682928967814860, -2.239500026962490953 ) ) ;
#7466=VERTEX_POINT ( 'NONE', #9958 ) ;
#7471=ADVANCED_FACE ( 'NONE', ( #747 ), #15675, .T. ) ;
#7473=CARTESIAN_POINT ( 'NONE',  ( -0.8375484967288000515, 29.60256380282000066, 2.186883670786000433 ) ) ;
#7477=CARTESIAN_POINT ( 'NONE',  ( -2.104642740648948074, 30.88517755921813901, -0.2852235104369513219 ) ) ;
#7482=EDGE_LOOP ( 'NONE', ( #5607, #12750 ) ) ;
#7486=CARTESIAN_POINT ( 'NONE',  ( -1.291923323229889231, 29.28551790513946074, -1.731104546042324221 ) ) ;
#7487=DIRECTION ( 'NONE',  ( 0.000000000000000000, 0.000000000000000000, -1.000000000000000000 ) ) ;
#7489=EDGE_CURVE ( 'NONE', #21635, #15998, #6013, .T. ) ;
#7491=CARTESIAN_POINT ( 'NONE',  ( -0.2897094055803834389, 23.75786872615814005, 2.255733293301447784 ) ) ;
#7493=CARTESIAN_POINT ( 'NONE',  ( 0.5753128712306000425, 24.08057988946000094, 2.281812558324999962 ) ) ;
#7496=B_SPLINE_CURVE_WITH_KNOTS ( 'NONE', 3,
 ( #4885, #4395, #12273, #8272, #19660, #13708, #4516, #2945 ),
 .UNSPECIFIED., .F., .F.,
 ( 4, 2, 2, 4 ),
 ( 0.000000000000000000, 0.2499999999999998890, 0.4999999999999997780, 1.000000000000000000 ),
 .UNSPECIFIED. ) ;
#7498=FACE_OUTER_BOUND ( 'NONE', #9216, .T. ) ;
#7500=AXIS2_PLACEMENT_3D ( 'NONE', #8514, #10199, #23021 ) ;
#7501=AXIS2_PLACEMENT_3D ( 'NONE', #2229, #18821, #13484 ) ;
#7503=DIRECTION ( 'NONE',  ( -1.000000000000000000, 0.000000000000000000, 0.000000000000000000 ) ) ;
#7507=CARTESIAN_POINT ( 'NONE',  ( -1.578943844734999935, 24.27961011138000202, -1.720344029022000010 ) ) ;
#7511=CARTESIAN_POINT ( 'NONE',  ( -2.395497655370999901, 30.70938692720000063, 0.5757869882262999228 ) ) ;
#7518=CARTESIAN_POINT ( 'NONE',  ( -2.186814738145873793, 24.16665839525370885, -1.278079063527637782 ) ) ;
#7521=FACE_OUTER_BOUND ( 'NONE', #17022, .T. ) ;
#7524=CIRCLE ( 'NONE', #10644, 0.5500000000000001554 ) ;
#7527=ORIENTED_CLOSED_SHELL ( 'NONE', *, #23556, .F. );
#7528=CARTESIAN_POINT ( 'NONE',  ( -0.6741018852137999895, 25.71212896666999725, -2.583184600869000036 ) ) ;
#7529=EDGE_LOOP ( 'NONE', ( #18559, #7901, #16211, #11593, #7854, #6173, #11289, #20673, #13904 ) ) ;
#7535=ORIENTED_EDGE ( 'NONE', *, *, #19989, .T. ) ;
#7542=CARTESIAN_POINT ( 'NONE',  ( 1.351857446083000180, 28.90405828138999667, -1.726400466208000140 ) ) ;
#7543=AXIS2_PLACEMENT_3D ( 'NONE', #12242, #3039, #23359 ) ;
#7546=CARTESIAN_POINT ( 'NONE',  ( 1.303752836300308804, 29.68620654978850482, 1.722188842540592457 ) ) ;
#7547=EDGE_LOOP ( 'NONE', ( #13442, #10504, #986, #13788 ) ) ;
#7548=CARTESIAN_POINT ( 'NONE',  ( -1.279456652065000144, 24.74056538345000078, 1.954075669677000082 ) ) ;
#7552=CARTESIAN_POINT ( 'NONE',  ( 2.384000448764866054, 30.27849728015833719, -0.8693082857020455467 ) ) ;
#7553=DIRECTION ( 'NONE',  ( 1.877655941804990996E-08, -0.9999999999999978906, -6.187284376306977451E-08 ) ) ;
#7554=ADVANCED_FACE ( 'NONE', ( #8751, #8879 ), #17596, .F. ) ;
#7559=CARTESIAN_POINT ( 'NONE',  ( 2.184465970885649977, 29.93333333333333002, 1.259047450927240686 ) ) ;
#7564=ADVANCED_FACE ( 'NONE', ( #12507 ), #3728, .T. ) ;
#7565=DIRECTION ( 'NONE',  ( 0.7071067811867457475, 0.7071067811863459562, -6.966834331432447605E-08 ) ) ;
#7568=CARTESIAN_POINT ( 'NONE',  ( -3.560623727957782148, 26.31534065533140421, -2.563075085697512634 ) ) ;
#7569=DIRECTION ( 'NONE',  ( 0.000000000000000000, 0.000000000000000000, -1.000000000000000000 ) ) ;
#7570=CARTESIAN_POINT ( 'NONE',  ( 0.6153010951426000075, 28.63250240009999814, -2.804372049896000085 ) ) ;
#7571=CARTESIAN_POINT ( 'NONE',  ( -0.6752522526669163527, 30.36340219175618671, 2.051621071677199648 ) ) ;
#7574=CARTESIAN_POINT ( 'NONE',  ( 1.659709954204918292, 24.76332575048712314, 1.345642078841861711 ) ) ;
#7578=CARTESIAN_POINT ( 'NONE',  ( -1.934529033667000020, 27.70696440325999887, 1.525059720042999833 ) ) ;
#7579=CARTESIAN_POINT ( 'NONE',  ( -2.123298534980464503, 30.87213863966240623, 0.1398201349483954581 ) ) ;
#7585=LINE ( 'NONE', #430, #17707 ) ;
#7586=CARTESIAN_POINT ( 'NONE',  ( 1.470238514176243960, 29.51959374728719609, 1.740011424867408119 ) ) ;
#7589=CIRCLE ( 'NONE', #11081, 4.649999999999999467 ) ;
#7590=CIRCLE ( 'NONE', #8776, 3.000000000000000000 ) ;
#7594=DIRECTION ( 'NONE',  ( 1.000000000000000000, 0.000000000000000000, 0.000000000000000000 ) ) ;
#7609=CARTESIAN_POINT ( 'NONE',  ( 1.816080815948163174, 29.07698660961091264, -1.174834969488964598 ) ) ;
#7613=CARTESIAN_POINT ( 'NONE',  ( 2.729128784747790970, 19.00000000000000000, 0.000000000000000000 ) ) ;
#7614=VERTEX_POINT ( 'NONE', #19535 ) ;
#7615=CARTESIAN_POINT ( 'NONE',  ( 2.072390219274999890, 24.98629352328999786, 1.114832866323000271 ) ) ;
#7617=CARTESIAN_POINT ( 'NONE',  ( 2.500000000000001776, 28.38333333333333997, 0.3272492347489265874 ) ) ;
#7618=CARTESIAN_POINT ( 'NONE',  ( 0.4658180156273000194, 28.71799822780999989, 2.070238309910999774 ) ) ;
#7619=DIRECTION ( 'NONE',  ( 0.000000000000000000, -1.000000000000000000, 0.000000000000000000 ) ) ;
#7620=EDGE_CURVE ( 'NONE', #14835, #18791, #14198, .T. ) ;
#7627=CARTESIAN_POINT ( 'NONE',  ( 0.000000000000000000, 18.50000000000000000, 0.000000000000000000 ) ) ;
#7634=ADVANCED_FACE ( 'NONE', ( #1362 ), #10345, .F. ) ;
#7635=CARTESIAN_POINT ( 'NONE',  ( -2.485790174642000139, 24.30225770961000009, 0.4464999199351999959 ) ) ;
#7640=CARTESIAN_POINT ( 'NONE',  ( -2.239268392087999882, 29.94342548081000288, 1.226391958772999891 ) ) ;
#7647=CARTESIAN_POINT ( 'NONE',  ( 1.236794719700695211, 24.50000548481460427, 2.172625763342098004 ) ) ;
#7650=AXIS2_PLACEMENT_3D ( 'NONE', #3095, #12050, #10226 ) ;
#7657=CARTESIAN_POINT ( 'NONE',  ( 0.000000000000000000, 15.04999987253367877, -4.699999872533999756 ) ) ;
#7658=CARTESIAN_POINT ( 'NONE',  ( -0.8328668639932000906, 28.33669433610000254, 2.747163055864000114 ) ) ;
#7661=CARTESIAN_POINT ( 'NONE',  ( 0.6543697108981985089, 27.20086340285667248, -2.434931691670790599 ) ) ;
#7671=CARTESIAN_POINT ( 'NONE',  ( -1.822202359507000047, 29.26374338476000148, 1.219654227816000081 ) ) ;
#7674=CARTESIAN_POINT ( 'NONE',  ( 1.439338077355937662, 29.69654873358969027, 1.610574062856036992 ) ) ;
#7676=CARTESIAN_POINT ( 'NONE',  ( 2.083478469512000331, 25.85240551230000250, -0.3289914792577999791 ) ) ;
#7677=LINE ( 'NONE', #23004, #17792 ) ;
#7678=DIRECTION ( 'NONE',  ( 0.000000000000000000, 0.000000000000000000, -1.000000000000000000 ) ) ;
#7680=VERTEX_POINT ( 'NONE', #14290 ) ;
#7691=LINE ( 'NONE', #16882, #11295 ) ;
#7696=CLOSED_SHELL ( 'NONE', ( #23822, #22265, #12472, #11317, #1230, #6444 ) ) ;
#7698=DIRECTION ( 'NONE',  ( 1.000000000000000000, 0.000000000000000000, 0.000000000000000000 ) ) ;
#7700=CARTESIAN_POINT ( 'NONE',  ( 1.678813317411953498, 26.50000000000001066, -3.649538832790644616 ) ) ;
#7701=DIRECTION ( 'NONE',  ( -1.000000000000000000, 0.000000000000000000, 0.000000000000000000 ) ) ;
#7702=EDGE_CURVE ( 'NONE', #23303, #17082, #11467, .T. ) ;
#7703=CARTESIAN_POINT ( 'NONE',  ( -0.1404717678206177378, 30.39552274579631685, 2.155312933377941498 ) ) ;
#7706=DIRECTION ( 'NONE',  ( 0.000000000000000000, 1.000000000000000000, 0.000000000000000000 ) ) ;
#7708=CARTESIAN_POINT ( 'NONE',  ( 2.184465970885649089, 27.76753006952332825, 1.259047450927240241 ) ) ;
#7709=CIRCLE ( 'NONE', #22416, 2.100000000000000089 ) ;
#7711=CARTESIAN_POINT ( 'NONE',  ( -0.2414528406811999872, 26.63446440325999731, -2.451511826319000331 ) ) ;
#7715=ORIENTED_EDGE ( 'NONE', *, *, #7761, .F. ) ;
#7721=CARTESIAN_POINT ( 'NONE',  ( -1.779764907139927077, 26.49975665830813298, 1.755621799651315262 ) ) ;
#7727=CARTESIAN_POINT ( 'NONE',  ( -0.6074916215089999350, 30.83999999999999986, -2.072813047478000215 ) ) ;
#7731=CARTESIAN_POINT ( 'NONE',  ( 4.000000000000000000, 24.80000000000000426, -2.309401076759000304 ) ) ;
#7739=CARTESIAN_POINT ( 'NONE',  ( -1.059324317249869862, 23.72850810831080537, 1.979001141744386016 ) ) ;
#7741=CARTESIAN_POINT ( 'NONE',  ( -0.5893288717795999165, 23.58034700824000041, -2.005185021572999826 ) ) ;
#7743=CARTESIAN_POINT ( 'NONE',  ( 2.169172474974999876, 25.72799822781000145, -0.6576354733792000307 ) ) ;
#7745=CARTESIAN_POINT ( 'NONE',  ( 0.000000000000000000, 24.49999999999999645, 0.000000000000000000 ) ) ;
#7749=CARTESIAN_POINT ( 'NONE',  ( 0.000000000000000000, 13.04999996922999905, 0.000000000000000000 ) ) ;
#7754=CARTESIAN_POINT ( 'NONE',  ( -1.025360869613999748, 24.32490530784000171, 2.515071452785000439 ) ) ;
#7758=ADVANCED_FACE ( 'NONE', ( #4851 ), #1083, .T. ) ;
#7759=CARTESIAN_POINT ( 'NONE',  ( -2.179821160686999715, 29.00990996801999700, -1.329187652093999805 ) ) ;
#7761=EDGE_CURVE ( 'NONE', #20998, #7342, #10310, .T. ) ;
#7763=CARTESIAN_POINT ( 'NONE',  ( 0.000000000000000000, 15.04999987253367877, 0.000000000000000000 ) ) ;
#7764=DIRECTION ( 'NONE',  ( -1.000000000000000000, 0.000000000000000000, 0.000000000000000000 ) ) ;
#7772=ORIENTED_EDGE ( 'NONE', *, *, #19152, .F. ) ;
#7774=AXIS2_PLACEMENT_3D ( 'NONE', #429, #4564, #9650 ) ;
#7775=CARTESIAN_POINT ( 'NONE',  ( 0.000000000000000000, 15.09999999999999964, 0.000000000000000000 ) ) ;
#7776=CARTESIAN_POINT ( 'NONE',  ( -2.656868203660999850, 27.46712896666999626, -0.2616786785207999566 ) ) ;
#7790=CARTESIAN_POINT ( 'NONE',  ( -2.192791562915999748, 30.85570112213000016, 0.6001452317431000827 ) ) ;
#7792=CARTESIAN_POINT ( 'NONE',  ( 0.4770046633850718032, 29.63206295647701438, 2.106562789758566367 ) ) ;
#7794=CARTESIAN_POINT ( 'NONE',  ( -1.286689466012000072, 24.54815262634000206, 1.965122128918000088 ) ) ;
#7805=DIRECTION ( 'NONE',  ( -0.7071067811865465735, -0.7071067811865465735, -5.144932280347337440E-08 ) ) ;
#7807=ORIENTED_EDGE ( 'NONE', *, *, #17535, .F. ) ;
#7815=CARTESIAN_POINT ( 'NONE',  ( -3.064125534931649852, 26.41068681084918879, -2.849728451093326065 ) ) ;
#7817=( NAMED_UNIT ( * ) SI_UNIT ( $, .STERADIAN. ) SOLID_ANGLE_UNIT ( ) );
#7818=CARTESIAN_POINT ( 'NONE',  ( 0.3272492347489341924, 28.01753006952333536, -2.500000000000000888 ) ) ;
#7820=CARTESIAN_POINT ( 'NONE',  ( 2.149588097096659656, 30.59149455840149656, 0.2106377642020627605 ) ) ;
#7826=CARTESIAN_POINT ( 'NONE',  ( -0.3375125786564999730, 27.80446440325999902, 2.440142399906000126 ) ) ;
#7829=ORIENTED_EDGE ( 'NONE', *, *, #14686, .T. ) ;
#7832=DIRECTION ( 'NONE',  ( 0.000000000000000000, 0.000000000000000000, -1.000000000000000000 ) ) ;
#7835=ORIENTED_EDGE ( 'NONE', *, *, #17108, .T. ) ;
#7838=CARTESIAN_POINT ( 'NONE',  ( 0.000000000000000000, 7.000000000000000000, -1.399999999999999911 ) ) ;
#7842=CARTESIAN_POINT ( 'NONE',  ( -1.938959741890676325, 30.88393747333224937, -0.8889222898575229737 ) ) ;
#7844=DIRECTION ( 'NONE',  ( 0.000000000000000000, -1.000000000000000000, 0.000000000000000000 ) ) ;
#7849=DIRECTION ( 'NONE',  ( 0.000000000000000000, 0.000000000000000000, -1.000000000000000000 ) ) ;
#7850=CARTESIAN_POINT ( 'NONE',  ( -1.812210406530999851, 27.25956776952000027, 1.960438172911999954 ) ) ;
#7852=CARTESIAN_POINT ( 'NONE',  ( 2.056388550342119981, 28.96414759127528171, 0.6606570080441251935 ) ) ;
#7854=ORIENTED_EDGE ( 'NONE', *, *, #14726, .T. ) ;
#7855=CARTESIAN_POINT ( 'NONE',  ( -4.750000000000000000, 24.29999999999999716, 0.000000000000000000 ) ) ;
#7856=ORIENTED_EDGE ( 'NONE', *, *, #2301, .F. ) ;
#7857=DIRECTION ( 'NONE',  ( 0.000000000000000000, 1.000000000000000000, 0.000000000000000000 ) ) ;
#7859=CARTESIAN_POINT ( 'NONE',  ( -1.538852087555999892, 26.99549822780999975, 1.664720809480999986 ) ) ;
#7861=CARTESIAN_POINT ( 'NONE',  ( -1.795213620510333064, 26.49800875556814006, 1.739922323311954511 ) ) ;
#7866=VECTOR ( 'NONE', #13112, 1000.000000000000227 ) ;
#7869=CARTESIAN_POINT ( 'NONE',  ( -1.109830502371000005, 31.11496756662999985, -2.398385042689000102 ) ) ;
#7870=CARTESIAN_POINT ( 'NONE',  ( -2.673271556775000057, 24.19682307903999785, 0.4801754984155000017 ) ) ;
#7875=CARTESIAN_POINT ( 'NONE',  ( -2.576169063563999551, 30.60395229662999839, 0.6192135579617999985 ) ) ;
#7878=DIRECTION ( 'NONE',  ( 1.000000000000000000, 0.000000000000000000, 0.000000000000000000 ) ) ;
#7886=CARTESIAN_POINT ( 'NONE',  ( -2.726577741920999998, 24.84881138680999868, -0.2402688989795999930 ) ) ;
#7887=DIRECTION ( 'NONE',  ( 0.000000000000000000, 1.000000000000000000, 0.000000000000000000 ) ) ;
#7888=CARTESIAN_POINT ( 'NONE',  ( -0.4887088349126519349, 23.97504838153446016, 2.138075895062909293 ) ) ;
#7894=CARTESIAN_POINT ( 'NONE',  ( -1.475897234648523293, 26.50000000000000711, 1.986511584949574249 ) ) ;
#7895=EDGE_LOOP ( 'NONE', ( #12462, #5780, #11445 ) ) ;
#7896=ORIENTED_EDGE ( 'NONE', *, *, #3908, .F. ) ;
#7900=DIRECTION ( 'NONE',  ( 1.000000000000000000, 0.000000000000000000, 0.000000000000000000 ) ) ;
#7901=ORIENTED_EDGE ( 'NONE', *, *, #4236, .F. ) ;
#7907=CARTESIAN_POINT ( 'NONE',  ( -2.040625142429000505, 30.82237883270000012, 0.5584987965637999707 ) ) ;
#7908=EDGE_CURVE ( 'NONE', #22927, #11959, #20367, .T. ) ;
#7910=B_SPLINE_CURVE_WITH_KNOTS ( 'NONE', 3,
 ( #19764, #12491, #23847, #3174, #1469, #8864, #5224, #17941 ),
 .UNSPECIFIED., .F., .F.,
 ( 4, 2, 2, 4 ),
 ( 0.000000000000000000, 0.2499999999999998890, 0.4999999999999997780, 1.000000000000000000 ),
 .UNSPECIFIED. ) ;
#7912=CARTESIAN_POINT ( 'NONE',  ( 0.2000898907656600834, 29.61553224063326795, 2.150689853480966196 ) ) ;
#7913=EDGE_LOOP ( 'NONE', ( #9057, #5565, #7401, #10798, #18391 ) ) ;
#7914=CARTESIAN_POINT ( 'NONE',  ( -0.2530461047814999698, 25.00341469540000006, -2.171193274693999697 ) ) ;
#7917=ORIENTED_EDGE ( 'NONE', *, *, #1582, .T. ) ;
#7918=CARTESIAN_POINT ( 'NONE',  ( -2.251894740644691417, 24.64810525581627587, -0.1522571951427112991 ) ) ;
#7921=EDGE_CURVE ( 'NONE', #3685, #20095, #2237, .T. ) ;
#7931=AXIS2_PLACEMENT_3D ( 'NONE', #21829, #15994, #12626 ) ;
#7932=CARTESIAN_POINT ( 'NONE',  ( 4.000000000000000000, 26.20000000000000284, 2.309401076759000304 ) ) ;
#7935=CARTESIAN_POINT ( 'NONE',  ( 0.000000000000000000, 20.10000000000000142, 0.000000000000000000 ) ) ;
#7942=CARTESIAN_POINT ( 'NONE',  ( 0.09195743698950356593, 30.40914314436703592, 2.158523876181588808 ) ) ;
#7948=CARTESIAN_POINT ( 'NONE',  ( -2.406140597653999791, 26.04946440326000001, 0.5279260092677999783 ) ) ;
#7949=AXIS2_PLACEMENT_3D ( 'NONE', #6050, #2424, #17078 ) ;
#7951=ORIENTED_EDGE ( 'NONE', *, *, #12545, .F. ) ;
#7953=CARTESIAN_POINT ( 'NONE',  ( 0.5271288625574210851, 26.26111511314614688, 2.095841999210956264 ) ) ;
#7954=CARTESIAN_POINT ( 'NONE',  ( 0.1848998096957392423, 27.84077103474808723, 2.192915077246018196 ) ) ;
#7959=CONICAL_SURFACE ( 'NONE', #2145, 4.699999872533999756, 0.7853981633972997312 ) ;
#7961=DIRECTION ( 'NONE',  ( 1.000000000000000000, 0.000000000000000000, 0.000000000000000000 ) ) ;
#7967=LINE ( 'NONE', #11609, #20476 ) ;
#7970=CARTESIAN_POINT ( 'NONE',  ( 2.844001364980000002, 26.87750240009999914, -0.3933730402103999824 ) ) ;
#7977=CYLINDRICAL_SURFACE ( 'NONE', #9147, 2.500000000000000000 ) ;
#7979=DIRECTION ( 'NONE',  ( -1.000000000000000000, 0.000000000000000000, 0.000000000000000000 ) ) ;
#7980=TOROIDAL_SURFACE ( 'NONE', #16098, 2.100000000000000089, 0.1000000000000000056 ) ;
#7988=CARTESIAN_POINT ( 'NONE',  ( 2.711127088422999876, 30.87230859155000218, -0.2628573326712999592 ) ) ;
#7989=CARTESIAN_POINT ( 'NONE',  ( 2.446868772696999983, 24.51702865104000040, 1.178890382843999829 ) ) ;
#7992=CARTESIAN_POINT ( 'NONE',  ( 2.000000000000000000, 18.89999999999999858, 0.000000000000000000 ) ) ;
#7993=CARTESIAN_POINT ( 'NONE',  ( -0.8857055135539000368, 28.33000425264999933, 2.448665480424999874 ) ) ;
#7996=AXIS2_PLACEMENT_3D ( 'NONE', #11210, #5744, #16873 ) ;
#7998=DIRECTION ( 'NONE',  ( -1.000000000000000000, 0.000000000000000000, 0.000000000000000000 ) ) ;
#8002=DIRECTION ( 'NONE',  ( 8.130136936064000824E-11, 0.000000000000000000, 1.000000000000000000 ) ) ;
#8003=EDGE_LOOP ( 'NONE', ( #23123, #6927, #17605, #16332, #21601, #7772 ) ) ;
#8004=CARTESIAN_POINT ( 'NONE',  ( 1.988422905474999780, 25.96353585921000118, 1.881031091488000184 ) ) ;
#8007=CARTESIAN_POINT ( 'NONE',  ( 3.099999776787000005, 15.00000022320933013, 5.570936504208000122E-07 ) ) ;
#8008=AXIS2_PLACEMENT_3D ( 'NONE', #16817, #7619, #2167 ) ;
#8011=CARTESIAN_POINT ( 'NONE',  ( -0.8020744510286262896, 26.50000000000000355, 2.262007200476410684 ) ) ;
#8012=EDGE_CURVE ( 'NONE', #19991, #11598, #19202, .T. ) ;
#8013=EDGE_LOOP ( 'NONE', ( #14873, #2175, #11610, #18404, #4697, #18295, #6940, #10054, #6830 ) ) ;
#8015=CIRCLE ( 'NONE', #21573, 2.270871215252209030 ) ;
#8022=DIRECTION ( 'NONE',  ( 0.000000000000000000, -1.000000000000000000, 0.000000000000000000 ) ) ;
#8027=AXIS2_PLACEMENT_3D ( 'NONE', #948, #1072, #6279 ) ;
#8029=EDGE_CURVE ( 'NONE', #4988, #11075, #7590, .T. ) ;
#8030=CARTESIAN_POINT ( 'NONE',  ( -0.01426998130716234520, 29.60301338715854058, 2.159908921319442232 ) ) ;
#8032=CARTESIAN_POINT ( 'NONE',  ( 0.6119580278259999506, 25.45552357783000019, 2.267762994067999749 ) ) ;
#8036=CARTESIAN_POINT ( 'NONE',  ( 0.4476285504030235729, 30.41139891206333346, -2.497755735888799400 ) ) ;
#8037=DIRECTION ( 'NONE',  ( 0.000000000000000000, -1.000000000000000000, 0.000000000000000000 ) ) ;
#8038=CARTESIAN_POINT ( 'NONE',  ( 1.699999999999999956, 9.063112730255063809, -0.9835110234548531949 ) ) ;
#8039=ADVANCED_FACE ( 'NONE', ( #897, #23420 ), #19445, .T. ) ;
#8042=ORIENTED_EDGE ( 'NONE', *, *, #20223, .T. ) ;
#8044=VECTOR ( 'NONE', #12837, 1000.000000000000000 ) ;
#8048=VERTEX_POINT ( 'NONE', #8661 ) ;
#8049=CARTESIAN_POINT ( 'NONE',  ( -1.799315205405667806, 24.70347107637078565, 1.274838228386613093 ) ) ;
#8059=DIRECTION ( 'NONE',  ( 1.000000000000000000, 0.000000000000000000, 0.000000000000000000 ) ) ;
#8062=CARTESIAN_POINT ( 'NONE',  ( 1.500000000000000000, 7.100000000000000533, 0.000000000000000000 ) ) ;
#8064=CARTESIAN_POINT ( 'NONE',  ( -0.02785460051843529836, 30.40211518515314282, 2.159877924567529028 ) ) ;
#8065=ORIENTED_EDGE ( 'NONE', *, *, #2225, .T. ) ;
#8070=DIRECTION ( 'NONE',  ( 0.000000000000000000, 0.000000000000000000, -1.000000000000000000 ) ) ;
#8071=CIRCLE ( 'NONE', #10411, 2.729128784747790970 ) ;
#8074=CARTESIAN_POINT ( 'NONE',  ( 0.000000000000000000, 24.49999999999999645, 0.000000000000000000 ) ) ;
#8075=VERTEX_POINT ( 'NONE', #9254 ) ;
#8078=ADVANCED_FACE ( 'NONE', ( #20277 ), #1458, .F. ) ;
#8079=CARTESIAN_POINT ( 'NONE',  ( 4.000000000000000000, 24.80000000000000426, 2.309401076759000304 ) ) ;
#8081=CONICAL_SURFACE ( 'NONE', #21627, 2.250000000000000000, 0.7853981633972997312 ) ;
#8082=CARTESIAN_POINT ( 'NONE',  ( -0.1005214697688198294, 28.23526083320289715, -2.196413288871530423 ) ) ;
#8090=PLANE ( 'NONE',  #3084 ) ;
#8092=CARTESIAN_POINT ( 'NONE',  ( -4.000000000000000000, 26.50000000000000355, 0.000000000000000000 ) ) ;
#8097=VERTEX_POINT ( 'NONE', #2826 ) ;
#8098=CARTESIAN_POINT ( 'NONE',  ( -4.000000000000000000, 24.80000000000000426, 2.309401076759000304 ) ) ;
#8099=CARTESIAN_POINT ( 'NONE',  ( 2.747163055864000114, 26.09750240010000155, -0.8328668639933000106 ) ) ;
#8100=AXIS2_PLACEMENT_3D ( 'NONE', #21800, #4735, #5215 ) ;
#8108=DIRECTION ( 'NONE',  ( -1.000000000000000000, 0.000000000000000000, 0.000000000000000000 ) ) ;
#8109=DIRECTION ( 'NONE',  ( 2.317847042770929243E-07, 0.9999999999999731326, 0.000000000000000000 ) ) ;
#8110=EDGE_CURVE ( 'NONE', #3493, #479, #7496, .T. ) ;
#8116=CIRCLE ( 'NONE', #3859, 4.000000000000000000 ) ;
#8122=CARTESIAN_POINT ( 'NONE',  ( -1.399447169867999996, 23.70324008177000152, 1.869294607855000123 ) ) ;
#8124=VERTEX_POINT ( 'NONE', #8154 ) ;
#8127=LINE ( 'NONE', #6415, #11935 ) ;
#8132=CARTESIAN_POINT ( 'NONE',  ( -0.3272492347489394104, 29.65086340285666466, -2.499999999999999112 ) ) ;
#8135=ORIENTED_EDGE ( 'NONE', *, *, #7439, .F. ) ;
#8136=CARTESIAN_POINT ( 'NONE',  ( 0.000000000000000000, 21.95000012746600149, 0.000000000000000000 ) ) ;
#8138=CARTESIAN_POINT ( 'NONE',  ( 1.440866150671271440, 24.31242210092122491, -1.654208956319656032 ) ) ;
#8141=CARTESIAN_POINT ( 'NONE',  ( -0.9779981048622099493, 26.50000000000000711, 2.217847022944143376 ) ) ;
#8154=CARTESIAN_POINT ( 'NONE',  ( 0.000000000000000000, 20.00000000000000000, -4.649999999999999467 ) ) ;
#8157=CARTESIAN_POINT ( 'NONE',  ( -1.918585267525981797, 29.34217026962017982, -1.008785855482386973 ) ) ;
#8158=EDGE_LOOP ( 'NONE', ( #15191, #18945, #11884, #2549, #22148, #5002 ) ) ;
#8159=CARTESIAN_POINT ( 'NONE',  ( -2.122260425170999998, 24.47835486083999967, 1.006620808079000007 ) ) ;
#8161=CIRCLE ( 'NONE', #10490, 1.000000000000000000 ) ;
#8164=CARTESIAN_POINT ( 'NONE',  ( 0.000000000000000000, 7.000000000000000000, 0.000000000000000000 ) ) ;
#8165=CARTESIAN_POINT ( 'NONE',  ( 3.050000000000000266, 18.50000000000000000, 0.000000000000000000 ) ) ;
#8169=CARTESIAN_POINT ( 'NONE',  ( -0.6543697108982037269, 27.03333333333333499, -2.434931691670788823 ) ) ;
#8171=EDGE_CURVE ( 'NONE', #10966, #8048, #17723, .T. ) ;
#8172=ORIENTED_EDGE ( 'NONE', *, *, #23537, .F. ) ;
#8174=DIRECTION ( 'NONE',  ( 0.000000000000000000, -1.000000000000000000, 0.000000000000000000 ) ) ;
#8181=CARTESIAN_POINT ( 'NONE',  ( 0.000000000000000000, 20.00000000000000000, 0.000000000000000000 ) ) ;
#8183=CARTESIAN_POINT ( 'NONE',  ( 0.000000000000000000, 24.29999999999999716, 0.000000000000000000 ) ) ;
#8185=CARTESIAN_POINT ( 'NONE',  ( -2.159897835357240226, 30.20132937181709565, -0.03950432281413149282 ) ) ;
#8193=ORIENTED_EDGE ( 'NONE', *, *, #14930, .F. ) ;
#8198=CARTESIAN_POINT ( 'NONE',  ( 1.977975842973895393, 28.08732715878234387, -0.9681838510627849281 ) ) ;
#8201=ADVANCED_FACE ( 'NONE', ( #6571 ), #1794, .T. ) ;
#8209=CARTESIAN_POINT ( 'NONE',  ( 2.100000000000000089, 19.00000000000000000, 0.000000000000000000 ) ) ;
#8214=ORIENTED_EDGE ( 'NONE', *, *, #6136, .T. ) ;
#8216=CARTESIAN_POINT ( 'NONE',  ( -2.096579189799000265, 28.03956776952000141, 1.652809762273000027 ) ) ;
#8219=CARTESIAN_POINT ( 'NONE',  ( 2.085423526801265748, 28.97009402253615917, 0.5636491508442302845 ) ) ;
#8220=CARTESIAN_POINT ( 'NONE',  ( 0.04809324771324000047, 27.21687716035999927, 2.449054215377000077 ) ) ;
#8222=ORIENTED_EDGE ( 'NONE', *, *, #2389, .T. ) ;
#8224=CARTESIAN_POINT ( 'NONE',  ( 0.5551539414043799026, 26.26248452079970619, 2.089084675604010233 ) ) ;
#8225=DIRECTION ( 'NONE',  ( 0.000000000000000000, 1.000000000000000000, 0.000000000000000000 ) ) ;
#8228=EDGE_CURVE ( 'NONE', #11130, #13776, #15761, .T. ) ;
#8231=CIRCLE ( 'NONE', #109, 2.099999992707999308 ) ;
#8233=CARTESIAN_POINT ( 'NONE',  ( 2.434931691670791931, 27.56666666666666643, 0.6543697108981911814 ) ) ;
#8239=ORIENTED_EDGE ( 'NONE', *, *, #22821, .F. ) ;
#8246=CARTESIAN_POINT ( 'NONE',  ( 0.000000000000000000, 18.00000000000000000, 0.000000000000000000 ) ) ;
#8247=CARTESIAN_POINT ( 'NONE',  ( 2.500000000000000000, 29.43419673618999965, 0.000000000000000000 ) ) ;
#8249=DIRECTION ( 'NONE',  ( 0.000000000000000000, 1.000000000000000000, 0.000000000000000000 ) ) ;
#8250=CARTESIAN_POINT ( 'NONE',  ( -1.258584843124999963, 24.77728268470999851, 1.988370622766999940 ) ) ;
#8251=CARTESIAN_POINT ( 'NONE',  ( 1.142577977447108317, 24.50000000000001066, -2.156693640880154472 ) ) ;
#8254=FACE_OUTER_BOUND ( 'NONE', #2787, .T. ) ;
#8255=CARTESIAN_POINT ( 'NONE',  ( 0.6543697108982239330, 28.46753006952333109, 2.434931691670783049 ) ) ;
#8258=FACE_BOUND ( 'NONE', #4632, .T. ) ;
#8261=ORIENTED_EDGE ( 'NONE', *, *, #18126, .T. ) ;
#8263=B_SPLINE_CURVE_WITH_KNOTS ( 'NONE', 3,
 ( #10498, #21275, #1284, #4684, #21633, #4923, #15916, #5052, #12308, #8669, #17998, #19454, #2982, #16036, #1403, #22944, #3351, #14812, #23907, #3576, #16283, #3688, #12664, #7084, #14360, #18463, #20403, #21866, #12779, #8917, #1528, #23788, #9142, #7196, #16638, #3809, #9262, #1875, #14586, #47, #7315 ),
 .UNSPECIFIED., .F., .F.,
 ( 4, 2, 2, 2, 2, 1, 1, 1, 2, 2, 2, 2, 1, 2, 2, 2, 1, 2, 2, 2, 2, 2, 4 ),
 ( 0.000000000000000000, 0.1249999999999944489, 0.2499999999999888978, 0.3749999999999833467, 0.4374999999999805156, 0.4687499999999791278, 0.4843749999999784617, 0.4921874999999780731, 0.4960937499999777955, 0.4999999999999775180, 0.6249999999999618083, 0.6874999999999540368, 0.7187499999999502620, 0.7343749999999485967, 0.7499999999999470424, 0.8124999999999422684, 0.8437499999999414912, 0.8593749999999420464, 0.8749999999999427125, 0.9062499999999577005, 0.9218749999999646949, 0.9374999999999718003, 1.000000000000000000 ),
 .UNSPECIFIED. ) ;
#8265=CARTESIAN_POINT ( 'NONE',  ( 3.099999776787000005, 16.99999977679100027, 5.570936506502000395E-07 ) ) ;
#8268=CARTESIAN_POINT ( 'NONE',  ( 1.717851791802367689, 12.95712093925186181, -1.058657081467656802 ) ) ;
#8272=CARTESIAN_POINT ( 'NONE',  ( 1.346439123301719665, 24.53198827073828170, 3.841100253455552060 ) ) ;
#8275=CARTESIAN_POINT ( 'NONE',  ( 0.000000000000000000, 24.49999999999999645, 0.000000000000000000 ) ) ;
#8276=CONICAL_SURFACE ( 'NONE', #15597, 4.309401076758999416, 1.119376321708719590 ) ;
#8277=CARTESIAN_POINT ( 'NONE',  ( -0.7226321071931195439, 29.56039541046514074, 2.038962400747685866 ) ) ;
#8278=VERTEX_POINT ( 'NONE', #12399 ) ;
#8279=CARTESIAN_POINT ( 'NONE',  ( 1.160309977445999952, 24.68774815733999972, 2.042291732285999917 ) ) ;
#8295=FACE_OUTER_BOUND ( 'NONE', #23383, .T. ) ;
#8296=CARTESIAN_POINT ( 'NONE',  ( 4.000000000000000888, 26.50000000000000711, 0.1857058784358716907 ) ) ;
#8301=CARTESIAN_POINT ( 'NONE',  ( -0.8020744510286262896, 26.50000000000000355, 2.262007200476410684 ) ) ;
#8303=CARTESIAN_POINT ( 'NONE',  ( 0.000000000000000000, 24.65000000000000213, 0.000000000000000000 ) ) ;
#8304=CARTESIAN_POINT ( 'NONE',  ( -1.585299566500308455, 30.10873184028566740, -1.466893546891119948 ) ) ;
#8305=VERTEX_POINT ( 'NONE', #12511 ) ;
#8315=CARTESIAN_POINT ( 'NONE',  ( 0.000000000000000000, 9.100092063578999912, 0.000000000000000000 ) ) ;
#8316=CARTESIAN_POINT ( 'NONE',  ( 0.1384749747861074853, 27.42162562388985947, -2.167302550213716206 ) ) ;
#8319=ADVANCED_FACE ( 'NONE', ( #5472 ), #21763, .F. ) ;
#8320=EDGE_LOOP ( 'NONE', ( #5118, #8261, #1999, #16284 ) ) ;
#8327=CARTESIAN_POINT ( 'NONE',  ( -1.281400481305768446, 28.72500111167598291, 1.780029602772844166 ) ) ;
#8332=CARTESIAN_POINT ( 'NONE',  ( -0.7249434865795999494, 26.29250240010000184, -2.778011591584000239 ) ) ;
#8339=EDGE_LOOP ( 'NONE', ( #14248, #16203, #23662, #189, #17166, #8065, #10703 ) ) ;
#8344=CARTESIAN_POINT ( 'NONE',  ( 2.749999993363999806, 22.20000000663619844, -7.185653629187000299E-09 ) ) ;
#8346=ADVANCED_FACE ( 'NONE', ( #11639 ), #22358, .T. ) ;
#8347=CARTESIAN_POINT ( 'NONE',  ( 2.500000000000000000, 27.03419673618999752, 0.000000000000000000 ) ) ;
#8352=EDGE_LOOP ( 'NONE', ( #14725, #22676, #7404, #18129 ) ) ;
#8354=CARTESIAN_POINT ( 'NONE',  ( -1.013429452669000197, 30.50215507907999779, 2.321226178608000179 ) ) ;
#8355=DIRECTION ( 'NONE',  ( 1.000000000000000000, 0.000000000000000000, 0.000000000000000000 ) ) ;
#8358=EDGE_CURVE ( 'NONE', #20706, #13184, #8127, .T. ) ;
#8360=FACE_OUTER_BOUND ( 'NONE', #23175, .T. ) ;
#8365=LINE ( 'NONE', #6546, #6141 ) ;
#8366=ADVANCED_FACE ( 'NONE', ( #20956 ), #6656, .F. ) ;
#8370=ADVANCED_FACE ( 'NONE', ( #15367 ), #1500, .T. ) ;
#8371=AXIS2_PLACEMENT_3D ( 'NONE', #3263, #18034, #19491 ) ;
#8374=VERTEX_POINT ( 'NONE', #11755 ) ;
#8375=CARTESIAN_POINT ( 'NONE',  ( 2.676712279640000247, 26.03320613874000244, 0.5717015712084999590 ) ) ;
#8376=CARTESIAN_POINT ( 'NONE',  ( -1.764527535379162293, 23.88508205627838521, 1.302939369652649448 ) ) ;
#8385=DIRECTION ( 'NONE',  ( 0.000000000000000000, -1.000000000000000000, 0.000000000000000000 ) ) ;
#8390=DIRECTION ( 'NONE',  ( 0.000000000000000000, 1.000000000000000000, 0.000000000000000000 ) ) ;
#8399=CARTESIAN_POINT ( 'NONE',  ( -2.058542572094083756, 29.36339098118925151, -0.6772705394161806502 ) ) ;
#8402=CARTESIAN_POINT ( 'NONE',  ( -0.9500571175814802594, 24.08332894998783758, -2.348467497242777480 ) ) ;
#8405=EDGE_LOOP ( 'NONE', ( #12364, #14935, #8602, #10044 ) ) ;
#8406=CARTESIAN_POINT ( 'NONE',  ( 2.000000000000000000, 23.50000000000000000, 0.000000000000000000 ) ) ;
#8409=VECTOR ( 'NONE', #9207, 1000.000000000000114 ) ;
#8412=VERTEX_POINT ( 'NONE', #4484 ) ;
#8413=CARTESIAN_POINT ( 'NONE',  ( 2.053005267516999902E-14, 28.63049582772000079, 2.160000000000000142 ) ) ;
#8414=CARTESIAN_POINT ( 'NONE',  ( 1.536366799937286087, 26.91666666666666785, -1.999167105995451665 ) ) ;
#8417=CARTESIAN_POINT ( 'NONE',  ( -2.239152124149412781, 24.66084788045843723, 0.1975086853543606968 ) ) ;
#8420=CARTESIAN_POINT ( 'NONE',  ( -3.643546194520564274, 26.29977277844447414, 2.515199777306226903 ) ) ;
#8423=CARTESIAN_POINT ( 'NONE',  ( 0.000000000000000000, 24.29999999999999716, 0.000000000000000000 ) ) ;
#8426=DIRECTION ( 'NONE',  ( 0.000000000000000000, 1.000000000000000000, 0.000000000000000000 ) ) ;
#8427=CARTESIAN_POINT ( 'NONE',  ( 2.000000000000000000, 26.50000000000000355, 3.464101615137999968 ) ) ;
#8429=CARTESIAN_POINT ( 'NONE',  ( -2.134590991208236144, 30.18387669342094526, -0.3366029040113500681 ) ) ;
#8433=DIRECTION ( 'NONE',  ( 0.000000000000000000, 1.000000000000000000, 0.000000000000000000 ) ) ;
#8434=DIRECTION ( 'NONE',  ( 0.000000000000000000, 1.000000000000000000, 0.000000000000000000 ) ) ;
#8440=ORIENTED_EDGE ( 'NONE', *, *, #3775, .T. ) ;
#8443=CARTESIAN_POINT ( 'NONE',  ( -2.157336997581982274, 26.80523531380421787, -0.4247655906842845441 ) ) ;
#8444=CONICAL_SURFACE ( 'NONE', #19672, 4.309401076758999416, 1.119376321708719590 ) ;
#8454=CARTESIAN_POINT ( 'NONE',  ( 1.578394010650965962, 28.30098268268568162, -1.492322616203947572 ) ) ;
#8455=AXIS2_PLACEMENT_3D ( 'NONE', #13477, #20525, #7678 ) ;
#8460=CARTESIAN_POINT ( 'NONE',  ( -1.184521108792000010, 28.41369850838000133, -1.932944458086000017 ) ) ;
#8462=AXIS2_PLACEMENT_3D ( 'NONE', #1900, #5530, #6993 ) ;
#8466=CIRCLE ( 'NONE', #22363, 1.000000000000000000 ) ;
#8467=ORIENTED_EDGE ( 'NONE', *, *, #19152, .T. ) ;
#8471=CARTESIAN_POINT ( 'NONE',  ( 0.5931794701136839931, 30.59672703127345272, -2.199405972370846563 ) ) ;
#8476=CARTESIAN_POINT ( 'NONE',  ( -1.259047450927242462, 27.33333333333333925, 2.184465970885648201 ) ) ;
#8477=CIRCLE ( 'NONE', #1519, 2.500000000000000000 ) ;
#8481=CARTESIAN_POINT ( 'NONE',  ( -0.9369953447464000051, 30.39672044851000265, 2.146156417431999586 ) ) ;
#8483=CARTESIAN_POINT ( 'NONE',  ( -2.000000000000000000, 24.50000000000000000, 3.464101615137999968 ) ) ;
#8484=AXIS2_PLACEMENT_3D ( 'NONE', #22634, #6413, #9809 ) ;
#8487=DIRECTION ( 'NONE',  ( 0.000000000000000000, 1.000000000000000000, 0.000000000000000000 ) ) ;
#8488=CARTESIAN_POINT ( 'NONE',  ( -1.135623862809999940, 29.11990199424000281, 2.499808603183999889 ) ) ;
#8491=CARTESIAN_POINT ( 'NONE',  ( -2.653270836322015214, 24.53198827073824617, 3.086600612158310941 ) ) ;
#8492=AXIS2_PLACEMENT_3D ( 'NONE', #17081, #19134, #7764 ) ;
#8494=ADVANCED_FACE ( 'NONE', ( #64 ), #8444, .T. ) ;
#8495=LINE ( 'NONE', #12488, #17777 ) ;
#8496=ORIENTED_EDGE ( 'NONE', *, *, #1089, .F. ) ;
#8499=VERTEX_POINT ( 'NONE', #19632 ) ;
#8500=AXIS2_PLACEMENT_3D ( 'NONE', #20313, #3719, #18965 ) ;
#8501=CARTESIAN_POINT ( 'NONE',  ( -1.583728643957000193, 25.44007955149000111, -1.992425406035000179 ) ) ;
#8507=CONICAL_SURFACE ( 'NONE', #16610, 4.699999872533999756, 0.7853981633972997312 ) ;
#8509=LINE ( 'NONE', #23259, #12873 ) ;
#8510=ORIENTED_EDGE ( 'NONE', *, *, #4184, .T. ) ;
#8511=CARTESIAN_POINT ( 'NONE',  ( 0.3272492347489454056, 30.05086340285667745, 2.499999999999998668 ) ) ;
#8514=CARTESIAN_POINT ( 'NONE',  ( 0.000000000000000000, 8.900000000000000355, 0.000000000000000000 ) ) ;
#8515=EDGE_CURVE ( 'NONE', #21280, #15589, #12368, .T. ) ;
#8516=ORIENTED_EDGE ( 'NONE', *, *, #12622, .F. ) ;
#8521=FACE_OUTER_BOUND ( 'NONE', #19628, .T. ) ;
#8527=CARTESIAN_POINT ( 'NONE',  ( -2.053677740305431598, 29.44401705994312479, 0.6690189489189264371 ) ) ;
#8530=CARTESIAN_POINT ( 'NONE',  ( 2.434931691670788823, 29.23333333333333073, -0.6543697108982009514 ) ) ;
#8533=VERTEX_POINT ( 'NONE', #18606 ) ;
#8538=EDGE_LOOP ( 'NONE', ( #13973, #5017, #10352, #7142 ) ) ;
#8541=DIRECTION ( 'NONE',  ( 0.000000000000000000, 1.000000000000000000, 0.000000000000000000 ) ) ;
#8550=DIRECTION ( 'NONE',  ( 1.000000000000000000, 0.000000000000000000, 0.000000000000000000 ) ) ;
#8553=CARTESIAN_POINT ( 'NONE',  ( -1.143039311806165026, 30.33272233741166701, 1.832923158551177822 ) ) ;
#8554=ADVANCED_FACE ( 'NONE', ( #17819 ), #9990, .T. ) ;
#8559=ORIENTED_EDGE ( 'NONE', *, *, #10443, .T. ) ;
#8566=CARTESIAN_POINT ( 'NONE',  ( -1.815862101691702479, 26.75592408899736085, -1.190014743604365322 ) ) ;
#8571=CARTESIAN_POINT ( 'NONE',  ( 1.699986222664000124, 9.100024384209000061, 1.053575639828000066 ) ) ;
#8576=FACE_OUTER_BOUND ( 'NONE', #21775, .T. ) ;
#8579=ORIENTED_EDGE ( 'NONE', *, *, #9772, .T. ) ;
#8580=CARTESIAN_POINT ( 'NONE',  ( -1.182434930542718865, 26.44682129341586574, -3.936123028068912344 ) ) ;
#8582=CARTESIAN_POINT ( 'NONE',  ( 2.254114612530000006, 25.82163313895000201, 0.5071914623444000458 ) ) ;
#8584=CARTESIAN_POINT ( 'NONE',  ( 0.5033195914047999819, 28.84187716036000282, 2.236906829057999868 ) ) ;
#8589=FACE_OUTER_BOUND ( 'NONE', #4960, .T. ) ;
#8592=CARTESIAN_POINT ( 'NONE',  ( -0.3272492347488898945, 24.18333333333333357, 2.500000000000005329 ) ) ;
#8595=CARTESIAN_POINT ( 'NONE',  ( 2.500000000000000000, 27.59999999999999787, 0.000000000000000000 ) ) ;
#8599=CARTESIAN_POINT ( 'NONE',  ( -2.554677365147000057, 29.61489390254000043, -0.9449442378532999509 ) ) ;
#8602=ORIENTED_EDGE ( 'NONE', *, *, #16321, .F. ) ;
#8603=CARTESIAN_POINT ( 'NONE',  ( -0.3380190453170119902, 26.50000000000001421, -2.400617273097169768 ) ) ;
#8604=CARTESIAN_POINT ( 'NONE',  ( 0.000000000000000000, 19.04999994433000055, 0.000000000000000000 ) ) ;
#8612=FACE_OUTER_BOUND ( 'NONE', #570, .T. ) ;
#8616=CARTESIAN_POINT ( 'NONE',  ( 2.488989593372999742, 25.92777150816999665, 0.5316071032648000960 ) ) ;
#8622=ORIENTED_EDGE ( 'NONE', *, *, #12608, .T. ) ;
#8624=CARTESIAN_POINT ( 'NONE',  ( -1.970034741582993298, 26.25401323305582935, 0.8711804643216717325 ) ) ;
#8632=CARTESIAN_POINT ( 'NONE',  ( 0.1261743698658000234, 30.29791251314999911, 2.164316091856000046 ) ) ;
#8635=ORIENTED_EDGE ( 'NONE', *, *, #381, .T. ) ;
#8638=CARTESIAN_POINT ( 'NONE',  ( -0.09735432568101735906, 29.20954443492663444, -2.161772490294577853 ) ) ;
#8640=DIRECTION ( 'NONE',  ( -0.000000000000000000, 1.000000000000000000, 0.000000000000000000 ) ) ;
#8643=EDGE_CURVE ( 'NONE', #4710, #9272, #19665, .T. ) ;
#8644=CARTESIAN_POINT ( 'NONE',  ( 0.5756525555721964116, 30.79585480968119171, -2.147306472175536385 ) ) ;
#8647=CARTESIAN_POINT ( 'NONE',  ( 0.1453149127350999992, 27.37756359724000177, -2.464088664829000130 ) ) ;
#8652=DIRECTION ( 'NONE',  ( 0.000000000000000000, 0.000000000000000000, -1.000000000000000000 ) ) ;
#8653=ORIENTED_EDGE ( 'NONE', *, *, #4552, .T. ) ;
#8654=EDGE_CURVE ( 'NONE', #18916, #5087, #14461, .T. ) ;
#8659=BREP_WITH_VOIDS ( 'NONE', #10812, ( #16553, #414, #21897, #7527, #855 ) );
#8661=CARTESIAN_POINT ( 'NONE',  ( -4.750000000000000000, 16.89999999999999858, 0.000000000000000000 ) ) ;
#8662=CARTESIAN_POINT ( 'NONE',  ( 0.3564538054804341494, 26.29977277844468020, 4.413003452969197049 ) ) ;
#8664=CARTESIAN_POINT ( 'NONE',  ( -1.587703551898336896, 30.10893883470173904, -1.464285708681415388 ) ) ;
#8666=CARTESIAN_POINT ( 'NONE',  ( 0.9782764959233999358, 25.15935197643999999, -2.120942277036999890 ) ) ;
#8669=CARTESIAN_POINT ( 'NONE',  ( -1.310299540072302538, 23.61517381211949029, -1.660816364045096583 ) ) ;
#8673=CARTESIAN_POINT ( 'NONE',  ( 0.000000000000000000, 16.95000012746599793, -4.699999872533999756 ) ) ;
#8675=ADVANCED_FACE ( 'NONE', ( #11943 ), #19327, .T. ) ;
#8676=DIRECTION ( 'NONE',  ( -1.000000000000000000, 0.000000000000000000, 0.000000000000000000 ) ) ;
#8679=DIRECTION ( 'NONE',  ( 1.000000000000000000, 0.000000000000000000, 0.000000000000000000 ) ) ;
#8681=ORIENTED_EDGE ( 'NONE', *, *, #9828, .T. ) ;
#8682=CARTESIAN_POINT ( 'NONE',  ( 0.9584783449968901081, 26.28746745333229029, 1.979923197800155688 ) ) ;
#8685=EDGE_CURVE ( 'NONE', #8374, #14961, #2618, .T. ) ;
#8689=B_SPLINE_CURVE_WITH_KNOTS ( 'NONE', 3,
 ( #3705, #533, #7568, #15187, #14947, #7815, #295, #15071, #9285, #22465 ),
 .UNSPECIFIED., .F., .F.,
 ( 4, 1, 1, 2, 2, 4 ),
 ( 0.000000000000000000, 0.2499999999999987788, 0.3749999999999986122, 0.4374999999999987232, 0.4999999999999988898, 1.000000000000000000 ),
 .UNSPECIFIED. ) ;
#8694=CARTESIAN_POINT ( 'NONE',  ( -2.173007427726788343, 27.00242624193079521, -0.03385292825698651975 ) ) ;
#8696=DIRECTION ( 'NONE',  ( 0.000000000000000000, 0.000000000000000000, -1.000000000000000000 ) ) ;
#8697=ORIENTED_EDGE ( 'NONE', *, *, #13248, .T. ) ;
#8700=CARTESIAN_POINT ( 'NONE',  ( 2.231710853292999897, 28.12119850838000090, 0.3985328791175999918 ) ) ;
#8701=LINE ( 'NONE', #23463, #18891 ) ;
#8706=EDGE_LOOP ( 'NONE', ( #488, #8042, #8510, #6533 ) ) ;
#8707=DIRECTION ( 'NONE',  ( 1.000000000000000000, 0.000000000000000000, 0.000000000000000000 ) ) ;
#8711=CARTESIAN_POINT ( 'NONE',  ( 0.000000000000000000, 22.00000000000000000, 0.000000000000000000 ) ) ;
#8712=ORIENTED_EDGE ( 'NONE', *, *, #3218, .T. ) ;
#8718=EDGE_LOOP ( 'NONE', ( #1232, #1871, #16398 ) ) ;
#8720=CARTESIAN_POINT ( 'NONE',  ( 2.395043234180000091, 29.11238094911999852, 0.8239347788672000128 ) ) ;
#8723=VECTOR ( 'NONE', #3163, 1000.000000000000000 ) ;
#8726=CARTESIAN_POINT ( 'NONE',  ( -0.8905775397556899842, 26.49999999999999289, -2.306335956037367296 ) ) ;
#8727=LINE ( 'NONE', #10299, #16609 ) ;
#8732=DIRECTION ( 'NONE',  ( 1.877655941804990996E-08, -0.9999999999999978906, -6.187284376306977451E-08 ) ) ;
#8736=CARTESIAN_POINT ( 'NONE',  ( -0.003072356603141344206, 30.56339746047213524, 2.483727271772852241 ) ) ;
#8739=CARTESIAN_POINT ( 'NONE',  ( -0.8094216628179000672, 24.22177887107999794, 2.614725727772000408 ) ) ;
#8742=CIRCLE ( 'NONE', #7949, 4.724999999999999645 ) ;
#8745=ORIENTED_EDGE ( 'NONE', *, *, #19470, .T. ) ;
#8751=FACE_BOUND ( 'NONE', #15977, .T. ) ;
#8756=CARTESIAN_POINT ( 'NONE',  ( -1.812968411601999952, 29.36439700036000033, 1.188835414341000041 ) ) ;
#8760=CIRCLE ( 'NONE', #6812, 1.999999999999998668 ) ;
#8764=CARTESIAN_POINT ( 'NONE',  ( 2.500000000000000000, 29.19999999999999929, 0.000000000000000000 ) ) ;
#8765=CARTESIAN_POINT ( 'NONE',  ( 0.000000000000000000, 20.10000000000000142, -4.750000000000305533 ) ) ;
#8767=CYLINDRICAL_SURFACE ( 'NONE', #20366, 2.500000000000000000 ) ;
#8772=CARTESIAN_POINT ( 'NONE',  ( -1.675531247043999805, 26.89006359724000106, 1.812579491195999815 ) ) ;
#8776=AXIS2_PLACEMENT_3D ( 'NONE', #3105, #21263, #8550 ) ;
#8779=ORIENTED_EDGE ( 'NONE', *, *, #19913, .T. ) ;
#8780=DIRECTION ( 'NONE',  ( 1.000000000000000000, 0.000000000000000000, 0.000000000000000000 ) ) ;
#8787=CARTESIAN_POINT ( 'NONE',  ( -1.795619090332999823, 30.15525342005999576, -1.250754954668999996 ) ) ;
#8791=CARTESIAN_POINT ( 'NONE',  ( 1.636241036409593397, 29.89441029013897122, -1.410665930300490478 ) ) ;
#8792=VERTEX_POINT ( 'NONE', #12034 ) ;
#8796=AXIS2_PLACEMENT_3D ( 'NONE', #16585, #3878, #11271 ) ;
#8797=DIRECTION ( 'NONE',  ( 1.000000000000000000, 0.000000000000000000, 0.000000000000000000 ) ) ;
#8799=DIRECTION ( 'NONE',  ( 0.5000000000000169864, 0.000000000000000000, -0.8660254037844289376 ) ) ;
#8801=EDGE_CURVE ( 'NONE', #15589, #2559, #14876, .T. ) ;
#8803=EDGE_LOOP ( 'NONE', ( #18470, #5170, #23576, #1404 ) ) ;
#8807=CARTESIAN_POINT ( 'NONE',  ( 0.7852232940904583236, 27.07644705024190657, 2.043071344251131460 ) ) ;
#8809=ADVANCED_FACE ( 'NONE', ( #6575, #17603 ), #13958, .T. ) ;
#8812=VERTEX_POINT ( 'NONE', #10209 ) ;
#8818=EDGE_CURVE ( 'NONE', #16646, #13895, #3310, .T. ) ;
#8823=CARTESIAN_POINT ( 'NONE',  ( 1.475904072323096727, 26.71091357114880083, -1.643089912458857826 ) ) ;
#8825=CARTESIAN_POINT ( 'NONE',  ( 1.739122139606305906, 30.68463495477586989, -1.280904342922043693 ) ) ;
#8828=CARTESIAN_POINT ( 'NONE',  ( -1.723852419406000092, 26.85369850837999905, -1.472309056329999866 ) ) ;
#8829=CONICAL_SURFACE ( 'NONE', #15765, 2.949999959913000236, 0.7853981633972997312 ) ;
#8832=CARTESIAN_POINT ( 'NONE',  ( 1.848781781241999989, 25.77271896306000443, 0.9420013681046000009 ) ) ;
#8833=EDGE_CURVE ( 'NONE', #7342, #16380, #20677, .T. ) ;
#8841=CARTESIAN_POINT ( 'NONE',  ( -2.153985071724999756, 30.83999999999999986, 0.1610847937796999751 ) ) ;
#8842=DIRECTION ( 'NONE',  ( 1.000000000000000000, 0.000000000000000000, 0.000000000000000000 ) ) ;
#8845=VERTEX_POINT ( 'NONE', #17350 ) ;
#8846=CARTESIAN_POINT ( 'NONE',  ( -1.259047450927251566, 28.66666666666666430, -2.184465970885643316 ) ) ;
#8847=CARTESIAN_POINT ( 'NONE',  ( -0.9541616508540999853, 30.90409830547999803, -2.061978857876999971 ) ) ;
#8849=CARTESIAN_POINT ( 'NONE',  ( 2.500000000000000000, 30.00000000000000000, 0.000000000000000000 ) ) ;
#8852=AXIS2_PLACEMENT_3D ( 'NONE', #23028, #624, #19290 ) ;
#8855=CARTESIAN_POINT ( 'NONE',  ( 0.5294722038327828173, 24.50879627117540238, -2.335604389998253261 ) ) ;
#8861=ORIENTED_EDGE ( 'NONE', *, *, #4172, .F. ) ;
#8863=DIRECTION ( 'NONE',  ( 0.000000000000000000, 1.000000000000000000, 0.000000000000000000 ) ) ;
#8864=CARTESIAN_POINT ( 'NONE',  ( 1.350644574821315613, 24.52555747447237877, -3.839035148326051861 ) ) ;
#8866=ORIENTED_EDGE ( 'NONE', *, *, #19783, .F. ) ;
#8870=CARTESIAN_POINT ( 'NONE',  ( -2.500000000000000000, 28.00000000000000000, 0.000000000000000000 ) ) ;
#8875=CARTESIAN_POINT ( 'NONE',  ( 1.699999999999999956, 9.000014497636620092, -0.2828405775381332421 ) ) ;
#8879=FACE_OUTER_BOUND ( 'NONE', #7462, .T. ) ;
#8883=CARTESIAN_POINT ( 'NONE',  ( 0.2266750768320999754, 29.07716145795999907, -2.156108152400999955 ) ) ;
#8886=ORIENTED_EDGE ( 'NONE', *, *, #17835, .T. ) ;
#8890=CARTESIAN_POINT ( 'NONE',  ( -1.999167105995452998, 29.51666666666667282, -1.536366799937284089 ) ) ;
#8892=CONICAL_SURFACE ( 'NONE', #23957, 2.197442471388999952, 0.7853981633972997312 ) ;
#8898=ADVANCED_FACE ( 'NONE', ( #10337 ), #13318, .T. ) ;
#8903=AXIS2_PLACEMENT_3D ( 'NONE', #4131, #20608, #2191 ) ;
#8908=CARTESIAN_POINT ( 'NONE',  ( 2.142501703538999713, 30.65881256477999983, -0.4453337693464999858 ) ) ;
#8909=CIRCLE ( 'NONE', #19751, 3.000000000000000000 ) ;
#8910=PRODUCT_DEFINITION_CONTEXT ( 'detailed design', #23342, 'design' ) ;
#8912=CARTESIAN_POINT ( 'NONE',  ( 1.882286714434961761, 29.86920771456559365, -1.059984207813917445 ) ) ;
#8917=CARTESIAN_POINT ( 'NONE',  ( -0.8595773952324387013, 23.63862887798046586, -1.958280311448067579 ) ) ;
#8918=EDGE_LOOP ( 'NONE', ( #19549, #17173, #23538, #3361, #21492 ) ) ;
#8920=DIRECTION ( 'NONE',  ( 0.000000000000000000, 1.000000000000000000, 0.000000000000000000 ) ) ;
#8925=ORIENTED_EDGE ( 'NONE', *, *, #3091, .F. ) ;
#8926=CARTESIAN_POINT ( 'NONE',  ( -1.834421572440270376, 26.90385776341792834, 1.215053711552148696 ) ) ;
#8927=CARTESIAN_POINT ( 'NONE',  ( 2.500000000000001776, 29.98333333333333783, 0.3272492347489265874 ) ) ;
#8935=CARTESIAN_POINT ( 'NONE',  ( 0.7772763509246626290, 27.55895043119048182, -2.062997027023658614 ) ) ;
#8937=CARTESIAN_POINT ( 'NONE',  ( 2.146814458760614386, 30.61776554068781309, -0.2373564554389892833 ) ) ;
#8940=CARTESIAN_POINT ( 'NONE',  ( 1.429826439988904019, 26.29738147351989141, 1.686326896136374653 ) ) ;
#8941=CARTESIAN_POINT ( 'NONE',  ( 0.1453149127350999992, 27.64163313894999874, -2.464088664829000130 ) ) ;
#8944=CARTESIAN_POINT ( 'NONE',  ( 1.617729300723999897, 27.33271896306000315, 1.617729300723999897 ) ) ;
#8945=AXIS2_PLACEMENT_3D ( 'NONE', #21053, #23098, #11855 ) ;
#8952=CARTESIAN_POINT ( 'NONE',  ( -2.147911019905105690, 30.79742692913817592, -0.5598789276575362184 ) ) ;
#8953=ORIENTED_EDGE ( 'NONE', *, *, #190, .T. ) ;
#8954=CARTESIAN_POINT ( 'NONE',  ( 1.259047450927277323, 24.26666666666667282, 2.184465970885627772 ) ) ;
#8960=CARTESIAN_POINT ( 'NONE',  ( 2.033768963815000053, 28.90151168796999670, 0.6996504102948000181 ) ) ;
#8963=ORIENTED_EDGE ( 'NONE', *, *, #2422, .T. ) ;
#8964=DIRECTION ( 'NONE',  ( 0.000000000000000000, -1.000000000000000000, 0.000000000000000000 ) ) ;
#8966=PLANE ( 'NONE',  #5407 ) ;
#8967=FACE_OUTER_BOUND ( 'NONE', #968, .T. ) ;
#8971=EDGE_LOOP ( 'NONE', ( #633, #19527, #17579, #8866 ) ) ;
#8972=CARTESIAN_POINT ( 'NONE',  ( 0.000000000000000000, 17.95000004008999994, 0.000000000000000000 ) ) ;
#8973=CARTESIAN_POINT ( 'NONE',  ( -4.000000000000000000, 26.37490599056222962, 1.464369514602714251 ) ) ;
#8974=ORIENTED_EDGE ( 'NONE', *, *, #10021, .T. ) ;
#8975=CARTESIAN_POINT ( 'NONE',  ( -1.937279285829999864, 24.60217777461999944, 0.9581223917076999719 ) ) ;
#8976=EDGE_CURVE ( 'NONE', #20510, #21669, #5134, .T. ) ;
#8983=CARTESIAN_POINT ( 'NONE',  ( 0.000000000000000000, 0.000000000000000000, 0.000000000000000000 ) ) ;
#8986=FACE_OUTER_BOUND ( 'NONE', #9094, .T. ) ;
#8987=CARTESIAN_POINT ( 'NONE',  ( -3.999987874060712656, 24.60222989788993431, 1.328900689436825377 ) ) ;
#8989=EDGE_CURVE ( 'NONE', #23711, #2468, #11748, .T. ) ;
#8991=CARTESIAN_POINT ( 'NONE',  ( 1.487333709577000063, 24.19292139875000203, -1.545051636020000174 ) ) ;
#8994=FACE_OUTER_BOUND ( 'NONE', #18319, .T. ) ;
#8996=CARTESIAN_POINT ( 'NONE',  ( -0.6988337043581999142, 30.62333119616999966, -2.254725353931999798 ) ) ;
#8999=B_SPLINE_CURVE_WITH_KNOTS ( 'NONE', 3,
 ( #15336, #2636, #2387, #9778, #13528, #10031, #15577, #21166, #13764, #4577, #11968, #19357, #9542, #13206, #14898, #1839, #22289, #16836 ),
 .UNSPECIFIED., .F., .F.,
 ( 4, 2, 2, 2, 2, 2, 2, 2, 4 ),
 ( 0.000000000000000000, 0.1250000000000000000, 0.2500000000000000000, 0.3750000000000000000, 0.5000000000000000000, 0.6250000000000000000, 0.7500000000000000000, 0.8750000000000000000, 1.000000000000000000 ),
 .UNSPECIFIED. ) ;
#9005=CARTESIAN_POINT ( 'NONE',  ( -1.853875633792771760, 30.49394709125570557, 1.681730189323883629 ) ) ;
#9012=CARTESIAN_POINT ( 'NONE',  ( 0.000000000000000000, 15.09999999999999964, 0.000000000000000000 ) ) ;
#9014=FACE_OUTER_BOUND ( 'NONE', #4383, .T. ) ;
#9022=CARTESIAN_POINT ( 'NONE',  ( 2.133167008818035004, 29.82381322641220578, -0.3387237046597101897 ) ) ;
#9026=CARTESIAN_POINT ( 'NONE',  ( 0.000000000000000000, 26.50000000000000355, 0.000000000000000000 ) ) ;
#9034=CARTESIAN_POINT ( 'NONE',  ( 0.000000000000000000, 26.50000000000000355, 0.000000000000000000 ) ) ;
#9035=ORIENTED_EDGE ( 'NONE', *, *, #6572, .F. ) ;
#9038=CARTESIAN_POINT ( 'NONE',  ( 1.536366799937295413, 29.88333333333333641, 1.999167105995444338 ) ) ;
#9040=CARTESIAN_POINT ( 'NONE',  ( 2.434987841376199835, 24.43331912268990180, -0.6540909589892343057 ) ) ;
#9045=CARTESIAN_POINT ( 'NONE',  ( -1.443311851948678060, 26.31339629256746804, 1.671814658486965088 ) ) ;
#9046=CARTESIAN_POINT ( 'NONE',  ( -0.3933730402102999513, 28.24250240010000113, 2.844001364980000002 ) ) ;
#9047=EDGE_CURVE ( 'NONE', #10311, #21798, #14554, .T. ) ;
#9048=CARTESIAN_POINT ( 'NONE',  ( 1.386897540580403820, 30.71498289799559345, -1.655823646851495967 ) ) ;
#9052=CARTESIAN_POINT ( 'NONE',  ( 1.640193969998194001, 24.74015355458762144, 1.405240085690787843 ) ) ;
#9055=CARTESIAN_POINT ( 'NONE',  ( -0.6185023500890999282, 26.04687716036000111, -2.370125023230000405 ) ) ;
#9057=ORIENTED_EDGE ( 'NONE', *, *, #17108, .F. ) ;
#9061=CARTESIAN_POINT ( 'NONE',  ( -0.9421903349202591649, 29.37597597608807831, 2.074010226627299502 ) ) ;
#9063=ORIENTED_EDGE ( 'NONE', *, *, #11482, .F. ) ;
#9067=CARTESIAN_POINT ( 'NONE',  ( -1.999167105995446780, 29.11753006952333322, 1.536366799937292305 ) ) ;
#9068=CARTESIAN_POINT ( 'NONE',  ( -1.665222063820000153, 29.43094945177000099, 1.361169993929999933 ) ) ;
#9075=EDGE_CURVE ( 'NONE', #17995, #22357, #11165, .T. ) ;
#9081=CARTESIAN_POINT ( 'NONE',  ( 1.894783946879184722, 29.06763461832910167, -1.038242862623748985 ) ) ;
#9083=ORIENTED_EDGE ( 'NONE', *, *, #6748, .T. ) ;
#9087=CARTESIAN_POINT ( 'NONE',  ( -2.127787408056999841, 23.76613442030999934, 0.3788700132753000105 ) ) ;
#9089=ADVANCED_FACE ( 'NONE', ( #16716 ), #23387, .T. ) ;
#9094=EDGE_LOOP ( 'NONE', ( #4243, #14485, #12922, #1161 ) ) ;
#9096=AXIS2_PLACEMENT_3D ( 'NONE', #1456, #18179, #15851 ) ;
#9097=CARTESIAN_POINT ( 'NONE',  ( -1.973507970679954981, 26.24528935287325737, 0.8411564517195385671 ) ) ;
#9098=EDGE_CURVE ( 'NONE', #16136, #9967, #11405, .T. ) ;
#9100=ORIENTED_EDGE ( 'NONE', *, *, #3558, .F. ) ;
#9102=CARTESIAN_POINT ( 'NONE',  ( 1.634048540053999909, 24.00079805554999979, 1.388967512015999883 ) ) ;
#9104=CARTESIAN_POINT ( 'NONE',  ( -2.500000000000000000, 29.03419673619000108, 0.000000000000000000 ) ) ;
#9107=CARTESIAN_POINT ( 'NONE',  ( -1.851011522465999981, 29.22077922916000148, -1.128689685153000166 ) ) ;
#9116=DIRECTION ( 'NONE',  ( 0.000000000000000000, 0.7071067811866525998, -0.7071067811864425456 ) ) ;
#9118=EDGE_CURVE ( 'NONE', #16168, #3528, #16037, .T. ) ;
#9120=EDGE_CURVE ( 'NONE', #14191, #4710, #13092, .T. ) ;
#9123=CARTESIAN_POINT ( 'NONE',  ( 0.1571687770951999963, 27.27212896666999953, -2.665093312283999705 ) ) ;
#9129=ORIENTED_EDGE ( 'NONE', *, *, #18001, .F. ) ;
#9131=AXIS2_PLACEMENT_3D ( 'NONE', #1531, #6726, #23430 ) ;
#9132=CARTESIAN_POINT ( 'NONE',  ( 2.899999929817000055, 18.99999992981999952, 2.312669445490000216E-07 ) ) ;
#9138=CARTESIAN_POINT ( 'NONE',  ( 1.324993377608203460, 29.91963323941933695, -1.705809634641242134 ) ) ;
#9140=CARTESIAN_POINT ( 'NONE',  ( 1.812154074756000099, 25.10789601364000134, -1.214490967170999802 ) ) ;
#9142=CARTESIAN_POINT ( 'NONE',  ( -0.8552766487867897727, 23.64350003464605265, -1.965477479697049112 ) ) ;
#9143=ORIENTED_EDGE ( 'NONE', *, *, #21266, .T. ) ;
#9147=AXIS2_PLACEMENT_3D ( 'NONE', #4344, #7857, #11735 ) ;
#9148=MECHANICAL_DESIGN_GEOMETRIC_PRESENTATION_REPRESENTATION('',(#5735),#17598);
#9152=EDGE_LOOP ( 'NONE', ( #433, #138, #12263 ) ) ;
#9153=LINE ( 'NONE', #7327, #13692 ) ;
#9162=CARTESIAN_POINT ( 'NONE',  ( 0.2359769429284387376, 26.79041702683161930, -2.194852148367845146 ) ) ;
#9165=CARTESIAN_POINT ( 'NONE',  ( 2.022581721832676926, 30.64951854208338133, -0.7578523236017076226 ) ) ;
#9168=CARTESIAN_POINT ( 'NONE',  ( 3.100000000000000089, 17.00000000000000000, 0.000000000000000000 ) ) ;
#9171=CARTESIAN_POINT ( 'NONE',  ( 0.9439018917106000162, 28.64864211381999937, 1.852511768836999861 ) ) ;
#9190=VERTEX_POINT ( 'NONE', #4007 ) ;
#9194=DIRECTION ( 'NONE',  ( 0.000000000000000000, 0.000000000000000000, -1.000000000000000000 ) ) ;
#9198=CARTESIAN_POINT ( 'NONE',  ( 1.006368030278437464, 29.14341433222939415, -1.945138833163934100 ) ) ;
#9199=CARTESIAN_POINT ( 'NONE',  ( -3.099999776787000005, 21.99999977679100027, -5.570936493763999179E-07 ) ) ;
#9200=EDGE_LOOP ( 'NONE', ( #12409, #12282, #20452, #13749 ) ) ;
#9201=DIRECTION ( 'NONE',  ( 1.000000000000000000, 0.000000000000000000, 0.000000000000000000 ) ) ;
#9202=ORIENTED_EDGE ( 'NONE', *, *, #23599, .F. ) ;
#9203=CARTESIAN_POINT ( 'NONE',  ( -1.763881168339999750, 23.94123933040999930, 1.557685456931000134 ) ) ;
#9204=CARTESIAN_POINT ( 'NONE',  ( -2.184465970885641539, 28.06666666666667354, 1.259047450927253120 ) ) ;
#9207=DIRECTION ( 'NONE',  ( -0.7071067811864980568, -0.7071067811865969777, 1.093190268588995838E-08 ) ) ;
#9208=CYLINDRICAL_SURFACE ( 'NONE', #16513, 2.000000000000000000 ) ;
#9210=EDGE_CURVE ( 'NONE', #12844, #16360, #20368, .T. ) ;
#9211=EDGE_LOOP ( 'NONE', ( #23958, #14657, #3648, #6852, #5150, #6311 ) ) ;
#9213=DIRECTION ( 'NONE',  ( 0.000000000000000000, 1.000000000000000000, 0.000000000000000000 ) ) ;
#9215=FACE_OUTER_BOUND ( 'NONE', #10385, .T. ) ;
#9216=EDGE_LOOP ( 'NONE', ( #16773, #18764, #97, #19049 ) ) ;
#9218=CARTESIAN_POINT ( 'NONE',  ( 2.141482600577999662, 24.89737365715999928, -0.1157515109216999960 ) ) ;
#9222=CARTESIAN_POINT ( 'NONE',  ( 1.605714764276999995, 29.68981568338000088, -1.730281315055000046 ) ) ;
#9226=VECTOR ( 'NONE', #8002, 1000.000000000000000 ) ;
#9229=CARTESIAN_POINT ( 'NONE',  ( -2.531009774008887270, 24.22915547920286627, -0.09632474734362661550 ) ) ;
#9231=EDGE_CURVE ( 'NONE', #1224, #8048, #20473, .T. ) ;
#9234=CARTESIAN_POINT ( 'NONE',  ( 4.750000000000000000, 15.09999999999999964, 0.000000000000000000 ) ) ;
#9236=AXIS2_PLACEMENT_3D ( 'NONE', #10034, #17419, #2154 ) ;
#9240=EDGE_CURVE ( 'NONE', #20732, #15990, #15023, .T. ) ;
#9241=CARTESIAN_POINT ( 'NONE',  ( -1.876963106047000007, 26.69506359724000077, -1.603077936557000038 ) ) ;
#9242=ADVANCED_FACE ( 'NONE', ( #14054 ), #7306, .T. ) ;
#9243=ORIENTED_EDGE ( 'NONE', *, *, #9240, .F. ) ;
#9246=LINE ( 'NONE', #5950, #1270 ) ;
#9253=AXIS2_PLACEMENT_3D ( 'NONE', #17747, #13980, #13855 ) ;
#9254=CARTESIAN_POINT ( 'NONE',  ( 2.000000000000000000, 18.72912878474779319, 0.000000000000000000 ) ) ;
#9256=CIRCLE ( 'NONE', #9628, 4.724999999999999645 ) ;
#9258=CARTESIAN_POINT ( 'NONE',  ( 2.157175093438090219, 29.79162255941403359, 0.2087797654426111760 ) ) ;
#9259=ORIENTED_EDGE ( 'NONE', *, *, #18938, .F. ) ;
#9260=CARTESIAN_POINT ( 'NONE',  ( -2.008968276635000105, 23.78173846916000045, -0.8503130695115000970 ) ) ;
#9262=CARTESIAN_POINT ( 'NONE',  ( -0.8767952504666675084, 23.65152616175392453, -1.964765437033486162 ) ) ;
#9265=CARTESIAN_POINT ( 'NONE',  ( 0.000000000000000000, 9.100092063578999912, 0.000000000000000000 ) ) ;
#9269=EDGE_CURVE ( 'NONE', #23400, #5348, #1128, .T. ) ;
#9271=EDGE_CURVE ( 'NONE', #14835, #21669, #4603, .T. ) ;
#9272=VERTEX_POINT ( 'NONE', #23000 ) ;
#9273=CIRCLE ( 'NONE', #11197, 4.649999999999999467 ) ;
#9285=CARTESIAN_POINT ( 'NONE',  ( -2.321186682587941696, 26.50000000000000711, -3.278664397485417492 ) ) ;
#9288=CARTESIAN_POINT ( 'NONE',  ( 2.128973442807626792, 30.62540607072664400, -0.3665344719387015338 ) ) ;
#9290=CARTESIAN_POINT ( 'NONE',  ( 1.014628930286358699, 26.27923812234717005, 1.944022540165884383 ) ) ;
#9291=CARTESIAN_POINT ( 'NONE',  ( 1.666184814955848026, 24.76080278563852133, 1.341642937687889114 ) ) ;
#9293=CARTESIAN_POINT ( 'NONE',  ( -0.2242450566330000117, 26.84521896305999888, -2.276798263289999902 ) ) ;
#9294=DIRECTION ( 'NONE',  ( 0.000000000000000000, -1.000000000000000000, 0.000000000000000000 ) ) ;
#9300=CARTESIAN_POINT ( 'NONE',  ( -1.904955016777212684, 29.30416709048808244, 1.249154685861223912 ) ) ;
#9305=CARTESIAN_POINT ( 'NONE',  ( -2.184465970885641983, 29.10086340285666751, 1.259047450927253564 ) ) ;
#9310=CARTESIAN_POINT ( 'NONE',  ( -2.000000000000000000, 18.10000000000000142, 0.000000000000000000 ) ) ;
#9312=CARTESIAN_POINT ( 'NONE',  ( 0.000000000000000000, 15.04999987253368943, -2.704938617610999654E-14 ) ) ;
#9317=CARTESIAN_POINT ( 'NONE',  ( 1.737941468486482455, 29.08498798696146181, -1.285333566862393972 ) ) ;
#9320=ORIENTED_EDGE ( 'NONE', *, *, #5722, .F. ) ;
#9321=CARTESIAN_POINT ( 'NONE',  ( 1.699994387327691481, 10.36668292280599957, 1.053574431676630008 ) ) ;
#9323=CARTESIAN_POINT ( 'NONE',  ( 1.678513321804000036, 24.15025016897999777, 1.649317033692999868 ) ) ;
#9326=CARTESIAN_POINT ( 'NONE',  ( 0.000000000000000000, 18.89999999999999858, 0.000000000000000000 ) ) ;
#9327=FACE_OUTER_BOUND ( 'NONE', #16218, .T. ) ;
#9329=( NAMED_UNIT ( * ) PLANE_ANGLE_UNIT ( ) SI_UNIT ( $, .RADIAN. ) );
#9336=CARTESIAN_POINT ( 'NONE',  ( 1.820465805901000156, 24.96141477156000121, -1.133688841959000104 ) ) ;
#9340=CARTESIAN_POINT ( 'NONE',  ( 2.226929716040000340, 28.82810905619000152, -0.7829338363701999759 ) ) ;
#9345=ORIENTED_EDGE ( 'NONE', *, *, #12310, .F. ) ;
#9353=CARTESIAN_POINT ( 'NONE',  ( 1.994688225595000253, 25.52506359724000262, 1.016344414748000080 ) ) ;
#9354=EDGE_CURVE ( 'NONE', #11075, #20732, #8365, .T. ) ;
#9355=VERTEX_POINT ( 'NONE', #4741 ) ;
#9356=ORIENTED_EDGE ( 'NONE', *, *, #14726, .F. ) ;
#9359=DIRECTION ( 'NONE',  ( -0.000000000000000000, 1.000000000000000000, -0.000000000000000000 ) ) ;
#9366=CARTESIAN_POINT ( 'NONE',  ( 2.146824282253999794, 30.41473571554000088, -0.4462322471723000339 ) ) ;
#9371=CARTESIAN_POINT ( 'NONE',  ( 1.464084226283197454, 29.69852001067018676, 1.588251168237700739 ) ) ;
#9373=CARTESIAN_POINT ( 'NONE',  ( -1.732027827905000095, 24.54951388964999737, -1.326261777753000137 ) ) ;
#9376=EDGE_LOOP ( 'NONE', ( #21836, #8974, #339, #3635 ) ) ;
#9378=DIRECTION ( 'NONE',  ( 0.8500000000000165201, 0.000000000000000000, -0.5267826876426102700 ) ) ;
#9381=EDGE_CURVE ( 'NONE', #8812, #12420, #6939, .T. ) ;
#9386=CARTESIAN_POINT ( 'NONE',  ( 1.999167105995457661, 29.91666666666667496, 1.536366799937278760 ) ) ;
#9394=B_SPLINE_CURVE_WITH_KNOTS ( 'NONE', 3,
 ( #7731, #22728, #6142, #13531, #690, #19098, #13287, #21041 ),
 .UNSPECIFIED., .F., .F.,
 ( 4, 2, 2, 4 ),
 ( 0.000000000000000000, 0.2499999999999998890, 0.4999999999999997780, 1.000000000000000000 ),
 .UNSPECIFIED. ) ;
#9396=FACE_OUTER_BOUND ( 'NONE', #5232, .T. ) ;
#9400=CARTESIAN_POINT ( 'NONE',  ( 0.3983959897931292904, 30.42739071784584937, 2.122834239064325779 ) ) ;
#9405=CARTESIAN_POINT ( 'NONE',  ( 1.656631363487247821, 24.76418780987420476, 1.348065658398109434 ) ) ;
#9406=CIRCLE ( 'NONE', #22922, 2.399999999999999911 ) ;
#9408=CARTESIAN_POINT ( 'NONE',  ( -1.556103512505999875, 26.89364211382000036, 1.683383295848999817 ) ) ;
#9409=CARTESIAN_POINT ( 'NONE',  ( 0.000000000000000000, 18.00000000000000000, 0.000000000000000000 ) ) ;
#9413=EDGE_CURVE ( 'NONE', #11582, #2323, #19312, .T. ) ;
#9418=ORIENTED_EDGE ( 'NONE', *, *, #9118, .F. ) ;
#9423=CARTESIAN_POINT ( 'NONE',  ( 1.961083286043999951, 30.48982497936000158, 0.8831193726211999939 ) ) ;
#9430=CARTESIAN_POINT ( 'NONE',  ( 2.434931691670793263, 29.16666666666666430, 0.6543697108981857413 ) ) ;
#9435=CARTESIAN_POINT ( 'NONE',  ( 0.2973647920025167535, 29.18612839175506934, -2.139422557246009937 ) ) ;
#9437=ORIENTED_EDGE ( 'NONE', *, *, #21426, .T. ) ;
#9438=CARTESIAN_POINT ( 'NONE',  ( -2.051647590440843327, 23.66978687261612890, 0.7531949266739137450 ) ) ;
#9439=ORIENTED_EDGE ( 'NONE', *, *, #2730, .F. ) ;
#9440=AXIS2_PLACEMENT_3D ( 'NONE', #1024, #11815, #2855 ) ;
#9441=CARTESIAN_POINT ( 'NONE',  ( -1.344835081562999912, 25.22921029035000018, -1.691883008907999919 ) ) ;
#9442=CARTESIAN_POINT ( 'NONE',  ( 1.999167105995457661, 28.31666666666666998, 1.536366799937278760 ) ) ;
#9444=CARTESIAN_POINT ( 'NONE',  ( 0.000000000000000000, -1.550000000000000044, 0.000000000000000000 ) ) ;
#9445=DIRECTION ( 'NONE',  ( -0.000000000000000000, 1.000000000000000000, 0.000000000000000000 ) ) ;
#9446=LINE ( 'NONE', #111, #20770 ) ;
#9450=CARTESIAN_POINT ( 'NONE',  ( 0.000000000000000000, 22.00000000000000000, 0.000000000000000000 ) ) ;
#9452=ORIENTED_EDGE ( 'NONE', *, *, #1870, .T. ) ;
#9454=CARTESIAN_POINT ( 'NONE',  ( -1.271387008224000192, 25.40970257236000052, 1.727113330389000057 ) ) ;
#9459=CARTESIAN_POINT ( 'NONE',  ( -2.015416341576000026, 29.11534459859000279, -1.228938668624000030 ) ) ;
#9465=CARTESIAN_POINT ( 'NONE',  ( 0.8794326344061793588, 24.47914381499106184, 2.375062700745428135 ) ) ;
#9470=CARTESIAN_POINT ( 'NONE',  ( 1.460999620166917756, 24.69858516586207386, 1.653668814814927890 ) ) ;
#9472=DIRECTION ( 'NONE',  ( 0.000000000000000000, -1.000000000000000000, 0.000000000000000000 ) ) ;
#9473=CARTESIAN_POINT ( 'NONE',  ( 0.05241653317065999435, 26.88212896666999896, 2.669209039122999894 ) ) ;
#9477=CARTESIAN_POINT ( 'NONE',  ( -4.000000000000000000, 24.50000000000000000, 0.000000000000000000 ) ) ;
#9479=EDGE_CURVE ( 'NONE', #18038, #11323, #15044, .T. ) ;
#9486=CARTESIAN_POINT ( 'NONE',  ( 0.5124189445521000197, 30.55860975689000014, -2.131997105840000017 ) ) ;
#9490=CARTESIAN_POINT ( 'NONE',  ( -0.2454928412648832159, 29.58943779370164151, 2.147640904564822151 ) ) ;
#9491=ORIENTED_EDGE ( 'NONE', *, *, #11278, .T. ) ;
#9492=CARTESIAN_POINT ( 'NONE',  ( 2.261417238927000195, 24.18218325944999947, 0.5843056356417000163 ) ) ;
#9493=CARTESIAN_POINT ( 'NONE',  ( 0.000000000000000000, 22.09999988306816832, -4.649999883068000273 ) ) ;
#9502=CONICAL_SURFACE ( 'NONE', #3339, 3.049999825846000157, 0.7853981633972997312 ) ;
#9505=EDGE_CURVE ( 'NONE', #23934, #21619, #8477, .T. ) ;
#9512=DIRECTION ( 'NONE',  ( 0.000000000000000000, 0.000000000000000000, -1.000000000000000000 ) ) ;
#9513=CARTESIAN_POINT ( 'NONE',  ( 2.500000000000000000, 28.65086340285666111, -0.3272492347489373565 ) ) ;
#9515=EDGE_CURVE ( 'NONE', #8048, #21798, #22767, .T. ) ;
#9516=CARTESIAN_POINT ( 'NONE',  ( 2.146464929684074541, 30.58969480563138887, 0.2409270991070303070 ) ) ;
#9521=CARTESIAN_POINT ( 'NONE',  ( 2.434931691670791487, 27.80086340285666680, 0.6543697108981911814 ) ) ;
#9523=CARTESIAN_POINT ( 'NONE',  ( 0.04836512055258999909, 27.02446440326000143, 2.462898805936000191 ) ) ;
#9533=ADVANCED_FACE ( 'NONE', ( #8295 ), #19317, .T. ) ;
#9534=EDGE_CURVE ( 'NONE', #10909, #13113, #16210, .T. ) ;
#9535=DIRECTION ( 'NONE',  ( 0.000000000000000000, 1.000000000000000000, 0.000000000000000000 ) ) ;
#9541=FACE_OUTER_BOUND ( 'NONE', #21506, .T. ) ;
#9542=CARTESIAN_POINT ( 'NONE',  ( -1.536366799937282313, 26.75086340285667319, 1.999167105995454552 ) ) ;
#9544=EDGE_CURVE ( 'NONE', #2323, #13406, #13878, .T. ) ;
#9552=CARTESIAN_POINT ( 'NONE',  ( 2.159136702051380308, 29.00043188692588103, 0.05903435693729322531 ) ) ;
#9556=LINE ( 'NONE', #2282, #11144 ) ;
#9559=CARTESIAN_POINT ( 'NONE',  ( 0.3985328791175999918, 26.31299822781000231, 2.231710853292999897 ) ) ;
#9560=DIRECTION ( 'NONE',  ( 0.000000000000000000, 1.000000000000000000, 0.000000000000000000 ) ) ;
#9561=CARTESIAN_POINT ( 'NONE',  ( 0.000000000000000000, -1.550000000000000044, 0.000000000000000000 ) ) ;
#9564=B_SPLINE_CURVE_WITH_KNOTS ( 'NONE', 3,
 ( #15299, #8296, #15183, #6100, #13732, #11810, #21007, #15544, #10110, #7932 ),
 .UNSPECIFIED., .F., .F.,
 ( 4, 1, 1, 2, 2, 4 ),
 ( 0.000000000000000000, 0.2499999999999994449, 0.3749999999999990563, 0.4374999999999988898, 0.4999999999999987788, 1.000000000000000000 ),
 .UNSPECIFIED. ) ;
#9568=CIRCLE ( 'NONE', #6479, 4.750000000000000000 ) ;
#9569=CARTESIAN_POINT ( 'NONE',  ( -1.497233415519999999, 25.19883331122000314, 2.033913964766000060 ) ) ;
#9573=CARTESIAN_POINT ( 'NONE',  ( 2.408588448076999899, 28.72267442561999928, -0.8468005884097000724 ) ) ;
#9578=CARTESIAN_POINT ( 'NONE',  ( -2.500000000000000888, 29.81753006952333251, -0.3272492347489316944 ) ) ;
#9583=EDGE_LOOP ( 'NONE', ( #8214, #12439, #17420, #15535 ) ) ;
#9585=CARTESIAN_POINT ( 'NONE',  ( 0.000000000000000000, 19.09999999999999787, 0.000000000000000000 ) ) ;
#9590=LINE ( 'NONE', #7657, #5199 ) ;
#9591=CARTESIAN_POINT ( 'NONE',  ( -2.857252503208999705, 27.36169433610000112, -0.2814148094396999866 ) ) ;
#9592=ORIENTED_EDGE ( 'NONE', *, *, #381, .F. ) ;
#9605=CARTESIAN_POINT ( 'NONE',  ( -2.190643450555000094, 29.98311359149999689, -0.09517956215792000574 ) ) ;
#9607=CARTESIAN_POINT ( 'NONE',  ( 1.207017934462505604, 29.67927007522607497, 1.791127842952921823 ) ) ;
#9609=CARTESIAN_POINT ( 'NONE',  ( -2.157700896676000291, 23.85153623465999928, 0.3212303798653999842 ) ) ;
#9612=CIRCLE ( 'NONE', #4200, 2.729128784747790970 ) ;
#9613=EDGE_LOOP ( 'NONE', ( #3765, #23411, #21758, #18267, #4918, #21255, #19248 ) ) ;
#9618=DIRECTION ( 'NONE',  ( 0.000000000000000000, 1.000000000000000000, 0.000000000000000000 ) ) ;
#9628=AXIS2_PLACEMENT_3D ( 'NONE', #12206, #12329, #14015 ) ;
#9634=AXIS2_PLACEMENT_3D ( 'NONE', #19872, #19515, #12374 ) ;
#9635=CARTESIAN_POINT ( 'NONE',  ( 0.9744765624120645953, 26.41693820796410819, -4.056187847889995979 ) ) ;
#9637=CARTESIAN_POINT ( 'NONE',  ( 2.142844928456669962, 30.58794887508146232, 0.2701627623478729534 ) ) ;
#9638=ORIENTED_EDGE ( 'NONE', *, *, #9413, .F. ) ;
#9642=AXIS2_PLACEMENT_3D ( 'NONE', #16915, #18975, #20799 ) ;
#9645=CARTESIAN_POINT ( 'NONE',  ( 0.4330518317348999724, 26.24446440326000030, 2.425010641684000046 ) ) ;
#9646=AXIS2_PLACEMENT_3D ( 'NONE', #1054, #4578, #11969 ) ;
#9648=CARTESIAN_POINT ( 'NONE',  ( -4.000000000000000000, 24.80000000000000426, -2.309401076759000304 ) ) ;
#9650=DIRECTION ( 'NONE',  ( 0.000000000000000000, 0.000000000000000000, -1.000000000000000000 ) ) ;
#9652=CARTESIAN_POINT ( 'NONE',  ( 2.169463140925995237, 28.02568812777378326, 0.06845542556112334254 ) ) ;
#9653=DIRECTION ( 'NONE',  ( 1.000000000000000000, 0.000000000000000000, 0.000000000000000000 ) ) ;
#9655=EDGE_LOOP ( 'NONE', ( #1845, #21981, #4503, #11895, #17680 ) ) ;
#9661=CARTESIAN_POINT ( 'NONE',  ( 4.750000000000000000, 21.89999999999999858, 0.000000000000000000 ) ) ;
#9663=LINE ( 'NONE', #441, #3695 ) ;
#9666=EDGE_LOOP ( 'NONE', ( #18641, #5284, #1614, #11116 ) ) ;
#9667=FACE_OUTER_BOUND ( 'NONE', #16551, .T. ) ;
#9668=CARTESIAN_POINT ( 'NONE',  ( -2.607696352436000176, 26.38206776952000254, 0.5721489135198000175 ) ) ;
#9669=AXIS2_PLACEMENT_3D ( 'NONE', #22342, #2124, #3950 ) ;
#9679=CARTESIAN_POINT ( 'NONE',  ( 1.403495832404999977, 26.60549822781000273, -1.780325977227999790 ) ) ;
#9688=CARTESIAN_POINT ( 'NONE',  ( 2.411685057264000065, 23.91801102320000183, -0.7498601224302000601 ) ) ;
#9690=ORIENTED_EDGE ( 'NONE', *, *, #21060, .T. ) ;
#9693=CARTESIAN_POINT ( 'NONE',  ( -2.375794074296999625, 30.62788859182999701, 1.065851494486000028 ) ) ;
#9701=DIRECTION ( 'NONE',  ( 1.000000000000000000, 0.000000000000000000, 0.000000000000000000 ) ) ;
#9703=CARTESIAN_POINT ( 'NONE',  ( -0.04686596309914999731, 25.05782222538000070, 2.736742389782000018 ) ) ;
#9704=FACE_OUTER_BOUND ( 'NONE', #9211, .T. ) ;
#9705=CARTESIAN_POINT ( 'NONE',  ( -2.163337044627856365, 24.58232107606292516, -0.3658931050139514474 ) ) ;
#9709=CONICAL_SURFACE ( 'NONE', #18600, 4.674999979945999584, 0.7853981633972997312 ) ;
#9710=CARTESIAN_POINT ( 'NONE',  ( 0.000000000000000000, 16.95000012746599793, -2.704938617610999654E-14 ) ) ;
#9711=CARTESIAN_POINT ( 'NONE',  ( -1.948889566018999986, 26.67919433610000013, 2.108296854627000005 ) ) ;
#9715=EDGE_CURVE ( 'NONE', #13716, #23321, #13498, .T. ) ;
#9719=LINE ( 'NONE', #9834, #508 ) ;
#9720=VERTEX_POINT ( 'NONE', #17925 ) ;
#9726=CARTESIAN_POINT ( 'NONE',  ( 0.3249195791085000007, 29.65169427534999969, 2.164038618295999861 ) ) ;
#9728=CARTESIAN_POINT ( 'NONE',  ( 0.4950218517047121902, 29.63316247012222604, 2.102426574152561400 ) ) ;
#9729=VERTEX_POINT ( 'NONE', #3032 ) ;
#9731=CARTESIAN_POINT ( 'NONE',  ( -1.974988437399999963, 24.44503257140999963, 0.9367674359008000273 ) ) ;
#9754=CARTESIAN_POINT ( 'NONE',  ( 0.3916584102265154854, 30.42698342189353866, 2.124085250123096902 ) ) ;
#9755=ORIENTED_EDGE ( 'NONE', *, *, #20221, .F. ) ;
#9760=CARTESIAN_POINT ( 'NONE',  ( -2.288454502553999959, 26.79614211382000022, 0.1349572241793000060 ) ) ;
#9763=ORIENTED_EDGE ( 'NONE', *, *, #22703, .F. ) ;
#9764=DIRECTION ( 'NONE',  ( 0.000000000000000000, 0.000000000000000000, 1.000000000000000000 ) ) ;
#9766=EDGE_CURVE ( 'NONE', #8792, #18916, #23883, .T. ) ;
#9767=CARTESIAN_POINT ( 'NONE',  ( 1.359641396650144607, 27.91473787195837275, 1.732418534185389047 ) ) ;
#9772=EDGE_CURVE ( 'NONE', #2323, #10715, #3855, .T. ) ;
#9778=CARTESIAN_POINT ( 'NONE',  ( 2.184465970885649089, 26.96753006952332399, 1.259047450927240241 ) ) ;
#9780=CARTESIAN_POINT ( 'NONE',  ( 0.000000000000000000, 15.05000017415440006, 0.000000000000000000 ) ) ;
#9782=CARTESIAN_POINT ( 'NONE',  ( 0.000000000000000000, 16.95000012746599793, 0.000000000000000000 ) ) ;
#9783=CARTESIAN_POINT ( 'NONE',  ( 2.628147087956000050, 28.33206776952000183, 0.4693273880717999669 ) ) ;
#9785=CARTESIAN_POINT ( 'NONE',  ( 2.091722048788486887, 29.03591149769223989, -0.5394191446943552570 ) ) ;
#9788=EDGE_LOOP ( 'NONE', ( #13249, #5591 ) ) ;
#9790=VERTEX_POINT ( 'NONE', #23953 ) ;
#9792=CARTESIAN_POINT ( 'NONE',  ( 0.000000000000000000, 14.95000002005000006, 0.000000000000000000 ) ) ;
#9793=CARTESIAN_POINT ( 'NONE',  ( 0.5289967318967999654, 28.15756359723999935, -2.411020654974999733 ) ) ;
#9805=CARTESIAN_POINT ( 'NONE',  ( 2.480184517804000066, 25.41360425264999634, -0.7931718914648999696 ) ) ;
#9807=ORIENTED_EDGE ( 'NONE', *, *, #16810, .T. ) ;
#9809=DIRECTION ( 'NONE',  ( 0.000000000000000000, 0.000000000000000000, 1.000000000000000000 ) ) ;
#9817=CARTESIAN_POINT ( 'NONE',  ( -2.500000000000000000, 29.83419673618999823, 0.000000000000000000 ) ) ;
#9819=DIRECTION ( 'NONE',  ( -1.000000000000000000, 0.000000000000000000, 0.000000000000000000 ) ) ;
#9821=LINE ( 'NONE', #13688, #23454 ) ;
#9823=CARTESIAN_POINT ( 'NONE',  ( -2.128189877949903774, 23.77262414965302284, -0.5291991134722092704 ) ) ;
#9824=DIRECTION ( 'NONE',  ( -0.7071067811823850136, 0.7071067811898851252, -1.080116767747976029E-06 ) ) ;
#9825=AXIS2_PLACEMENT_3D ( 'NONE', #20356, #21822, #14542 ) ;
#9828=EDGE_CURVE ( 'NONE', #3305, #11676, #23937, .T. ) ;
#9829=DIRECTION ( 'NONE',  ( 0.000000000000000000, -0.7071067811866525998, -0.7071067811864425456 ) ) ;
#9834=CARTESIAN_POINT ( 'NONE',  ( -4.549999861571000004, 21.99999986157541798, 6.289351259589999728E-08 ) ) ;
#9835=EDGE_CURVE ( 'NONE', #22702, #3216, #3079, .T. ) ;
#9843=CARTESIAN_POINT ( 'NONE',  ( 1.691667482778999920, 30.51999502565000100, -1.640128175915999797 ) ) ;
#9846=CARTESIAN_POINT ( 'NONE',  ( -0.04072186729643159642, 29.60146742886088589, 2.159503982503783615 ) ) ;
#9849=CARTESIAN_POINT ( 'NONE',  ( 2.054615896157999888, 24.75754592284000211, 1.138344536031999921 ) ) ;
#9852=LINE ( 'NONE', #16869, #10043 ) ;
#9861=DIRECTION ( 'NONE',  ( 0.000000000000000000, -1.000000000000000000, 0.000000000000000000 ) ) ;
#9863=CARTESIAN_POINT ( 'NONE',  ( 4.000000000000000000, 26.37490599056222962, -1.464369514602714251 ) ) ;
#9866=CARTESIAN_POINT ( 'NONE',  ( -4.649999999999999467, 22.00000000000000000, 0.000000000000000000 ) ) ;
#9872=CARTESIAN_POINT ( 'NONE',  ( 1.350914310362234527, 26.47444252552741872, -3.838851412777818606 ) ) ;
#9873=CARTESIAN_POINT ( 'NONE',  ( 2.434931691670788823, 27.86753006952332612, -0.6543697108982007293 ) ) ;
#9874=CARTESIAN_POINT ( 'NONE',  ( 0.3871515648526898112, 30.42671105185918279, 2.124914593381988848 ) ) ;
#9875=EDGE_CURVE ( 'NONE', #11676, #3528, #22485, .T. ) ;
#9876=VERTEX_POINT ( 'NONE', #2504 ) ;
#9879=CARTESIAN_POINT ( 'NONE',  ( 1.699999998837999904, 12.90000000000000036, -1.053565373074999867 ) ) ;
#9880=CARTESIAN_POINT ( 'NONE',  ( -0.7145966149424999303, 28.58446440326000015, 2.357055497444999759 ) ) ;
#9886=CARTESIAN_POINT ( 'NONE',  ( -1.817280340265412519, 28.50647256964058229, 1.244239457231288926 ) ) ;
#9888=ORIENTED_EDGE ( 'NONE', *, *, #2144, .T. ) ;
#9889=CARTESIAN_POINT ( 'NONE',  ( 0.000000000000000000, 16.95000012746599793, 0.000000000000000000 ) ) ;
#9893=CARTESIAN_POINT ( 'NONE',  ( 0.000000000000000000, 19.00000000000000000, 0.000000000000000000 ) ) ;
#9894=CARTESIAN_POINT ( 'NONE',  ( 0.000000000000000000, 18.00000000000000000, 0.000000000000000000 ) ) ;
#9901=DIRECTION ( 'NONE',  ( -1.000000000000000000, 0.000000000000000000, 0.000000000000000000 ) ) ;
#9904=CARTESIAN_POINT ( 'NONE',  ( -1.289728978252000058, 28.51913313895000002, -2.104626470933999904 ) ) ;
#9906=CARTESIAN_POINT ( 'NONE',  ( 2.159790447331193075, 29.00657262603238351, -0.04485059893192275965 ) ) ;
#9909=CARTESIAN_POINT ( 'NONE',  ( 1.800000000175999926, 13.00000000000000000, 1.081665382745000015 ) ) ;
#9911=EDGE_CURVE ( 'NONE', #12880, #9729, #3838, .T. ) ;
#9913=CARTESIAN_POINT ( 'NONE',  ( 0.000000000000000000, 26.34999999328000087, 0.000000000000000000 ) ) ;
#9915=VECTOR ( 'NONE', #18783, 1000.000000000000000 ) ;
#9922=VERTEX_POINT ( 'NONE', #7838 ) ;
#9923=EDGE_CURVE ( 'NONE', #2115, #12128, #7709, .T. ) ;
#9924=CARTESIAN_POINT ( 'NONE',  ( 2.222509048435000079, 30.93848831202999961, -1.574711173318000146 ) ) ;
#9925=AXIS2_PLACEMENT_3D ( 'NONE', #9026, #16893, #783 ) ;
#9926=CARTESIAN_POINT ( 'NONE',  ( 2.474460460966999786, 23.85396990879999990, 0.5055298778630998857 ) ) ;
#9928=CIRCLE ( 'NONE', #19211, 3.000000000000000000 ) ;
#9930=CARTESIAN_POINT ( 'NONE',  ( -0.4253681007931999769, 28.35394054784999796, 2.615173885854999991 ) ) ;
#9934=DIRECTION ( 'NONE',  ( -1.000000000000000000, 0.000000000000000000, 0.000000000000000000 ) ) ;
#9935=LINE ( 'NONE', #11644, #13110 ) ;
#9936=VERTEX_POINT ( 'NONE', #14971 ) ;
#9938=ORIENTED_EDGE ( 'NONE', *, *, #14435, .F. ) ;
#9942=CARTESIAN_POINT ( 'NONE',  ( -2.143277222256999792, 23.64327722226000006, 4.118360636503000477E-13 ) ) ;
#9946=CARTESIAN_POINT ( 'NONE',  ( -1.767805011140364924, 26.50018596745192312, 1.767686163102024643 ) ) ;
#9948=AXIS2_PLACEMENT_3D ( 'NONE', #9889, #919, #6011 ) ;
#9953=CIRCLE ( 'NONE', #10747, 4.649999999999999467 ) ;
#9958=CARTESIAN_POINT ( 'NONE',  ( 4.750000000000000000, 24.29999999999999716, 0.000000000000000000 ) ) ;
#9961=CARTESIAN_POINT ( 'NONE',  ( 2.256627625724999753, 29.58481375689000004, 0.6777845771746999759 ) ) ;
#9963=VECTOR ( 'NONE', #23101, 1000.000000000000114 ) ;
#9964=CARTESIAN_POINT ( 'NONE',  ( 0.000000000000000000, 18.50000000000000000, 0.000000000000000000 ) ) ;
#9966=CARTESIAN_POINT ( 'NONE',  ( -2.070194703216106991, 29.44071876932419585, 0.6155423327383686694 ) ) ;
#9967=VERTEX_POINT ( 'NONE', #14603 ) ;
#9968=CARTESIAN_POINT ( 'NONE',  ( -1.864937606498999978, 24.33875932984999935, -1.428034483940999966 ) ) ;
#9976=ORIENTED_EDGE ( 'NONE', *, *, #15472, .F. ) ;
#9979=CARTESIAN_POINT ( 'NONE',  ( -0.3272492347489393549, 27.01666666666667282, -2.499999999999999556 ) ) ;
#9982=ORIENTED_EDGE ( 'NONE', *, *, #5282, .T. ) ;
#9983=EDGE_CURVE ( 'NONE', #9190, #8278, #15058, .T. ) ;
#9984=LINE ( 'NONE', #4296, #13478 ) ;
#9985=B_SPLINE_CURVE_WITH_KNOTS ( 'NONE', 3,
 ( #5367, #12757, #5141, #20147, #3554, #5481, #18436, #8644, #12411, #12523 ),
 .UNSPECIFIED., .F., .F.,
 ( 4, 2, 2, 2, 4 ),
 ( 0.000000000000000000, 0.2115962377624443225, 0.4231924755248886449, 0.6347887132873327731, 0.8463849510497769568 ),
 .UNSPECIFIED. ) ;
#9990=CONICAL_SURFACE ( 'NONE', #23531, 4.649999926447000220, 0.7853981633972997312 ) ;
#9991=DIRECTION ( 'NONE',  ( 1.000000000000000000, 0.000000000000000000, 0.000000000000000000 ) ) ;
#9994=CARTESIAN_POINT ( 'NONE',  ( 0.000000000000000000, 26.20000000000000284, 4.618802153517000519 ) ) ;
#9996=CARTESIAN_POINT ( 'NONE',  ( -2.184465970885646424, 28.96753006952333465, -1.259047450927245126 ) ) ;
#9997=DIRECTION ( 'NONE',  ( -0.000000000000000000, 1.000000000000000000, 0.000000000000000000 ) ) ;
#9998=CARTESIAN_POINT ( 'NONE',  ( -1.086675645002173507, 30.07086948948929006, -1.869048572787896489 ) ) ;
#9999=ORIENTED_EDGE ( 'NONE', *, *, #3445, .T. ) ;
#10003=FACE_OUTER_BOUND ( 'NONE', #20289, .T. ) ;
#10007=DIRECTION ( 'NONE',  ( 0.000000000000000000, 0.000000000000000000, -1.000000000000000000 ) ) ;
#10010=ORIENTED_EDGE ( 'NONE', *, *, #11029, .T. ) ;
#10011=VECTOR ( 'NONE', #12630, 1000.000000000000000 ) ;
#10013=CARTESIAN_POINT ( 'NONE',  ( -2.899999929817000055, 18.99999992981999952, -2.312669444528000281E-07 ) ) ;
#10014=AXIS2_PLACEMENT_3D ( 'NONE', #13766, #10521, #13894 ) ;
#10016=CARTESIAN_POINT ( 'NONE',  ( -1.533591067958279819, 27.72982077893267316, 1.536412323194911833 ) ) ;
#10018=DIRECTION ( 'NONE',  ( 0.000000000000000000, 1.000000000000000000, 0.000000000000000000 ) ) ;
#10019=ORIENTED_EDGE ( 'NONE', *, *, #4022, .T. ) ;
#10021=EDGE_CURVE ( 'NONE', #23288, #16360, #1551, .T. ) ;
#10023=ADVANCED_FACE ( 'NONE', ( #21729 ), #13509, .T. ) ;
#10024=AXIS2_PLACEMENT_3D ( 'NONE', #5642, #7706, #3956 ) ;
#10031=CARTESIAN_POINT ( 'NONE',  ( 1.536366799937295413, 26.91753006952333749, 1.999167105995444338 ) ) ;
#10033=AXIS2_PLACEMENT_3D ( 'NONE', #11932, #15542, #22930 ) ;
#10034=CARTESIAN_POINT ( 'NONE',  ( 0.000000000000000000, 19.00000000000000000, 0.000000000000000000 ) ) ;
#10037=CARTESIAN_POINT ( 'NONE',  ( -1.483218624018999954, 26.47956776952000268, 2.219793368323999871 ) ) ;
#10040=CARTESIAN_POINT ( 'NONE',  ( 2.145115102489369097, 28.98698980757362875, 0.2846114639472765440 ) ) ;
#10043=VECTOR ( 'NONE', #22675, 999.9999999999998863 ) ;
#10044=ORIENTED_EDGE ( 'NONE', *, *, #13758, .T. ) ;
#10045=CARTESIAN_POINT ( 'NONE',  ( 0.5097591796037457268, 26.26046041277498233, 2.099534046982708180 ) ) ;
#10049=AXIS2_PLACEMENT_3D ( 'NONE', #133, #14788, #18784 ) ;
#10054=ORIENTED_EDGE ( 'NONE', *, *, #20745, .T. ) ;
#10057=CARTESIAN_POINT ( 'NONE',  ( -2.465106068310999987, 25.02935756624999541, 1.140263770482999872 ) ) ;
#10061=DIRECTION ( 'NONE',  ( 0.000000000000000000, 1.000000000000000000, 0.000000000000000000 ) ) ;
#10066=CARTESIAN_POINT ( 'NONE',  ( 1.536366799937286087, 29.55086340285667035, -1.999167105995451221 ) ) ;
#10067=ORIENTED_EDGE ( 'NONE', *, *, #20310, .T. ) ;
#10068=FACE_OUTER_BOUND ( 'NONE', #5335, .T. ) ;
#10070=ORIENTED_EDGE ( 'NONE', *, *, #314, .F. ) ;
#10071=CARTESIAN_POINT ( 'NONE',  ( 0.000000000000000000, 18.10000000000000142, 0.000000000000000000 ) ) ;
#10072=CARTESIAN_POINT ( 'NONE',  ( 1.999167105995460769, 28.55086340285666324, 1.536366799937272765 ) ) ;
#10074=CARTESIAN_POINT ( 'NONE',  ( -2.500000000000000000, 18.50000000000000000, 0.000000000000000000 ) ) ;
#10076=CARTESIAN_POINT ( 'NONE',  ( 2.322750540216000026, 26.09419433610000283, 1.687576972922000040 ) ) ;
#10084=CARTESIAN_POINT ( 'NONE',  ( 0.000000000000000000, 19.04999994433000055, 0.000000000000000000 ) ) ;
#10087=EDGE_CURVE ( 'NONE', #18064, #22068, #9985, .T. ) ;
#10088=CARTESIAN_POINT ( 'NONE',  ( -1.933408640761000052, 29.94449886025999774, -1.346733530429999881 ) ) ;
#10091=CARTESIAN_POINT ( 'NONE',  ( -0.5972122245493562964, 29.56816721632387512, 2.075699671229644050 ) ) ;
#10093=CARTESIAN_POINT ( 'NONE',  ( 2.116385362157999772, 23.95644821291999804, 0.5468322576709999661 ) ) ;
#10095=ORIENTED_EDGE ( 'NONE', *, *, #973, .T. ) ;
#10096=CARTESIAN_POINT ( 'NONE',  ( -1.016515298417790758, 24.56303148589417518, -2.109700942474796115 ) ) ;
#10100=CARTESIAN_POINT ( 'NONE',  ( 1.699986957659999964, 9.000014576061998284, -0.8485216275457999613 ) ) ;
#10102=VERTEX_POINT ( 'NONE', #22422 ) ;
#10104=CARTESIAN_POINT ( 'NONE',  ( -1.536366799937290084, 27.08333333333333570, -1.999167105995448113 ) ) ;
#10105=FACE_OUTER_BOUND ( 'NONE', #7316, .T. ) ;
#10106=EDGE_LOOP ( 'NONE', ( #918, #9202, #445, #17837, #9491 ) ) ;
#10107=DIRECTION ( 'NONE',  ( 0.000000000000000000, 1.000000000000000000, 0.000000000000000000 ) ) ;
#10110=CARTESIAN_POINT ( 'NONE',  ( 4.000000000000000000, 26.29977277844473349, 1.897803675662218970 ) ) ;
#10112=CARTESIAN_POINT ( 'NONE',  ( 0.000000000000000000, 31.00000000000000000, 0.000000000000000000 ) ) ;
#10116=CARTESIAN_POINT ( 'NONE',  ( 2.267779804951839839, 26.36777980495183726, 5.387954023152814032E-08 ) ) ;
#10119=CARTESIAN_POINT ( 'NONE',  ( -1.595082304731897826, 30.10957549855011450, -1.456253076787439094 ) ) ;
#10127=EDGE_CURVE ( 'NONE', #15019, #3493, #17786, .T. ) ;
#10133=CARTESIAN_POINT ( 'NONE',  ( -1.094146582940317858, 27.49559246110014854, -1.910274834462101223 ) ) ;
#10142=EDGE_CURVE ( 'NONE', #20600, #6219, #3474, .T. ) ;
#10147=DIRECTION ( 'NONE',  ( 0.000000000000000000, 0.000000000000000000, -1.000000000000000000 ) ) ;
#10149=DIRECTION ( 'NONE',  ( -1.000000000000000000, 0.000000000000000000, 0.000000000000000000 ) ) ;
#10153=CARTESIAN_POINT ( 'NONE',  ( 0.05636985319968000618, 27.46250240009999999, 2.870524099806999629 ) ) ;
#10156=CARTESIAN_POINT ( 'NONE',  ( 2.649085689637680652, 26.47444252552741872, 3.089351817498230623 ) ) ;
#10166=CARTESIAN_POINT ( 'NONE',  ( -2.000000000000000000, 24.50000000000000000, -3.464101615137999968 ) ) ;
#10167=FACE_BOUND ( 'NONE', #10859, .T. ) ;
#10168=CARTESIAN_POINT ( 'NONE',  ( 2.434931691670788823, 27.06753006952333607, -0.6543697108982007293 ) ) ;
#10171=CARTESIAN_POINT ( 'NONE',  ( 0.3272492347489455167, 27.41666666666666075, 2.499999999999998668 ) ) ;
#10174=CARTESIAN_POINT ( 'NONE',  ( -0.3310328303844999875, 30.17125647670999911, -2.511084930423000294 ) ) ;
#10177=ORIENTED_EDGE ( 'NONE', *, *, #18938, .T. ) ;
#10179=CARTESIAN_POINT ( 'NONE',  ( 2.590247180112999814, 28.61723979505000059, -0.9106673404492000579 ) ) ;
#10180=CARTESIAN_POINT ( 'NONE',  ( -2.000000000000000000, 18.72912878474779319, -6.650110356573455395E-11 ) ) ;
#10189=EDGE_LOOP ( 'NONE', ( #404, #22020, #8779, #11794 ) ) ;
#10190=CARTESIAN_POINT ( 'NONE',  ( -1.703175425154000111, 25.54551418205999980, -2.142696604598000043 ) ) ;
#10195=CARTESIAN_POINT ( 'NONE',  ( 2.870524099806999629, 26.97169433610000411, 0.05636985319957999591 ) ) ;
#10197=CARTESIAN_POINT ( 'NONE',  ( -2.500000000000000444, 29.85086340285667461, 0.3272492347489422415 ) ) ;
#10199=DIRECTION ( 'NONE',  ( 0.000000000000000000, -1.000000000000000000, 0.000000000000000000 ) ) ;
#10203=CARTESIAN_POINT ( 'NONE',  ( 2.500000000000000000, 18.50000000000000000, 0.000000000000000000 ) ) ;
#10209=CARTESIAN_POINT ( 'NONE',  ( -4.750000000000000000, 20.10000000000000142, 0.000000000000000000 ) ) ;
#10211=CARTESIAN_POINT ( 'NONE',  ( -2.071762217469759193, 29.44039273301211423, 0.6102428019939168946 ) ) ;
#10213=CARTESIAN_POINT ( 'NONE',  ( 1.521291192730000130, 23.88665044741999921, 1.569645106012999891 ) ) ;
#10219=CARTESIAN_POINT ( 'NONE',  ( 0.000000000000000000, 17.00000000000000000, -3.099999999999986766 ) ) ;
#10223=EDGE_LOOP ( 'NONE', ( #10687, #20533, #17187, #3811 ) ) ;
#10224=CARTESIAN_POINT ( 'NONE',  ( 1.414030196417156471E-05, 28.49937488120688656, 2.386519462589231200 ) ) ;
#10226=DIRECTION ( 'NONE',  ( -1.000000000000000000, 0.000000000000000000, 0.000000000000000000 ) ) ;
#10240=FACE_OUTER_BOUND ( 'NONE', #160, .T. ) ;
#10241=CARTESIAN_POINT ( 'NONE',  ( -2.159905846019499531, 30.20377729254098753, 0.001675619632035371676 ) ) ;
#10242=ORIENTED_EDGE ( 'NONE', *, *, #9075, .F. ) ;
#10246=AXIS2_PLACEMENT_3D ( 'NONE', #11789, #3078, #19292 ) ;
#10248=DIRECTION ( 'NONE',  ( 0.000000000000000000, 1.000000000000000000, 0.000000000000000000 ) ) ;
#10250=VERTEX_POINT ( 'NONE', #248 ) ;
#10254=TOROIDAL_SURFACE ( 'NONE', #7931, 1.600000000000000089, 0.1000000000000000056 ) ;
#10255=CARTESIAN_POINT ( 'NONE',  ( 2.110282791597058782, 26.46005674015626496, -0.5113919139037653716 ) ) ;
#10258=ORIENTED_EDGE ( 'NONE', *, *, #195, .F. ) ;
#10259=FACE_OUTER_BOUND ( 'NONE', #11557, .T. ) ;
#10266=CARTESIAN_POINT ( 'NONE',  ( -0.4920218899694317471, 28.43348844177958767, -2.148916380170569074 ) ) ;
#10268=CARTESIAN_POINT ( 'NONE',  ( 0.000000000000000000, 9.000000000000000000, 0.000000000000000000 ) ) ;
#10271=CARTESIAN_POINT ( 'NONE',  ( 0.04450989311249999719, 27.14619850837999948, 2.266578917753999889 ) ) ;
#10272=ADVANCED_FACE ( 'NONE', ( #7406 ), #4643, .F. ) ;
#10275=CARTESIAN_POINT ( 'NONE',  ( -2.437731244915000151, 27.80187716036000367, -0.2400955718763000124 ) ) ;
#10276=CARTESIAN_POINT ( 'NONE',  ( 0.000000000000000000, 18.89999999999999858, 0.000000000000000000 ) ) ;
#10288=VECTOR ( 'NONE', #15773, 1000.000000000000000 ) ;
#10292=ADVANCED_FACE ( 'NONE', ( #9704 ), #15255, .T. ) ;
#10294=CARTESIAN_POINT ( 'NONE',  ( 1.910771868463999823, 30.72761905088000134, -1.353836472813999992 ) ) ;
#10299=CARTESIAN_POINT ( 'NONE',  ( 0.000000000000000000, 24.65000000000000213, -4.309401076758999416 ) ) ;
#10300=DIRECTION ( 'NONE',  ( 0.000000000000000000, -1.000000000000000000, 0.000000000000000000 ) ) ;
#10301=DIRECTION ( 'NONE',  ( 1.000000000000000000, 0.000000000000000000, 0.000000000000000000 ) ) ;
#10303=CARTESIAN_POINT ( 'NONE',  ( -3.000000000000000000, 22.00000000000000000, 0.000000000000000000 ) ) ;
#10310=CIRCLE ( 'NONE', #19599, 4.724999999999999645 ) ;
#10311=VERTEX_POINT ( 'NONE', #9234 ) ;
#10312=CARTESIAN_POINT ( 'NONE',  ( 1.952358158081999973, 24.36111943012999959, 1.918398575790000171 ) ) ;
#10320=AXIS2_PLACEMENT_3D ( 'NONE', #22095, #23676, #8797 ) ;
#10321=VERTEX_POINT ( 'NONE', #23596 ) ;
#10322=CARTESIAN_POINT ( 'NONE',  ( 0.000000000000000000, 24.39999999221199900, 0.000000000000000000 ) ) ;
#10323=LINE ( 'NONE', #17339, #91 ) ;
#10330=DIRECTION ( 'NONE',  ( 0.000000000000000000, 0.000000000000000000, -1.000000000000000000 ) ) ;
#10332=CARTESIAN_POINT ( 'NONE',  ( -1.399999855176999874, 6.999999855177000185, 5.700011345002000930E-07 ) ) ;
#10333=CARTESIAN_POINT ( 'NONE',  ( 2.297600999428000002, 28.79350652947999833, 0.5222559440399000552 ) ) ;
#10336=EDGE_LOOP ( 'NONE', ( #3670, #11265 ) ) ;
#10337=FACE_OUTER_BOUND ( 'NONE', #20142, .T. ) ;
#10338=CARTESIAN_POINT ( 'NONE',  ( -1.856171584524297202, 29.47206855671609205, 1.104583064503529277 ) ) ;
#10341=CARTESIAN_POINT ( 'NONE',  ( -1.368902347425000166, 23.50118614385000271, -1.908701113743999978 ) ) ;
#10343=VECTOR ( 'NONE', #11145, 1000.000000000000114 ) ;
#10345=B_SPLINE_SURFACE_WITH_KNOTS ( 'NONE', 3, 3, ( 
 ( #16117, #5581, #21826, #16708, #5239, #7272, #9454, #3541, #16474, #22059, #20009, #3430, #12624, #9336, #9218, #16597, #18205, #10814, #12850, #8, #5468, #1606, #21940, #1712, #23865, #8991, #120, #16362, #9102, #14431, #14664, #11280, #23751, #13081, #7155 ),
 ( #20246, #3652, #14545, #5350, #12739, #20133, #1950, #11038, #10924, #14890, #18421, #18311, #1832, #7391, #14774, #22170, #12963, #16828, #20359, #3768, #11156, #18542, #7507, #22281, #5696, #20481, #3889, #18657, #2063, #7048, #2302, #8122, #5926, #19252, #17311 ),
 ( #19121, #20952, #22517, #22872, #2176, #13198, #9569, #15009, #2534, #15238, #20591, #15486, #11635, #13310, #18890, #16953, #19003, #17069, #20831, #2663, #7635, #4245, #4357, #18766, #712, #4000, #9688, #9926, #585, #2414, #6289, #11749, #467, #13671, #20708 ),
 ( #9805, #17188, #21065, #4479, #4117, #11868, #354, #10057, #22752, #15122, #13554, #232, #22407, #5816, #22631, #7989, #11396, #15361, #7754, #11515, #7870, #6171, #6042, #13431, #23236, #19380, #21683, #15847, #15605, #5095, #19749, #2791, #3034, #4731, #13792 ) ),
 .UNSPECIFIED., .F., .F., .F.,
 ( 4, 4 ),
 ( 4, 1, 1, 1, 1, 1, 1, 1, 1, 1, 1, 1, 1, 1, 1, 1, 1, 1, 1, 1, 1, 1, 1, 1, 1, 1, 1, 1, 1, 1, 1, 1, 4 ),
 ( -0.3056682515952000023, 1.305668251594999996 ),
 ( -0.01313663885146000056, 0.008210399282161001330, 0.02955743741577999961, 0.05090447554939999536, 0.07225151368301999111, 0.09359855181663999379, 0.1149455899503000061, 0.1362926280838999971, 0.1576396662175000019, 0.1789867043511000066, 0.2003337424846999837, 0.2216807806182999885, 0.2430278187519999966, 0.2643748568855999737, 0.2857218950191999784, 0.3070689331527999832, 0.3284159712863999880, 0.3497630094201000239, 0.3711100475536999732, 0.3924570856872999780, 0.4138041238209000383, 0.4351511619544999876, 0.4564982000882000235, 0.4778452382218000283, 0.4991922763553999776, 0.5205393144889999268, 0.5418863526225999871, 0.5632333907561999364, 0.5845804288899000278, 0.6059274670234999771, 0.6272745051571000374, 0.6486215432906999867, 0.6699685814243000470 ),
 .UNSPECIFIED. ) ;
#10352=ORIENTED_EDGE ( 'NONE', *, *, #23581, .T. ) ;
#10353=DIRECTION ( 'NONE',  ( 0.000000000000000000, -1.000000000000000000, 0.000000000000000000 ) ) ;
#10354=DIRECTION ( 'NONE',  ( 0.000000000000000000, -1.000000000000000000, 0.000000000000000000 ) ) ;
#10361=AXIS2_PLACEMENT_3D ( 'NONE', #9444, #9560, #5916 ) ;
#10367=CARTESIAN_POINT ( 'NONE',  ( -1.992339167965410773, 30.25593788753863578, 0.8606820921618728581 ) ) ;
#10371=CARTESIAN_POINT ( 'NONE',  ( 0.6543697108982093891, 27.66753006952333038, 2.434931691670787490 ) ) ;
#10372=ORIENTED_EDGE ( 'NONE', *, *, #792, .T. ) ;
#10381=CARTESIAN_POINT ( 'NONE',  ( 1.997037326419333070, 27.17506949985559217, 0.9200039467642276980 ) ) ;
#10383=AXIS2_PLACEMENT_3D ( 'NONE', #22757, #6294, #13676 ) ;
#10385=EDGE_LOOP ( 'NONE', ( #21477, #9035, #18753, #15813 ) ) ;
#10392=CARTESIAN_POINT ( 'NONE',  ( 0.4078570127197936324, 28.38048613814547494, -2.134782185931087373 ) ) ;
#10393=VECTOR ( 'NONE', #16260, 1000.000000000000227 ) ;
#10394=DIRECTION ( 'NONE',  ( 0.000000000000000000, -1.000000000000000000, 0.000000000000000000 ) ) ;
#10397=ORIENTED_EDGE ( 'NONE', *, *, #12390, .F. ) ;
#10399=CARTESIAN_POINT ( 'NONE',  ( -1.932944458086000017, 26.07369850838000147, -1.184521108792000010 ) ) ;
#10403=CONICAL_SURFACE ( 'NONE', #3825, 3.049999825846000157, 0.7853981633972997312 ) ;
#10406=ORIENTED_EDGE ( 'NONE', *, *, #22848, .T. ) ;
#10407=DIRECTION ( 'NONE',  ( 0.000000000000000000, -1.000000000000000000, 0.000000000000000000 ) ) ;
#10409=EDGE_CURVE ( 'NONE', #18970, #19401, #18266, .T. ) ;
#10411=AXIS2_PLACEMENT_3D ( 'NONE', #9409, #11797, #16549 ) ;
#10417=DIRECTION ( 'NONE',  ( 1.000000000000000000, 0.000000000000000000, 0.000000000000000000 ) ) ;
#10421=CARTESIAN_POINT ( 'NONE',  ( 2.354726837831999653, 29.90653759481000051, 0.9329478987628000430 ) ) ;
#10422=CARTESIAN_POINT ( 'NONE',  ( 4.000000000000000000, 24.50000000000000000, 2.309401076759000304 ) ) ;
#10433=CIRCLE ( 'NONE', #338, 0.5500000000000001554 ) ;
#10434=DIRECTION ( 'NONE',  ( 0.000000000000000000, -1.000000000000000000, 0.000000000000000000 ) ) ;
#10435=CYLINDRICAL_SURFACE ( 'NONE', #9634, 3.000000000000000000 ) ;
#10436=ORIENTED_EDGE ( 'NONE', *, *, #7761, .T. ) ;
#10437=CARTESIAN_POINT ( 'NONE',  ( -2.500000000000000000, 18.50000000000000000, 0.000000000000000000 ) ) ;
#10440=AXIS2_PLACEMENT_3D ( 'NONE', #5027, #20262, #11053 ) ;
#10441=CARTESIAN_POINT ( 'NONE',  ( -0.9641736524564000765, 24.60403619718000101, -2.355488194562000093 ) ) ;
#10443=EDGE_CURVE ( 'NONE', #889, #12315, #750, .T. ) ;
#10452=CARTESIAN_POINT ( 'NONE',  ( -0.4031052425579070286, 26.23085661886908326, 2.096221175781856072 ) ) ;
#10454=ORIENTED_EDGE ( 'NONE', *, *, #23537, .T. ) ;
#10458=CARTESIAN_POINT ( 'NONE',  ( 4.000000000000000000, 24.50000000000000000, 0.000000000000000000 ) ) ;
#10460=DIRECTION ( 'NONE',  ( -0.7071067811905932254, -0.7071067811824932603, -1.099460899159990341E-07 ) ) ;
#10461=CARTESIAN_POINT ( 'NONE',  ( 3.099999776787000005, 20.00000022320933013, 5.570936504208000122E-07 ) ) ;
#10466=CARTESIAN_POINT ( 'NONE',  ( -1.646340102500975622, 29.31421555423750291, -1.398084700589298457 ) ) ;
#10468=FACE_OUTER_BOUND ( 'NONE', #10675, .T. ) ;
#10470=VECTOR ( 'NONE', #17258, 1000.000000000000114 ) ;
#10475=EDGE_CURVE ( 'NONE', #16783, #8124, #5035, .T. ) ;
#10480=FACE_OUTER_BOUND ( 'NONE', #8918, .T. ) ;
#10483=DIRECTION ( 'NONE',  ( 0.000000000000000000, 1.000000000000000000, 0.000000000000000000 ) ) ;
#10486=DIRECTION ( 'NONE',  ( 0.000000000000000000, 1.000000000000000000, 0.000000000000000000 ) ) ;
#10490=AXIS2_PLACEMENT_3D ( 'NONE', #1196, #16199, #21305 ) ;
#10493=CARTESIAN_POINT ( 'NONE',  ( -1.921593888566249131, 30.14343111292356880, -0.9863569469920862032 ) ) ;
#10495=CARTESIAN_POINT ( 'NONE',  ( -1.439810120399000137, 25.29894750743999765, -1.839121480912999873 ) ) ;
#10498=CARTESIAN_POINT ( 'NONE',  ( -2.143277222256999792, 23.64327722226000006, 4.118360636503000477E-13 ) ) ;
#10499=ORIENTED_EDGE ( 'NONE', *, *, #7194, .T. ) ;
#10500=FACE_OUTER_BOUND ( 'NONE', #10106, .T. ) ;
#10502=B_SPLINE_CURVE_WITH_KNOTS ( 'NONE', 3,
 ( #7141, #1347, #18189, #8973, #23502, #1696, #14530, #5109, #12606, #14305 ),
 .UNSPECIFIED., .F., .F.,
 ( 4, 1, 1, 2, 2, 4 ),
 ( 0.000000000000000000, 0.2499999999999989453, 0.3749999999999988343, 0.4374999999999989453, 0.4999999999999990008, 1.000000000000000000 ),
 .UNSPECIFIED. ) ;
#10504=ORIENTED_EDGE ( 'NONE', *, *, #17973, .T. ) ;
#10507=ORIENTED_EDGE ( 'NONE', *, *, #9354, .T. ) ;
#10508=B_SPLINE_CURVE_WITH_KNOTS ( 'NONE', 3,
 ( #22251, #5667, #18392, #23960, #7364, #16799, #22145, #4330, #15094, #17416 ),
 .UNSPECIFIED., .F., .F.,
 ( 4, 2, 2, 2, 4 ),
 ( 0.000000000000000000, 0.2499999999999998335, 0.4999999999999996669, 0.7499999999999997780, 1.000000000000000000 ),
 .UNSPECIFIED. ) ;
#10513=CARTESIAN_POINT ( 'NONE',  ( 2.351381211264389925, 26.74999873450825660, 0.9808036171101988110 ) ) ;
#10519=CARTESIAN_POINT ( 'NONE',  ( -1.315032585339712234, 27.12168142538949311, 1.729448944228739071 ) ) ;
#10521=DIRECTION ( 'NONE',  ( 0.000000000000000000, -1.000000000000000000, 0.000000000000000000 ) ) ;
#10522=ORIENTED_EDGE ( 'NONE', *, *, #18219, .T. ) ;
#10525=CARTESIAN_POINT ( 'NONE',  ( 2.266578917753999889, 27.34119850838000332, 0.04450989311242999763 ) ) ;
#10526=CARTESIAN_POINT ( 'NONE',  ( 0.000000000000000000, 23.75000000000000000, 0.000000000000000000 ) ) ;
#10527=B_SPLINE_CURVE_WITH_KNOTS ( 'NONE', 3,
 ( #19437, #15656, #22808, #9863, #17248, #13606, #4537, #13489, #2847, #18946 ),
 .UNSPECIFIED., .F., .F.,
 ( 4, 1, 1, 2, 2, 4 ),
 ( 0.000000000000000000, 0.2499999999999989453, 0.3749999999999988343, 0.4374999999999989453, 0.4999999999999990008, 1.000000000000000000 ),
 .UNSPECIFIED. ) ;
#10540=CARTESIAN_POINT ( 'NONE',  ( 2.434931691670788823, 28.43333333333332646, -0.6543697108982009514 ) ) ;
#10541=CARTESIAN_POINT ( 'NONE',  ( 2.309445831590999809, 30.70069424050999984, 1.039994766367999812 ) ) ;
#10545=FACE_OUTER_BOUND ( 'NONE', #8003, .T. ) ;
#10547=CARTESIAN_POINT ( 'NONE',  ( 0.000000000000000000, 26.35000000000000142, 0.000000000000000000 ) ) ;
#10548=EDGE_CURVE ( 'NONE', #2693, #19347, #17395, .T. ) ;
#10552=CARTESIAN_POINT ( 'NONE',  ( 0.000000000000000000, 20.10000000000000142, 0.000000000000000000 ) ) ;
#10553=DIRECTION ( 'NONE',  ( 1.000000000000000000, 0.000000000000000000, 0.000000000000000000 ) ) ;
#10558=CARTESIAN_POINT ( 'NONE',  ( 1.044258846366000082, 25.30073899244000302, -2.321094337967000154 ) ) ;
#10559=FACE_OUTER_BOUND ( 'NONE', #18346, .T. ) ;
#10563=CARTESIAN_POINT ( 'NONE',  ( 1.999167105995449889, 27.68333333333333357, -1.536366799937288086 ) ) ;
#10565=CARTESIAN_POINT ( 'NONE',  ( -1.686459531786994148, 23.77333333333334764, -1.586187310772563697 ) ) ;
#10574=DIRECTION ( 'NONE',  ( 0.000000000000000000, 1.000000000000000000, 0.000000000000000000 ) ) ;
#10575=CARTESIAN_POINT ( 'NONE',  ( -0.8039427155937000080, 29.93886808515000197, -2.013420029665999866 ) ) ;
#10576=EDGE_CURVE ( 'NONE', #3964, #20732, #3491, .T. ) ;
#10583=CARTESIAN_POINT ( 'NONE',  ( -0.6543697108982037269, 29.43333333333334068, -2.434931691670788823 ) ) ;
#10584=CARTESIAN_POINT ( 'NONE',  ( 0.000000000000000000, -1.550000000000000044, 0.000000000000000000 ) ) ;
#10592=CARTESIAN_POINT ( 'NONE',  ( 2.467893978438000069, 27.18256359724000149, 0.04846321314148000631 ) ) ;
#10595=EDGE_LOOP ( 'NONE', ( #4604, #971, #16486, #19649, #11900 ) ) ;
#10596=DIRECTION ( 'NONE',  ( 0.000000000000000000, -1.000000000000000000, 0.000000000000000000 ) ) ;
#10607=CARTESIAN_POINT ( 'NONE',  ( -2.009419033758999884, 29.34560438995000098, -1.204887936538999949 ) ) ;
#10609=EDGE_CURVE ( 'NONE', #13196, #3216, #16328, .T. ) ;
#10610=CARTESIAN_POINT ( 'NONE',  ( 1.346994075275769864, 29.91795814813315957, -1.688431679418926912 ) ) ;
#10626=DIRECTION ( 'NONE',  ( 0.000000000000000000, -1.000000000000000000, 0.000000000000000000 ) ) ;
#10633=EDGE_CURVE ( 'NONE', #19401, #1045, #20120, .T. ) ;
#10635=CARTESIAN_POINT ( 'NONE',  ( -1.015900767931854354, 27.66495503860647887, -1.959239081289818385 ) ) ;
#10638=ORIENTED_EDGE ( 'NONE', *, *, #8515, .T. ) ;
#10641=CARTESIAN_POINT ( 'NONE',  ( -0.5696873960579796892, 24.75754694542404621, 2.081016722391946239 ) ) ;
#10642=DIRECTION ( 'NONE',  ( 0.8947368421052591669, 0.000000000000000000, 0.4465937565388801156 ) ) ;
#10643=FACE_OUTER_BOUND ( 'NONE', #8339, .T. ) ;
#10644=AXIS2_PLACEMENT_3D ( 'NONE', #10437, #17827, #6786 ) ;
#10647=CYLINDRICAL_SURFACE ( 'NONE', #5296, 2.500000000000000000 ) ;
#10652=CARTESIAN_POINT ( 'NONE',  ( 0.000000000000000000, -1.550000000000000044, 0.000000000000000000 ) ) ;
#10657=CARTESIAN_POINT ( 'NONE',  ( 1.999167105995449889, 28.48333333333334139, -1.536366799937288086 ) ) ;
#10658=CARTESIAN_POINT ( 'NONE',  ( -0.9058703646527999087, 29.70799843338999935, 2.365275701699999900 ) ) ;
#10662=ORIENTED_EDGE ( 'NONE', *, *, #18855, .T. ) ;
#10663=DIRECTION ( 'NONE',  ( 1.000000000000000000, 0.000000000000000000, 0.000000000000000000 ) ) ;
#10668=CARTESIAN_POINT ( 'NONE',  ( -2.327192509895188000, 24.50639765414752347, 3.274853329251978362 ) ) ;
#10673=CARTESIAN_POINT ( 'NONE',  ( 2.204045812699286344, 30.65849365117777481, 0.9160123963385377044 ) ) ;
#10674=CARTESIAN_POINT ( 'NONE',  ( 1.724026015792058830, 12.96510883726990038, 1.060380412480157686 ) ) ;
#10675=EDGE_LOOP ( 'NONE', ( #2330, #12976, #21051 ) ) ;
#10676=CARTESIAN_POINT ( 'NONE',  ( 2.417770443646000356, 24.39502535860999899, -0.7951990710235999904 ) ) ;
#10678=AXIS2_PLACEMENT_3D ( 'NONE', #1391, #10486, #16145 ) ;
#10686=CYLINDRICAL_SURFACE ( 'NONE', #9825, 3.000000000000000000 ) ;
#10687=ORIENTED_EDGE ( 'NONE', *, *, #8171, .T. ) ;
#10689=DIRECTION ( 'NONE',  ( 0.000000000000000000, 1.000000000000000000, 0.000000000000000000 ) ) ;
#10693=CARTESIAN_POINT ( 'NONE',  ( -2.146043429168999594, 30.87238359794000075, -0.3073092761724999789 ) ) ;
#10698=CARTESIAN_POINT ( 'NONE',  ( -1.317207735313150607, 26.42011321481863106, 1.933357710794660012 ) ) ;
#10701=CARTESIAN_POINT ( 'NONE',  ( -2.500000000000000444, 29.58333333333333925, -0.3272492347489320275 ) ) ;
#10703=ORIENTED_EDGE ( 'NONE', *, *, #15327, .F. ) ;
#10705=DIRECTION ( 'NONE',  ( 0.000000000000000000, -1.000000000000000000, 0.000000000000000000 ) ) ;
#10707=B_SPLINE_CURVE_WITH_KNOTS ( 'NONE', 3,
 ( #9994, #655, #19447, #899, #13986, #11694, #21267, #15550, #19068, #11942 ),
 .UNSPECIFIED., .F., .F.,
 ( 4, 1, 1, 2, 2, 4 ),
 ( 0.000000000000000000, 0.2499999999999969469, 0.3749999999999960032, 0.4374999999999962252, 0.4999999999999963363, 1.000000000000000000 ),
 .UNSPECIFIED. ) ;
#10715=VERTEX_POINT ( 'NONE', #7161 ) ;
#10721=CARTESIAN_POINT ( 'NONE',  ( -1.052033064323999900, 29.27366736927999824, -2.093500996029999506 ) ) ;
#10724=ADVANCED_FACE ( 'NONE', ( #12969 ), #3896, .T. ) ;
#10725=CARTESIAN_POINT ( 'NONE',  ( 0.5984287563357140183, 29.96812122538106138, -2.076360886265356420 ) ) ;
#10726=ORIENTED_EDGE ( 'NONE', *, *, #17121, .F. ) ;
#10730=CIRCLE ( 'NONE', #13801, 2.000000000000000000 ) ;
#10733=CARTESIAN_POINT ( 'NONE',  ( 0.000000000000000000, 26.50000000000000355, 0.000000000000000000 ) ) ;
#10739=ORIENTED_EDGE ( 'NONE', *, *, #21364, .T. ) ;
#10741=CARTESIAN_POINT ( 'NONE',  ( 2.072318791391040360, 26.38608990294597945, 0.7342227717574281165 ) ) ;
#10744=CIRCLE ( 'NONE', #16132, 2.399999999999999911 ) ;
#10745=CARTESIAN_POINT ( 'NONE',  ( -0.006385721344668345532, 26.59999493803301007, 2.547730079617255505 ) ) ;
#10747=AXIS2_PLACEMENT_3D ( 'NONE', #2626, #10018, #9653 ) ;
#10749=CARTESIAN_POINT ( 'NONE',  ( 0.000000000000000000, 15.00000000000000000, 0.000000000000000000 ) ) ;
#10751=CARTESIAN_POINT ( 'NONE',  ( 1.053167012274741410, 27.26743776069429259, 1.938163248592302379 ) ) ;
#10753=CARTESIAN_POINT ( 'NONE',  ( 2.108296854627000005, 27.75500240010000041, -1.948889566018999986 ) ) ;
#10754=ADVANCED_FACE ( 'NONE', ( #14552 ), #15791, .T. ) ;
#10757=EDGE_CURVE ( 'NONE', #8812, #23948, #20139, .T. ) ;
#10759=CARTESIAN_POINT ( 'NONE',  ( 0.000000000000000000, -1.550000000000000044, 0.000000000000000000 ) ) ;
#10760=CARTESIAN_POINT ( 'NONE',  ( 0.1334610483750000021, 27.53619850838000360, -2.263084017374999757 ) ) ;
#10761=CIRCLE ( 'NONE', #2617, 4.750000000000000000 ) ;
#10763=LINE ( 'NONE', #14615, #21892 ) ;
#10764=CARTESIAN_POINT ( 'NONE',  ( -1.485816803342000281, 27.72271896306000016, -1.739667959131000030 ) ) ;
#10771=EDGE_CURVE ( 'NONE', #6636, #23948, #3059, .T. ) ;
#10772=CARTESIAN_POINT ( 'NONE',  ( 1.677026364909826706, 30.52491814567345685, -1.541694782284209753 ) ) ;
#10774=CARTESIAN_POINT ( 'NONE',  ( 1.536366799937312067, 24.28333333333333854, 1.999167105995431237 ) ) ;
#10780=CARTESIAN_POINT ( 'NONE',  ( -1.536366799937282313, 29.15086340285666822, 1.999167105995454552 ) ) ;
#10781=CARTESIAN_POINT ( 'NONE',  ( -0.3786279377524999767, 29.16623056986999885, -2.117165371715000077 ) ) ;
#10784=ORIENTED_EDGE ( 'NONE', *, *, #9505, .F. ) ;
#10785=CARTESIAN_POINT ( 'NONE',  ( -2.949999999999999734, 24.49999999999999645, 0.000000000000000000 ) ) ;
#10787=VECTOR ( 'NONE', #11492, 1000.000000000000114 ) ;
#10788=CARTESIAN_POINT ( 'NONE',  ( 1.999167105995462990, 29.11666666666667780, 1.536366799937272987 ) ) ;
#10796=CARTESIAN_POINT ( 'NONE',  ( 1.762815800531199351, 13.00000000278783219, 1.071352341330493507 ) ) ;
#10798=ORIENTED_EDGE ( 'NONE', *, *, #8358, .T. ) ;
#10799=CARTESIAN_POINT ( 'NONE',  ( 0.6222432282865000275, 24.18601452002999608, 2.467948282817999939 ) ) ;
#10800=DIRECTION ( 'NONE',  ( 0.000000000000000000, -1.000000000000000000, 0.000000000000000000 ) ) ;
#10803=DIRECTION ( 'NONE',  ( 0.000000000000000000, 1.000000000000000000, 0.000000000000000000 ) ) ;
#10805=CARTESIAN_POINT ( 'NONE',  ( 2.500000000000000000, 24.50000000000000000, 2.004655647840161273E-15 ) ) ;
#10806=VERTEX_POINT ( 'NONE', #20840 ) ;
#10807=DIRECTION ( 'NONE',  ( 0.000000000000000000, -1.000000000000000000, 0.000000000000000000 ) ) ;
#10808=B_SPLINE_CURVE_WITH_KNOTS ( 'NONE', 3,
 ( #23217, #4712, #10641, #13897, #17662, #1189, #11234, #22009, #14499, #3957, #18370, #11349, #3496, #9405, #7574, #9291, #13030, #21891, #10876, #7108, #22230, #9052 ),
 .UNSPECIFIED., .F., .F.,
 ( 4, 2, 2, 2, 2, 2, 2, 2, 2, 2, 4 ),
 ( 3.041894376390393310E-05, 0.0007972261352801803414, 0.001564033326796456912, 0.002330840518312733266, 0.002714244114070871444, 0.002905945911949940966, 0.003001796810889475076, 0.003013778173256916569, 0.003025759535624358062, 0.003049722260359241047, 0.003097647709829007018 ),
 .UNSPECIFIED. ) ;
#10809=CARTESIAN_POINT ( 'NONE',  ( -1.965891356465660378, 26.25632797282960951, 0.8861481259685903833 ) ) ;
#10811=ORIENTED_EDGE ( 'NONE', *, *, #10087, .T. ) ;
#10812=CLOSED_SHELL ( 'NONE', ( #16465, #18241, #5537, #5586, #8201, #11785, #20369, #9089, #11019, #15142, #21395, #7564, #718, #17256, #23641, #16340, #2984, #13564, #3526, #15894, #616, #19293, #21040, #2331, #2135, #12636, #7407, #14105, #21861, #10724, #6217, #6542, #365, #7445, #8675, #8078, #8319, #5258, #21105, #20772, #4050, #2285, #22583, #16653, #11796, #12064, #10900, #23696, #19852, #14217, #17824, #6151, #18268, #19426, #23726, #13787, #8494, #5559, #6356, #18701, #3785, #7758, #4250, #22700, #5359, #13192, #14128, #15715, #10754, #6690, #8809, #8554, #21383, #3753, #10292, #12681, #11187, #16792, #12415, #1303, #18096, #1124, #4382, #16740, #2602, #9533, #6274, #2434, #1077, #11662, #20938, #12926, #20418, #13320, #18837, #1302, #19444, #4060, #8366, #12045, #17468, #3949, #2845, #23174, #5100, #13949, #3181, #6589, #19867, #11632, #1381, #8039, #2777, #15017, #10023, #23292, #8898, #20815, #7471, #17387, #15547 ) ) ;
#10814=CARTESIAN_POINT ( 'NONE',  ( 0.2479243946193999959, 24.70525031395999704, 2.130229948954000196 ) ) ;
#10819=CARTESIAN_POINT ( 'NONE',  ( 1.596045994907000054, 30.58514805554999683, -1.467249313498999896 ) ) ;
#10825=CARTESIAN_POINT ( 'NONE',  ( -2.500000000000000000, 18.50000000000000000, 0.000000000000000000 ) ) ;
#10828=VECTOR ( 'NONE', #12716, 1000.000000000000000 ) ;
#10829=VERTEX_POINT ( 'NONE', #13438 ) ;
#10844=CARTESIAN_POINT ( 'NONE',  ( -1.499999883624000052, 7.099999883624000141, 4.580366260669000192E-07 ) ) ;
#10845=CARTESIAN_POINT ( 'NONE',  ( 1.682158182759999843, 30.71240778275999972, -1.630908591657999951 ) ) ;
#10846=AXIS2_PLACEMENT_3D ( 'NONE', #6379, #14139, #10147 ) ;
#10849=CARTESIAN_POINT ( 'NONE',  ( 2.101274614680348929, 29.83358767967074598, -0.5022599295738957581 ) ) ;
#10853=VERTEX_POINT ( 'NONE', #11641 ) ;
#10854=CARTESIAN_POINT ( 'NONE',  ( -2.070272442071251717, 23.66806414737387243, 0.6316710083233486595 ) ) ;
#10859=EDGE_LOOP ( 'NONE', ( #15973, #14056, #11929, #8712, #20174, #4502, #10784 ) ) ;
#10860=CARTESIAN_POINT ( 'NONE',  ( -0.6543697108981787469, 28.40086340285666822, 2.434931691670795484 ) ) ;
#10861=DIRECTION ( 'NONE',  ( 0.000000000000000000, 1.000000000000000000, 0.000000000000000000 ) ) ;
#10869=CARTESIAN_POINT ( 'NONE',  ( 1.625795695728253776, 26.51215493189252115, 1.441208665152567292 ) ) ;
#10870=CARTESIAN_POINT ( 'NONE',  ( -2.505154520421000175, 28.92500240009999857, 1.402946323589000066 ) ) ;
#10872=CARTESIAN_POINT ( 'NONE',  ( -0.2434897306343792311, 30.81781537185297992, -2.179389815440565314 ) ) ;
#10873=ORIENTED_EDGE ( 'NONE', *, *, #22973, .F. ) ;
#10874=CARTESIAN_POINT ( 'NONE',  ( -1.099193499486128101, 26.43562577624027199, -3.984182490697167900 ) ) ;
#10875=DIRECTION ( 'NONE',  ( 1.000000000000000000, 0.000000000000000000, 0.000000000000000000 ) ) ;
#10876=CARTESIAN_POINT ( 'NONE',  ( 1.667713432661086959, 24.74980862569434237, 1.357244015048324925 ) ) ;
#10877=CARTESIAN_POINT ( 'NONE',  ( -2.281391790424999844, 27.57614211382000136, -0.2246974795678000070 ) ) ;
#10885=EDGE_LOOP ( 'NONE', ( #1280, #21952, #11657, #2610 ) ) ;
#10887=EDGE_CURVE ( 'NONE', #12189, #19402, #18888, .T. ) ;
#10894=CARTESIAN_POINT ( 'NONE',  ( 1.696015419756000009, 29.82802777462000066, -1.322603481717999907 ) ) ;
#10900=ADVANCED_FACE ( 'NONE', ( #8967 ), #15402, .F. ) ;
#10901=CARTESIAN_POINT ( 'NONE',  ( 0.000000000000000000, 13.10000000000000142, -4.724999999995985966 ) ) ;
#10907=CARTESIAN_POINT ( 'NONE',  ( -1.240246564627624171, 29.28173428028883407, -1.768320821386759834 ) ) ;
#10909=VERTEX_POINT ( 'NONE', #22038 ) ;
#10910=CARTESIAN_POINT ( 'NONE',  ( 1.702244497849941807, 12.92465160051537332, 1.054166248807005157 ) ) ;
#10918=ORIENTED_EDGE ( 'NONE', *, *, #10142, .F. ) ;
#10920=DIRECTION ( 'NONE',  ( 0.000000000000000000, 1.000000000000000000, 0.000000000000000000 ) ) ;
#10921=CARTESIAN_POINT ( 'NONE',  ( 0.000000000000000000, 22.00000000000000000, 0.000000000000000000 ) ) ;
#10924=CARTESIAN_POINT ( 'NONE',  ( -2.329416328254999780, 25.17618571299000152, -0.1626863643163999895 ) ) ;
#10929=CARTESIAN_POINT ( 'NONE',  ( 2.112897800473000132, 28.86173480117000167, 0.4856074845446999855 ) ) ;
#10937=ORIENTED_EDGE ( 'NONE', *, *, #5722, .T. ) ;
#10947=ORIENTED_EDGE ( 'NONE', *, *, #4698, .F. ) ;
#10949=CONICAL_SURFACE ( 'NONE', #23702, 3.049999825846000157, 0.7853981633972997312 ) ;
#10950=CARTESIAN_POINT ( 'NONE',  ( 4.649999849441000421, 17.00000015055400127, -6.648422772555000414E-08 ) ) ;
#10955=CARTESIAN_POINT ( 'NONE',  ( 1.712616862212509972, 29.88731553013089126, -1.316065052317139772 ) ) ;
#10957=CARTESIAN_POINT ( 'NONE',  ( -0.5315530086984000535, 23.66540885998999855, -2.041217608508999692 ) ) ;
#10963=DIRECTION ( 'NONE',  ( -1.000000000000000000, 0.000000000000000000, 0.000000000000000000 ) ) ;
#10966=VERTEX_POINT ( 'NONE', #19986 ) ;
#10970=VECTOR ( 'NONE', #23775, 1000.000000000000114 ) ;
#10972=CARTESIAN_POINT ( 'NONE',  ( -2.102266727616999731, 23.66000000000000014, 0.4960590750638999569 ) ) ;
#10980=CARTESIAN_POINT ( 'NONE',  ( -0.7372999604405595653, 27.16143315320393015, 2.077662471664349475 ) ) ;
#10982=CARTESIAN_POINT ( 'NONE',  ( 1.838512823634357529, 30.67449951250407381, -1.138862448013022277 ) ) ;
#10983=VERTEX_POINT ( 'NONE', #23618 ) ;
#10987=EDGE_CURVE ( 'NONE', #14560, #4269, #11131, .T. ) ;
#10988=CARTESIAN_POINT ( 'NONE',  ( 1.196956196243999848, 25.94937716036000097, -2.137330684255000168 ) ) ;
#10989=CYLINDRICAL_SURFACE ( 'NONE', #5012, 1.500000000000000000 ) ;
#10991=ORIENTED_EDGE ( 'NONE', *, *, #17688, .T. ) ;
#10994=CARTESIAN_POINT ( 'NONE',  ( 0.2381761436251323971, 29.01693154808815223, -2.265505022230542398 ) ) ;
#10997=CARTESIAN_POINT ( 'NONE',  ( 4.000000000000000000, 24.50000000000000000, -2.309401076759000304 ) ) ;
#11001=CARTESIAN_POINT ( 'NONE',  ( -2.500000000000000444, 29.05086340285667035, 0.3272492347489422415 ) ) ;
#11002=CARTESIAN_POINT ( 'NONE',  ( 2.128941206161000466, 29.76184805414000323, -0.3055447833205000019 ) ) ;
#11003=AXIS2_PLACEMENT_3D ( 'NONE', #23170, #10353, #17741 ) ;
#11006=EDGE_LOOP ( 'NONE', ( #9320, #21851, #5059, #21148 ) ) ;
#11010=CARTESIAN_POINT ( 'NONE',  ( 2.184465970885653530, 29.13333333333333997, 1.259047450927233802 ) ) ;
#11011=CARTESIAN_POINT ( 'NONE',  ( 4.000000000000000000, 24.80000000000000426, 2.309401076759000304 ) ) ;
#11015=CARTESIAN_POINT ( 'NONE',  ( -1.402904250052608104, 29.29391569701615694, -1.642719484273872377 ) ) ;
#11019=ADVANCED_FACE ( 'NONE', ( #15216 ), #11937, .T. ) ;
#11022=CARTESIAN_POINT ( 'NONE',  ( 1.189766245367999797, 24.91662324376000015, 2.030297963902000014 ) ) ;
#11029=EDGE_CURVE ( 'NONE', #7614, #18970, #21625, .T. ) ;
#11031=CARTESIAN_POINT ( 'NONE',  ( 2.729128784747790970, 18.00000000000000000, 0.000000000000000000 ) ) ;
#11038=CARTESIAN_POINT ( 'NONE',  ( -2.119341350454000406, 25.24022682738999990, 0.9803262384023999632 ) ) ;
#11042=CARTESIAN_POINT ( 'NONE',  ( 2.021323174276000056, 30.26884416382999987, -1.858207751705999833 ) ) ;
#11047=ORIENTED_EDGE ( 'NONE', *, *, #20329, .T. ) ;
#11048=EDGE_CURVE ( 'NONE', #22927, #14207, #446, .T. ) ;
#11053=DIRECTION ( 'NONE',  ( 1.000000000000000000, 0.000000000000000000, 0.000000000000000000 ) ) ;
#11057=CARTESIAN_POINT ( 'NONE',  ( -0.2616786785208999877, 26.49212896666999839, -2.656868203660999850 ) ) ;
#11060=EDGE_CURVE ( 'NONE', #20057, #19401, #11954, .T. ) ;
#11062=DIRECTION ( 'NONE',  ( 1.000000000000000000, 0.000000000000000000, 9.309572557292015679E-11 ) ) ;
#11072=CARTESIAN_POINT ( 'NONE',  ( -0.9067637935996000209, 30.06497459668999994, -2.160393313164000073 ) ) ;
#11074=CARTESIAN_POINT ( 'NONE',  ( 0.7476305753117580277, 29.95889564184829368, -2.026589009648734674 ) ) ;
#11075=VERTEX_POINT ( 'NONE', #22851 ) ;
#11076=CARTESIAN_POINT ( 'NONE',  ( -1.344757420832000117, 25.31728931014000139, -1.717707233910999998 ) ) ;
#11081=AXIS2_PLACEMENT_3D ( 'NONE', #17546, #942, #8707 ) ;
#11082=AXIS2_PLACEMENT_3D ( 'NONE', #3160, #4607, #12117 ) ;
#11085=EDGE_LOOP ( 'NONE', ( #10873, #13668, #15349, #6565 ) ) ;
#11089=DIRECTION ( 'NONE',  ( 0.000000000000000000, -1.000000000000000000, 0.000000000000000000 ) ) ;
#11091=AXIS2_PLACEMENT_3D ( 'NONE', #22820, #6235, #7701 ) ;
#11098=CARTESIAN_POINT ( 'NONE',  ( -1.888459278277104156E-11, 26.49469377355791977, -2.394693773557865057 ) ) ;
#11101=CARTESIAN_POINT ( 'NONE',  ( -4.649999849441000421, 22.00000015055399771, 6.648422636708999828E-08 ) ) ;
#11102=CARTESIAN_POINT ( 'NONE',  ( 1.247171621864741953, 30.72546509146406279, -1.763763891515052640 ) ) ;
#11103=ORIENTED_EDGE ( 'NONE', *, *, #14565, .F. ) ;
#11104=CARTESIAN_POINT ( 'NONE',  ( 2.210755315046764480, 26.34981806843837759, 0.4830521748348369782 ) ) ;
#11107=CARTESIAN_POINT ( 'NONE',  ( -2.392615059649000120, 26.24187716036000495, 0.5249584007626999504 ) ) ;
#11108=DIRECTION ( 'NONE',  ( 1.000000000000000000, 0.000000000000000000, 0.000000000000000000 ) ) ;
#11115=CARTESIAN_POINT ( 'NONE',  ( 0.3124060177047779940, 29.44778486168719667, 2.256467045519745529 ) ) ;
#11116=ORIENTED_EDGE ( 'NONE', *, *, #1584, .F. ) ;
#11120=ADVANCED_FACE ( 'NONE', ( #9667 ), #3442, .F. ) ;
#11122=CARTESIAN_POINT ( 'NONE',  ( -0.2810990160142999295, 29.96038721557000173, -2.132306642366999849 ) ) ;
#11123=DIRECTION ( 'NONE',  ( -1.000000000000000000, 0.000000000000000000, 0.000000000000000000 ) ) ;
#11128=PRODUCT ( 'Valve Operating Stem', 'Valve Operating Stem', '', ( #12443 ) ) ;
#11130=VERTEX_POINT ( 'NONE', #8098 ) ;
#11131=LINE ( 'NONE', #11011, #2659 ) ;
#11132=CARTESIAN_POINT ( 'NONE',  ( -4.000000000000000000, 24.80000000000000426, -2.309401076759000304 ) ) ;
#11134=CARTESIAN_POINT ( 'NONE',  ( 0.6632315864332809507, 29.16452115530013955, -2.086780444890731889 ) ) ;
#11136=DIRECTION ( 'NONE',  ( -1.000000000000000000, 0.000000000000000000, 0.000000000000000000 ) ) ;
#11140=CARTESIAN_POINT ( 'NONE',  ( -1.894396370449000111, 24.56827184614000004, -1.396035791950000160 ) ) ;
#11144=VECTOR ( 'NONE', #14875, 1000.000000000000114 ) ;
#11145=DIRECTION ( 'NONE',  ( -0.7071067811867959296, 0.7071067811862957742, 6.966833095770957245E-08 ) ) ;
#11147=( LENGTH_UNIT ( ) NAMED_UNIT ( * ) SI_UNIT ( .MILLI., .METRE. ) );
#11156=CARTESIAN_POINT ( 'NONE',  ( -2.298308792509000220, 24.40769234017999878, 0.4128243414548999901 ) ) ;
#11161=CARTESIAN_POINT ( 'NONE',  ( 2.366606196949999852, 30.23066102319999970, 0.9578807050024000791 ) ) ;
#11163=DIRECTION ( 'NONE',  ( -0.000000000000000000, 1.000000000000000000, 0.000000000000000000 ) ) ;
#11165=LINE ( 'NONE', #15248, #3671 ) ;
#11168=VERTEX_POINT ( 'NONE', #15826 ) ;
#11169=CARTESIAN_POINT ( 'NONE',  ( -2.480627735891629548, 24.20832311788705482, -0.5148137458739096006 ) ) ;
#11170=CARTESIAN_POINT ( 'NONE',  ( 2.394884942776999814, 23.89488494277999919, 0.000000000000000000 ) ) ;
#11176=CIRCLE ( 'NONE', #1889, 3.000000000000000000 ) ;
#11180=CARTESIAN_POINT ( 'NONE',  ( -0.7744564004552000336, 28.44212896666999768, 2.554499528901000183 ) ) ;
#11181=ORIENTED_EDGE ( 'NONE', *, *, #11401, .T. ) ;
#11186=DIRECTION ( 'NONE',  ( -1.000000000000000000, 0.000000000000000000, 0.000000000000000000 ) ) ;
#11187=ADVANCED_FACE ( 'NONE', ( #19480 ), #308, .T. ) ;
#11196=CARTESIAN_POINT ( 'NONE',  ( 0.1900786975556000014, 30.23224694295999981, 2.348537901832999708 ) ) ;
#11197=AXIS2_PLACEMENT_3D ( 'NONE', #15915, #8433, #23426 ) ;
#11199=CARTESIAN_POINT ( 'NONE',  ( 1.357139981220319980, 29.69016086971108948, 1.680935446004558687 ) ) ;
#11202=CARTESIAN_POINT ( 'NONE',  ( -2.110330650965000387, 24.67076761794999840, 1.000962332422999923 ) ) ;
#11210=CARTESIAN_POINT ( 'NONE',  ( 0.000000000000000000, 22.09999988306816832, 0.000000000000000000 ) ) ;
#11214=ORIENTED_EDGE ( 'NONE', *, *, #5282, .F. ) ;
#11215=AXIS2_PLACEMENT_3D ( 'NONE', #6562, #8385, #19774 ) ;
#11218=ORIENTED_EDGE ( 'NONE', *, *, #20509, .F. ) ;
#11230=CARTESIAN_POINT ( 'NONE',  ( 2.018792404907182814, 30.65015847864969345, -0.7678982693529425863 ) ) ;
#11234=CARTESIAN_POINT ( 'NONE',  ( 0.9266888457184595529, 24.78564400243023869, 1.917495999108346894 ) ) ;
#11236=CARTESIAN_POINT ( 'NONE',  ( 1.979460888490000015, 25.75437716036000069, 1.008585698963999855 ) ) ;
#11248=CARTESIAN_POINT ( 'NONE',  ( -1.380185735549000148, 29.23241029034999627, -1.649495554458999980 ) ) ;
#11254=CARTESIAN_POINT ( 'NONE',  ( 1.536366799937303407, 29.08333333333333215, 1.999167105995437677 ) ) ;
#11257=CYLINDRICAL_SURFACE ( 'NONE', #997, 2.000000000000000000 ) ;
#11258=CIRCLE ( 'NONE', #13556, 4.724999999999999645 ) ;
#11260=B_SPLINE_CURVE_WITH_KNOTS ( 'NONE', 3,
 ( #8092, #19222, #15692, #2763, #4706, #12331, #2634, #15936, #17415, #6743 ),
 .UNSPECIFIED., .F., .F.,
 ( 4, 1, 1, 2, 2, 4 ),
 ( 0.000000000000000000, 0.2499999999999994449, 0.3749999999999989453, 0.4374999999999987788, 0.4999999999999985567, 1.000000000000000000 ),
 .UNSPECIFIED. ) ;
#11261=CARTESIAN_POINT ( 'NONE',  ( -0.3748402411544077273, 29.22614913440824935, -2.127372941641080040 ) ) ;
#11263=ORIENTED_EDGE ( 'NONE', *, *, #3356, .F. ) ;
#11264=DIRECTION ( 'NONE',  ( 0.000000000000000000, 0.000000000000000000, -1.000000000000000000 ) ) ;
#11265=ORIENTED_EDGE ( 'NONE', *, *, #6447, .T. ) ;
#11267=CARTESIAN_POINT ( 'NONE',  ( -0.2356110571030000100, 23.66255821230999956, -2.226257962701000181 ) ) ;
#11268=CARTESIAN_POINT ( 'NONE',  ( 0.3272492347489455167, 28.21666666666666856, 2.499999999999998668 ) ) ;
#11269=CARTESIAN_POINT ( 'NONE',  ( -0.6576354733792000307, 28.65299822781000216, 2.169172474974999876 ) ) ;
#11271=DIRECTION ( 'NONE',  ( -1.000000000000000000, 0.000000000000000000, 0.000000000000000000 ) ) ;
#11273=CARTESIAN_POINT ( 'NONE',  ( -3.100000000000000089, 17.00000000000000000, 0.000000000000000000 ) ) ;
#11277=ORIENTED_EDGE ( 'NONE', *, *, #14312, .F. ) ;
#11278=EDGE_CURVE ( 'NONE', #12315, #889, #6516, .T. ) ;
#11280=CARTESIAN_POINT ( 'NONE',  ( -1.285289189667999876, 23.80867471234000021, 1.716809468418999840 ) ) ;
#11282=CARTESIAN_POINT ( 'NONE',  ( 0.000000000000000000, 21.95000012746600149, -4.699999872533999756 ) ) ;
#11284=CARTESIAN_POINT ( 'NONE',  ( 1.736698740103000071, 29.58438105280999864, -1.871426636120000042 ) ) ;
#11289=ORIENTED_EDGE ( 'NONE', *, *, #23265, .T. ) ;
#11290=CARTESIAN_POINT ( 'NONE',  ( -0.3439877393419937257, 24.41664673104403960, 2.509216680981930736 ) ) ;
#11293=ADVANCED_FACE ( 'NONE', ( #12911 ), #20308, .F. ) ;
#11295=VECTOR ( 'NONE', #20648, 1000.000000000000114 ) ;
#11300=CARTESIAN_POINT ( 'NONE',  ( 2.437990915149000237, 25.45212896666999924, 0.5485649090615000167 ) ) ;
#11303=CARTESIAN_POINT ( 'NONE',  ( 0.3272492347489341924, 27.21753006952334530, -2.500000000000000888 ) ) ;
#11307=VERTEX_POINT ( 'NONE', #9168 ) ;
#11314=CARTESIAN_POINT ( 'NONE',  ( 1.433070709896999917, 29.72363129601999887, 1.653766674786000035 ) ) ;
#11315=AXIS2_PLACEMENT_3D ( 'NONE', #16854, #22545, #14795 ) ;
#11317=ADVANCED_FACE ( 'NONE', ( #14383 ), #12805, .T. ) ;
#11318=CARTESIAN_POINT ( 'NONE',  ( 0.4639490188554213912, 29.63126733662222989, 2.109472460375426017 ) ) ;
#11320=CARTESIAN_POINT ( 'NONE',  ( 1.450318268071000061, 24.34012059315000087, -1.629560560109000189 ) ) ;
#11321=CARTESIAN_POINT ( 'NONE',  ( 2.999999956181000016, 17.90000004382000043, -2.609181548331000199E-08 ) ) ;
#11323=VERTEX_POINT ( 'NONE', #21777 ) ;
#11328=FACE_OUTER_BOUND ( 'NONE', #15768, .T. ) ;
#11334=FACE_OUTER_BOUND ( 'NONE', #14910, .T. ) ;
#11337=EDGE_CURVE ( 'NONE', #15685, #5518, #17482, .T. ) ;
#11345=CARTESIAN_POINT ( 'NONE',  ( 0.4139582100457485092, 30.42833226141065595, 2.119867715313618728 ) ) ;
#11349=CARTESIAN_POINT ( 'NONE',  ( 1.607383496580327087, 24.77257767849905079, 1.394007648165144664 ) ) ;
#11353=CARTESIAN_POINT ( 'NONE',  ( 0.5279260092677000582, 28.19446440325999959, -2.406140597653999791 ) ) ;
#11358=DIRECTION ( 'NONE',  ( 0.000000000000000000, -1.000000000000000000, 0.000000000000000000 ) ) ;
#11365=DIRECTION ( 'NONE',  ( -0.000000000000000000, 1.000000000000000000, 0.000000000000000000 ) ) ;
#11371=AXIS2_PLACEMENT_3D ( 'NONE', #13882, #6980, #15684 ) ;
#11372=DIRECTION ( 'NONE',  ( 1.000000000000000000, 0.000000000000000000, 0.000000000000000000 ) ) ;
#11377=CARTESIAN_POINT ( 'NONE',  ( -1.234859021521087730, 29.28134306420319888, -1.772094427844483455 ) ) ;
#11382=CIRCLE ( 'NONE', #2878, 3.100000000000000089 ) ;
#11383=CARTESIAN_POINT ( 'NONE',  ( -2.316775158635999698, 23.87156905088000158, 0.4125208335121000602 ) ) ;
#11385=CARTESIAN_POINT ( 'NONE',  ( 2.266578917753999889, 27.28799822781000017, 0.04450989311242999763 ) ) ;
#11391=B_SPLINE_CURVE_WITH_KNOTS ( 'NONE', 3,
 ( #9817, #9578, #23002, #19262, #22884, #5934, #478, #2185, #8132, #6298, #22527, #2677, #10066, #13321, #17451, #844, #4367, #8247 ),
 .UNSPECIFIED., .F., .F.,
 ( 4, 2, 2, 2, 2, 2, 2, 2, 4 ),
 ( 0.000000000000000000, 0.1250000000000000555, 0.2500000000000000555, 0.3750000000000000555, 0.5000000000000000000, 0.6249999999999998890, 0.7499999999999998890, 0.8749999999999998890, 1.000000000000000000 ),
 .UNSPECIFIED. ) ;
#11393=DIRECTION ( 'NONE',  ( 0.000000000000000000, -1.000000000000000000, 0.000000000000000000 ) ) ;
#11396=CARTESIAN_POINT ( 'NONE',  ( 1.575558360453000128, 24.45298753663999847, 2.212366420454999982 ) ) ;
#11399=CARTESIAN_POINT ( 'NONE',  ( 0.000000000000000000, 22.19999999999999574, 0.000000000000000000 ) ) ;
#11401=EDGE_CURVE ( 'NONE', #10250, #7057, #16599, .T. ) ;
#11402=CARTESIAN_POINT ( 'NONE',  ( -2.552764028111999650, 29.08171885361999998, 0.04190466168120000195 ) ) ;
#11405=LINE ( 'NONE', #16963, #17999 ) ;
#11407=ORIENTED_EDGE ( 'NONE', *, *, #1640, .F. ) ;
#11413=ORIENTED_EDGE ( 'NONE', *, *, #6136, .F. ) ;
#11414=VECTOR ( 'NONE', #4002, 1000.000000000000114 ) ;
#11416=CARTESIAN_POINT ( 'NONE',  ( 0.000000000000000000, 26.50000000000000355, 0.000000000000000000 ) ) ;
#11417=CARTESIAN_POINT ( 'NONE',  ( -2.505154520421000175, 28.23919433610000240, 1.402946323589000066 ) ) ;
#11421=CARTESIAN_POINT ( 'NONE',  ( 2.500000000000000000, 27.05086340285665969, -0.3272492347489373565 ) ) ;
#11422=FACE_OUTER_BOUND ( 'NONE', #8158, .T. ) ;
#11431=CARTESIAN_POINT ( 'NONE',  ( -0.3402753032406000133, 28.56835218490999750, 2.088129448976000280 ) ) ;
#11434=CARTESIAN_POINT ( 'NONE',  ( 1.421375682288115838, 29.69513268992620780, 1.626398583794437691 ) ) ;
#11442=CARTESIAN_POINT ( 'NONE',  ( -3.000000000000000000, 22.00000000000000000, 0.000000000000000000 ) ) ;
#11443=VECTOR ( 'NONE', #15041, 1000.000000000000114 ) ;
#11445=ORIENTED_EDGE ( 'NONE', *, *, #8012, .T. ) ;
#11455=EDGE_CURVE ( 'NONE', #23934, #15484, #9935, .T. ) ;
#11458=CARTESIAN_POINT ( 'NONE',  ( 1.830943384928172435, 26.42105733796857692, -1.434664342410846505 ) ) ;
#11459=CARTESIAN_POINT ( 'NONE',  ( 1.536366799937286087, 28.75086340285666608, -1.999167105995451221 ) ) ;
#11460=CARTESIAN_POINT ( 'NONE',  ( -2.500000000000000888, 28.21753006952333109, -0.3272492347489316944 ) ) ;
#11461=CARTESIAN_POINT ( 'NONE',  ( 0.8968807111111073427, 30.45845794433010312, 1.964841723554275221 ) ) ;
#11465=CONICAL_SURFACE ( 'NONE', #21532, 4.649999926447000220, 0.7853981633972997312 ) ;
#11467=CIRCLE ( 'NONE', #11082, 2.948682383037074750 ) ;
#11469=CYLINDRICAL_SURFACE ( 'NONE', #14666, 2.000000000000000000 ) ;
#11471=ADVANCED_FACE ( 'NONE', ( #2545 ), #23561, .T. ) ;
#11477=CARTESIAN_POINT ( 'NONE',  ( -1.861289502244705574, 28.35853889522002191, -1.170032434317527237 ) ) ;
#11482=EDGE_CURVE ( 'NONE', #21511, #21635, #19716, .T. ) ;
#11485=EDGE_CURVE ( 'NONE', #18033, #12379, #21651, .T. ) ;
#11487=CARTESIAN_POINT ( 'NONE',  ( 0.3373768742556949585, 24.49999999999998224, 2.400465711495646914 ) ) ;
#11491=ORIENTED_EDGE ( 'NONE', *, *, #12823, .F. ) ;
#11492=DIRECTION ( 'NONE',  ( -1.877655957117991099E-08, -0.9999999999999978906, 6.187284373139976848E-08 ) ) ;
#11493=CARTESIAN_POINT ( 'NONE',  ( 0.05241653317063999645, 27.35706776952000041, 2.669209039122999894 ) ) ;
#11495=AXIS2_PLACEMENT_3D ( 'NONE', #18412, #20237, #20581 ) ;
#11496=CARTESIAN_POINT ( 'NONE',  ( 2.119314978498162638, 29.02854376302997252, -0.4166382853690258625 ) ) ;
#11498=VERTEX_POINT ( 'NONE', #15130 ) ;
#11499=EDGE_CURVE ( 'NONE', #16136, #8792, #11391, .T. ) ;
#11502=VERTEX_POINT ( 'NONE', #18902 ) ;
#11505=CARTESIAN_POINT ( 'NONE',  ( 1.016344414748000080, 28.64506359724000362, 1.994688225595000253 ) ) ;
#11507=CARTESIAN_POINT ( 'NONE',  ( 0.000000000000000000, -1.550000000000000044, 0.000000000000000000 ) ) ;
#11514=CIRCLE ( 'NONE', #14964, 1.899912543625999373 ) ;
#11515=CARTESIAN_POINT ( 'NONE',  ( -2.110727562395000145, 24.26086419343999978, 1.709321059049000002 ) ) ;
#11518=CARTESIAN_POINT ( 'NONE',  ( 2.488228344306999684, 28.65086554002000341, 0.5718697359529000268 ) ) ;
#11522=DIRECTION ( 'NONE',  ( 0.000000000000000000, 1.000000000000000000, 0.000000000000000000 ) ) ;
#11528=B_SPLINE_SURFACE_WITH_KNOTS ( 'NONE', 3, 3, ( 
 ( #19250, #7869, #13429, #20830, #9924, #7988, #2662, #4356, #711, #4244, #15604, #6169, #11633, #19002, #6408, #2413, #15360, #13553, #20590, #20950, #6772, #16213, #12238, #5094, #8599, #15961, #23354, #956, #19379, #12360, #18046, #19625, #4975, #14165, #21560 ),
 ( #19748, #4606, #17561, #13790, #3159, #11994, #10541, #2789, #21682, #8354, #15846, #23235, #3033, #15719, #10174, #23111, #6649, #6535, #10421, #13919, #23610, #10658, #1207, #4850, #21315, #17926, #14044, #17812, #3275, #1331, #8720, #1451, #4729, #16084, #23483 ),
 ( #1082, #8847, #12116, #21192, #10294, #19502, #6894, #17682, #2911, #8481, #14289, #21437, #12475, #19860, #7125, #23719, #22029, #7360, #5440, #14857, #2033, #7473, #88, #12822, #16680, #5549, #22246, #19978, #20214, #1575, #22139, #23954, #12928, #20103, #3620 ),
 ( #14515, #13047, #12709, #20324, #18280, #3732, #9423, #14745, #18173, #3398, #5662, #16327, #21908, #20444, #11122, #5320, #10894, #11002, #18387, #3513, #18507, #1679, #9068, #3856, #1918, #11248, #10781, #18626, #16441, #16794, #8960, #7014, #23830, #7240, #14630 ) ),
 .UNSPECIFIED., .F., .F., .F.,
 ( 4, 4 ),
 ( 4, 1, 1, 1, 1, 1, 1, 1, 1, 1, 1, 1, 1, 1, 1, 1, 1, 1, 1, 1, 1, 1, 1, 1, 1, 1, 1, 1, 1, 1, 1, 1, 4 ),
 ( -0.3056682515952000023, 1.305668251594999996 ),
 ( 0.3076583088816999823, 0.3297182157065000063, 0.3517781225314000060, 0.3738380293562000301, 0.3958979361811000297, 0.4179578430058999983, 0.4400177498307999979, 0.4620776566556000220, 0.4841375634804999661, 0.5061974703053000457, 0.5282573771301999344, 0.5503172839550000139, 0.5723771907799000136, 0.5944370976046999822, 0.6164970044295999818, 0.6385569112543999504, 0.6606168180793000611, 0.6826767249041000296, 0.7047366317289999182, 0.7267965385537999978, 0.7488564453786000774, 0.7709163522034999660, 0.7929762590283000456, 0.8150361658531999343, 0.8370960726780000138, 0.8591559795029000135, 0.8812158863276999821, 0.9032757931526000927, 0.9253356999774000613, 0.9473956068022999499, 0.9694555136271000295, 0.9915154204520000292, 1.013575327277000060 ),
 .UNSPECIFIED. ) ;
#11535=CARTESIAN_POINT ( 'NONE',  ( 1.569224139466999901, 27.75962896667000024, 2.159851832628000068 ) ) ;
#11536=ORIENTED_EDGE ( 'NONE', *, *, #3228, .F. ) ;
#11549=CARTESIAN_POINT ( 'NONE',  ( 0.2170015115553000085, 29.22007215129999835, -2.177509141144999827 ) ) ;
#11551=AXIS2_PLACEMENT_3D ( 'NONE', #7023, #1807, #18396 ) ;
#11552=CARTESIAN_POINT ( 'NONE',  ( 0.005795789622999577249, 29.60418495093035673, 2.160003967929674751 ) ) ;
#11553=ORIENTED_EDGE ( 'NONE', *, *, #15001, .T. ) ;
#11554=CARTESIAN_POINT ( 'NONE',  ( 1.815810164558999906, 24.86381916441000328, -1.216941248911999951 ) ) ;
#11556=CARTESIAN_POINT ( 'NONE',  ( 0.000000000000000000, 7.000000000000000000, 0.000000000000000000 ) ) ;
#11557=EDGE_LOOP ( 'NONE', ( #21607, #14567, #10499, #16674 ) ) ;
#11558=DIRECTION ( 'NONE',  ( 1.000000000000000000, 0.000000000000000000, 0.000000000000000000 ) ) ;
#11561=CARTESIAN_POINT ( 'NONE',  ( -3.050000000000000266, 18.50000000000000000, 0.000000000000000000 ) ) ;
#11566=CARTESIAN_POINT ( 'NONE',  ( 0.000000000000000000, 20.05000017415440183, 0.000000000000000000 ) ) ;
#11567=VECTOR ( 'NONE', #14401, 1000.000000000000000 ) ;
#11568=VERTEX_POINT ( 'NONE', #15372 ) ;
#11578=FACE_BOUND ( 'NONE', #3273, .T. ) ;
#11579=CARTESIAN_POINT ( 'NONE',  ( 1.259047450927247569, 28.76753006952334246, -2.184465970885645536 ) ) ;
#11580=CARTESIAN_POINT ( 'NONE',  ( 2.500000000000000000, 27.85086340285666395, -0.3272492347489373565 ) ) ;
#11581=CARTESIAN_POINT ( 'NONE',  ( 2.147225282976996219, 30.61754596991750077, -0.2336052812872324580 ) ) ;
#11582=VERTEX_POINT ( 'NONE', #17825 ) ;
#11586=CARTESIAN_POINT ( 'NONE',  ( 4.000000000000000000, 24.50000000000000000, 0.000000000000000000 ) ) ;
#11588=CARTESIAN_POINT ( 'NONE',  ( 1.447934651311999943, 27.90196440325999916, 1.992911166421000191 ) ) ;
#11593=ORIENTED_EDGE ( 'NONE', *, *, #196, .T. ) ;
#11597=CARTESIAN_POINT ( 'NONE',  ( -1.433323533133572081, 28.32155547661488626, -1.629608261536916070 ) ) ;
#11598=VERTEX_POINT ( 'NONE', #2924 ) ;
#11599=EDGE_LOOP ( 'NONE', ( #23003, #12665, #21680, #13826, #3806 ) ) ;
#11604=FACE_BOUND ( 'NONE', #17494, .T. ) ;
#11606=CARTESIAN_POINT ( 'NONE',  ( -2.116994795175099142, 30.88300524173097017, -0.1245676364603316710 ) ) ;
#11609=CARTESIAN_POINT ( 'NONE',  ( -2.999999956181000016, 17.90000004382000043, 2.609181505839000138E-08 ) ) ;
#11610=ORIENTED_EDGE ( 'NONE', *, *, #17121, .T. ) ;
#11612=CARTESIAN_POINT ( 'NONE',  ( 2.320116128650000054, 26.00000240009999786, 1.182158213329999930 ) ) ;
#11616=CARTESIAN_POINT ( 'NONE',  ( 2.154679880121377344, 28.99501662734741458, 0.1501254452029534836 ) ) ;
#11621=FACE_OUTER_BOUND ( 'NONE', #15629, .T. ) ;
#11624=CARTESIAN_POINT ( 'NONE',  ( -2.153772461420000006, 28.45006359724000333, 1.206163983883000057 ) ) ;
#11625=EDGE_CURVE ( 'NONE', #6758, #1877, #8495, .T. ) ;
#11626=CARTESIAN_POINT ( 'NONE',  ( 0.000000000000000000, 24.50000000000000000, 0.000000000000000000 ) ) ;
#11631=ORIENTED_EDGE ( 'NONE', *, *, #17854, .F. ) ;
#11632=ADVANCED_FACE ( 'NONE', ( #967 ), #10435, .T. ) ;
#11633=CARTESIAN_POINT ( 'NONE',  ( -2.508635807456999434, 30.40905054822999887, -1.061151462325000017 ) ) ;
#11635=CARTESIAN_POINT ( 'NONE',  ( 1.234780954647000106, 24.81458662482000221, -2.203141158743999739 ) ) ;
#11639=FACE_OUTER_BOUND ( 'NONE', #9666, .T. ) ;
#11641=CARTESIAN_POINT ( 'NONE',  ( -1.963703823225463774, 26.25920717875808563, 0.8995588027868727243 ) ) ;
#11644=CARTESIAN_POINT ( 'NONE',  ( 2.500000000000000000, 24.63419673618999894, 0.000000000000000000 ) ) ;
#11646=CARTESIAN_POINT ( 'NONE',  ( 0.9226519948152428485, 23.99124041189808310, -2.329934127714008429 ) ) ;
#11648=ORIENTED_EDGE ( 'NONE', *, *, #1934, .T. ) ;
#11651=CARTESIAN_POINT ( 'NONE',  ( -2.051578334272556425, 24.64979581979662626, 0.7778699027752854489 ) ) ;
#11655=LINE ( 'NONE', #19026, #20601 ) ;
#11657=ORIENTED_EDGE ( 'NONE', *, *, #18219, .F. ) ;
#11660=CYLINDRICAL_SURFACE ( 'NONE', #19482, 4.750000000000000000 ) ;
#11661=ORIENTED_EDGE ( 'NONE', *, *, #10771, .T. ) ;
#11662=ADVANCED_FACE ( 'NONE', ( #4862 ), #23497, .F. ) ;
#11668=CARTESIAN_POINT ( 'NONE',  ( 1.574276030777000068, 30.48667273621999740, -1.526313238878999945 ) ) ;
#11669=LINE ( 'NONE', #10461, #2689 ) ;
#11671=CARTESIAN_POINT ( 'NONE',  ( 0.5301375200171086766, 29.63531083614599737, 2.093953783698239590 ) ) ;
#11672=ORIENTED_EDGE ( 'NONE', *, *, #10987, .F. ) ;
#11673=B_SPLINE_CURVE_WITH_KNOTS ( 'NONE', 3,
 ( #11886, #6187, #19270, #2684, #10072, #17457, #850, #8255, #4995, #5227 ),
 .UNSPECIFIED., .F., .F.,
 ( 4, 2, 2, 2, 4 ),
 ( 0.000000000000000000, 0.2499999999999998890, 0.4999999999999997780, 0.7499999999999998890, 1.000000000000000000 ),
 .UNSPECIFIED. ) ;
#11674=CARTESIAN_POINT ( 'NONE',  ( -0.2719153812508000034, 25.03673698483999743, -2.333095969081999677 ) ) ;
#11676=VERTEX_POINT ( 'NONE', #7027 ) ;
#11677=CARTESIAN_POINT ( 'NONE',  ( -2.241935917934180011, 24.64274320532739893, -0.3031776926340762901 ) ) ;
#11685=ORIENTED_EDGE ( 'NONE', *, *, #10475, .F. ) ;
#11686=DIRECTION ( 'NONE',  ( 0.000000000000000000, 0.000000000000000000, -1.000000000000000000 ) ) ;
#11691=CARTESIAN_POINT ( 'NONE',  ( -2.121106334292000017, 30.87889366360999688, 6.284935476095000148E-07 ) ) ;
#11694=CARTESIAN_POINT ( 'NONE',  ( -0.9358744650684699407, 26.41068681084919589, 4.078474779182607257 ) ) ;
#11695=( NAMED_UNIT ( * ) PLANE_ANGLE_UNIT ( ) SI_UNIT ( $, .RADIAN. ) );
#11698=CARTESIAN_POINT ( 'NONE',  ( 0.6344839516865840023, 30.44182778481178175, 2.065287063757580199 ) ) ;
#11699=EDGE_LOOP ( 'NONE', ( #15269, #19283, #5965 ) ) ;
#11703=CARTESIAN_POINT ( 'NONE',  ( 0.000000000000000000, 18.10000000000000142, 0.000000000000000000 ) ) ;
#11704=CARTESIAN_POINT ( 'NONE',  ( -0.6219987658658999718, 25.85446440325999973, -2.383523424258999768 ) ) ;
#11708=ORIENTED_EDGE ( 'NONE', *, *, #4022, .F. ) ;
#11711=LINE ( 'NONE', #21026, #16545 ) ;
#11712=CARTESIAN_POINT ( 'NONE',  ( 0.000000000000000000, 24.65000000674550051, 0.000000000000000000 ) ) ;
#11728=CARTESIAN_POINT ( 'NONE',  ( 2.157402177123000087, 25.89456776952000183, 1.099251314038999894 ) ) ;
#11730=CARTESIAN_POINT ( 'NONE',  ( 2.098996325922923845, 29.03416195166998293, -0.5104432153915662296 ) ) ;
#11735=DIRECTION ( 'NONE',  ( 1.000000000000000000, 0.000000000000000000, 0.000000000000000000 ) ) ;
#11737=EDGE_CURVE ( 'NONE', #11953, #5391, #23967, .T. ) ;
#11745=DIRECTION ( 'NONE',  ( -1.000000000000000000, 0.000000000000000000, 0.000000000000000000 ) ) ;
#11746=VERTEX_POINT ( 'NONE', #3524 ) ;
#11748=B_SPLINE_CURVE_WITH_KNOTS ( 'NONE', 3,
 ( #3317, #23650, #12403, #5247, #16605, #10698, #5018, #16257 ),
 .UNSPECIFIED., .F., .F.,
 ( 4, 2, 2, 4 ),
 ( 2.284496667305657708E-05, 0.0004791365171912424304, 0.0009354280677094282091, 0.001848011168745799983 ),
 .UNSPECIFIED. ) ;
#11749=CARTESIAN_POINT ( 'NONE',  ( -1.513605150068000116, 23.59780545119999928, 2.021779747291999829 ) ) ;
#11754=EDGE_CURVE ( 'NONE', #6219, #20600, #13500, .T. ) ;
#11755=CARTESIAN_POINT ( 'NONE',  ( 2.000000000000000000, 26.50000000000000355, 3.464101615137999968 ) ) ;
#11758=DIRECTION ( 'NONE',  ( 0.000000000000000000, -1.000000000000000000, 0.000000000000000000 ) ) ;
#11767=CARTESIAN_POINT ( 'NONE',  ( -2.148333256768187205, 23.64833325676920595, 0.1693336218410599059 ) ) ;
#11769=DIRECTION ( 'NONE',  ( 0.000000000000000000, 0.000000000000000000, -1.000000000000000000 ) ) ;
#11770=TOROIDAL_SURFACE ( 'NONE', #7500, 1.600000000000000089, 0.1000000000000000056 ) ;
#11771=DIRECTION ( 'NONE',  ( -1.000000000000000000, 0.000000000000000000, 0.000000000000000000 ) ) ;
#11785=ADVANCED_FACE ( 'NONE', ( #22042 ), #18919, .T. ) ;
#11786=CARTESIAN_POINT ( 'NONE',  ( 1.575836833087000066, 29.72868779823999930, -1.751713004377999816 ) ) ;
#11789=CARTESIAN_POINT ( 'NONE',  ( 0.000000000000000000, 14.90000000000000036, 0.000000000000000000 ) ) ;
#11790=CARTESIAN_POINT ( 'NONE',  ( -1.099324150219182838, 29.53577431558094446, 1.859157437254163714 ) ) ;
#11792=CIRCLE ( 'NONE', #14487, 4.750000000000000000 ) ;
#11794=ORIENTED_EDGE ( 'NONE', *, *, #7921, .F. ) ;
#11796=ADVANCED_FACE ( 'NONE', ( #10643 ), #14787, .F. ) ;
#11797=DIRECTION ( 'NONE',  ( 0.000000000000000000, 1.000000000000000000, 0.000000000000000000 ) ) ;
#11799=CARTESIAN_POINT ( 'NONE',  ( 1.699986466736000068, 9.100024030970999434, -1.053574575520999757 ) ) ;
#11802=PLANE ( 'NONE',  #7501 ) ;
#11803=CARTESIAN_POINT ( 'NONE',  ( -0.3502059142650870704, 24.70197603011383691, -4.416610674644637413 ) ) ;
#11804=CARTESIAN_POINT ( 'NONE',  ( 0.000000000000000000, 24.80000000000000426, 4.618802153517000519 ) ) ;
#11806=CARTESIAN_POINT ( 'NONE',  ( -1.219598243196123644, 24.73228032484876593, 1.802923274881913729 ) ) ;
#11810=CARTESIAN_POINT ( 'NONE',  ( 4.000000000000000000, 26.43562577624026488, 1.040161751118762634 ) ) ;
#11812=CARTESIAN_POINT ( 'NONE',  ( 0.7867367962552690441, 24.50000000000000000, -2.267387309971103271 ) ) ;
#11815=DIRECTION ( 'NONE',  ( 0.000000000000000000, 1.000000000000000000, 0.000000000000000000 ) ) ;
#11816=CARTESIAN_POINT ( 'NONE',  ( -1.259047450927251788, 28.90086340285667532, -2.184465970885643316 ) ) ;
#11818=CARTESIAN_POINT ( 'NONE',  ( -1.317397315007501346, 30.08744644730780493, -1.712080957474261478 ) ) ;
#11830=CARTESIAN_POINT ( 'NONE',  ( 1.671483013463360923, 27.93939348436179060, 1.428772922976359050 ) ) ;
#11833=ADVANCED_FACE ( 'NONE', ( #22475 ), #11469, .T. ) ;
#11849=CARTESIAN_POINT ( 'NONE',  ( -2.656868203660999850, 27.94206776952000126, -0.2616786785207999566 ) ) ;
#11851=CARTESIAN_POINT ( 'NONE',  ( 2.053969861739825653, 29.04388804318223194, -0.6701222371007186096 ) ) ;
#11853=CARTESIAN_POINT ( 'NONE',  ( -2.500000000000000000, 28.00000000000000000, 0.000000000000000000 ) ) ;
#11854=ORIENTED_EDGE ( 'NONE', *, *, #2389, .F. ) ;
#11855=DIRECTION ( 'NONE',  ( -1.000000000000000000, 0.000000000000000000, 0.000000000000000000 ) ) ;
#11856=CARTESIAN_POINT ( 'NONE',  ( 0.000000000000000000, 20.04999987253367877, 0.000000000000000000 ) ) ;
#11860=ADVANCED_FACE ( 'NONE', ( #5999 ), #15815, .F. ) ;
#11864=ORIENTED_EDGE ( 'NONE', *, *, #15398, .T. ) ;
#11868=CARTESIAN_POINT ( 'NONE',  ( -0.3563741520152000075, 25.15743979504999928, 2.692573825428000056 ) ) ;
#11870=EDGE_LOOP ( 'NONE', ( #3031, #10177, #11661, #1057 ) ) ;
#11880=DIRECTION ( 'NONE',  ( 0.000000000000000000, -1.000000000000000000, 1.493818482293000218E-14 ) ) ;
#11884=ORIENTED_EDGE ( 'NONE', *, *, #22074, .T. ) ;
#11886=CARTESIAN_POINT ( 'NONE',  ( 2.500000000000000000, 28.63419673618999894, 0.000000000000000000 ) ) ;
#11889=CARTESIAN_POINT ( 'NONE',  ( 1.699999999999999956, 11.63334134365700123, -1.053568440557163255 ) ) ;
#11893=EDGE_LOOP ( 'NONE', ( #21580, #13288 ) ) ;
#11894=CIRCLE ( 'NONE', #3767, 2.100000000000000089 ) ;
#11895=ORIENTED_EDGE ( 'NONE', *, *, #5231, .F. ) ;
#11897=CARTESIAN_POINT ( 'NONE',  ( 2.329590180150573175, 24.49999999999984368, 3.273812635905912316 ) ) ;
#11900=ORIENTED_EDGE ( 'NONE', *, *, #19338, .F. ) ;
#11903=CARTESIAN_POINT ( 'NONE',  ( -2.000000000000000000, 23.50000000000000000, 0.000000000000000000 ) ) ;
#11912=CARTESIAN_POINT ( 'NONE',  ( -2.024508947676616266, 29.44926370956269324, 0.7533795805217576858 ) ) ;
#11914=CARTESIAN_POINT ( 'NONE',  ( -0.7536363891467999787, 23.78037720585000159, 2.224703581606000125 ) ) ;
#11924=ORIENTED_EDGE ( 'NONE', *, *, #4638, .F. ) ;
#11927=CARTESIAN_POINT ( 'NONE',  ( 2.434931691670788823, 26.83333333333333570, -0.6543697108982009514 ) ) ;
#11928=PRODUCT_DEFINITION_SHAPE ( 'NONE', 'NONE',  #2646 ) ;
#11929=ORIENTED_EDGE ( 'NONE', *, *, #4195, .T. ) ;
#11930=DIRECTION ( 'NONE',  ( 0.000000000000000000, -0.7071067811866525998, -0.7071067811864425456 ) ) ;
#11932=CARTESIAN_POINT ( 'NONE',  ( 0.000000000000000000, 16.89999999999999858, 0.000000000000000000 ) ) ;
#11935=VECTOR ( 'NONE', #10300, 1000.000000000000000 ) ;
#11937=CONICAL_SURFACE ( 'NONE', #19294, 4.699999872533999756, 0.7853981633972997312 ) ;
#11942=CARTESIAN_POINT ( 'NONE',  ( -2.000000000000000000, 26.50000000000000355, 3.464101615137999968 ) ) ;
#11943=FACE_OUTER_BOUND ( 'NONE', #15871, .T. ) ;
#11944=CARTESIAN_POINT ( 'NONE',  ( -2.088094669011058890, 30.23733246308190559, 0.5613753303782254012 ) ) ;
#11953=VERTEX_POINT ( 'NONE', #15919 ) ;
#11954=CIRCLE ( 'NONE', #13859, 0.09999999999999939493 ) ;
#11957=CARTESIAN_POINT ( 'NONE',  ( -2.163866556553845744, 27.61887052311726976, -0.1841620332587457221 ) ) ;
#11959=VERTEX_POINT ( 'NONE', #17515 ) ;
#11965=CARTESIAN_POINT ( 'NONE',  ( -1.350644574833474776, 24.52555747447238588, 3.839035148322985425 ) ) ;
#11967=CARTESIAN_POINT ( 'NONE',  ( -0.2249661094972814634, 28.79125399117670270, 2.160068143722255307 ) ) ;
#11968=CARTESIAN_POINT ( 'NONE',  ( -0.6543697108981929578, 26.80086340285666680, 2.434931691670791487 ) ) ;
#11969=DIRECTION ( 'NONE',  ( 1.000000000000000000, 0.000000000000000000, 0.000000000000000000 ) ) ;
#11974=CARTESIAN_POINT ( 'NONE',  ( -1.938452583514000072, 27.93413313894999916, 1.528152797339000113 ) ) ;
#11975=VECTOR ( 'NONE', #23115, 1000.000000000000000 ) ;
#11978=CARTESIAN_POINT ( 'NONE',  ( 0.4257810925096244814, 28.82890265351812431, 2.127227403366187986 ) ) ;
#11985=CARTESIAN_POINT ( 'NONE',  ( 6.356497079780072168E-07, 30.81706029784504963, -2.183072574220335849 ) ) ;
#11986=DIRECTION ( 'NONE',  ( -0.000000000000000000, 1.000000000000000000, 0.000000000000000000 ) ) ;
#11987=AXIS2_PLACEMENT_3D ( 'NONE', #23691, #14489, #21881 ) ;
#11994=CARTESIAN_POINT ( 'NONE',  ( 2.520990829206000150, 30.76687396097999638, -0.2444226712511999577 ) ) ;
#11997=CIRCLE ( 'NONE', #17815, 4.000000000000000000 ) ;
#12001=DIRECTION ( 'NONE',  ( 1.000000000000000000, 0.000000000000000000, 0.000000000000000000 ) ) ;
#12005=DIRECTION ( 'NONE',  ( -1.000000000000000000, 0.000000000000000000, 0.000000000000000000 ) ) ;
#12018=DIRECTION ( 'NONE',  ( 0.000000000000000000, -1.000000000000000000, 0.000000000000000000 ) ) ;
#12021=ORIENTED_EDGE ( 'NONE', *, *, #12899, .F. ) ;
#12023=FACE_OUTER_BOUND ( 'NONE', #8352, .T. ) ;
#12024=CARTESIAN_POINT ( 'NONE',  ( 2.000000000000000000, 24.50000000000000000, 3.464101615137999968 ) ) ;
#12031=CARTESIAN_POINT ( 'NONE',  ( -1.057980244643000001, 29.08125461216999952, -2.105335631596999768 ) ) ;
#12034=CARTESIAN_POINT ( 'NONE',  ( 2.500000000000000000, 29.43419673618999965, 0.000000000000000000 ) ) ;
#12036=CARTESIAN_POINT ( 'NONE',  ( -1.851996671504216430, 29.47254427382508268, 1.111577618485255048 ) ) ;
#12038=CARTESIAN_POINT ( 'NONE',  ( 0.9155365142161999703, 24.93361692991000211, -1.984919506156000324 ) ) ;
#12041=ORIENTED_EDGE ( 'NONE', *, *, #23568, .T. ) ;
#12045=ADVANCED_FACE ( 'NONE', ( #7319 ), #5278, .T. ) ;
#12049=CARTESIAN_POINT ( 'NONE',  ( -2.500000000000000000, 27.19999999999999929, 0.000000000000000000 ) ) ;
#12050=DIRECTION ( 'NONE',  ( 0.000000000000000000, 1.000000000000000000, 0.000000000000000000 ) ) ;
#12057=EDGE_CURVE ( 'NONE', #8075, #18038, #10433, .T. ) ;
#12064=ADVANCED_FACE ( 'NONE', ( #16642 ), #23946, .F. ) ;
#12065=CARTESIAN_POINT ( 'NONE',  ( -1.284157455750906118, 30.08499832656240258, -1.737012890293607503 ) ) ;
#12066=EDGE_LOOP ( 'NONE', ( #1262, #6009, #23341, #18076 ) ) ;
#12072=CARTESIAN_POINT ( 'NONE',  ( -0.8506511933622447064, 24.58106360703828841, 2.086532260108333592 ) ) ;
#12080=CARTESIAN_POINT ( 'NONE',  ( 0.7890445379464539055, 26.58333480217339684, -2.052919754909737104 ) ) ;
#12085=AXIS2_PLACEMENT_3D ( 'NONE', #15958, #3030, #10417 ) ;
#12094=DIRECTION ( 'NONE',  ( 0.000000000000000000, 1.000000000000000000, 0.000000000000000000 ) ) ;
#12097=CARTESIAN_POINT ( 'NONE',  ( 2.467893978438000069, 27.44663313894999845, 0.04846321314148000631 ) ) ;
#12100=CARTESIAN_POINT ( 'NONE',  ( -2.370125023230000405, 28.58187716036000126, -0.6185023500890999282 ) ) ;
#12103=CARTESIAN_POINT ( 'NONE',  ( -3.000000000000000000, 15.00000000000000000, 0.000000000000000000 ) ) ;
#12104=DIRECTION ( 'NONE',  ( 0.000000000000000000, 0.000000000000000000, -1.000000000000000000 ) ) ;
#12107=CARTESIAN_POINT ( 'NONE',  ( -0.2074533927172730330, 30.82465819688974662, -2.175341810225499550 ) ) ;
#12108=LINE ( 'NONE', #8344, #20411 ) ;
#12116=CARTESIAN_POINT ( 'NONE',  ( -0.1992920871147000061, 30.85997849182999886, -2.333249878129000088 ) ) ;
#12117=DIRECTION ( 'NONE',  ( 0.000000000000000000, 0.000000000000000000, 1.000000000000000000 ) ) ;
#12119=EDGE_LOOP ( 'NONE', ( #12596, #12780, #21042, #1962 ) ) ;
#12121=DIRECTION ( 'NONE',  ( 0.000000000000000000, 1.000000000000000000, 0.000000000000000000 ) ) ;
#12122=CARTESIAN_POINT ( 'NONE',  ( 1.702290430855999848, 28.68904868065000002, -2.154272664354000000 ) ) ;
#12128=VERTEX_POINT ( 'NONE', #2461 ) ;
#12129=LINE ( 'NONE', #9493, #15444 ) ;
#12131=EDGE_LOOP ( 'NONE', ( #13131, #20384, #884 ) ) ;
#12132=CARTESIAN_POINT ( 'NONE',  ( -1.875449657889999955, 25.64909039007000047, 1.720651897418999932 ) ) ;
#12143=EDGE_CURVE ( 'NONE', #14442, #13340, #20754, .T. ) ;
#12150=CARTESIAN_POINT ( 'NONE',  ( -1.958081313796000034, 29.29706567419000152, 1.310602052684999963 ) ) ;
#12155=CARTESIAN_POINT ( 'NONE',  ( -1.832658730057130203, 29.47472325661898651, 1.143358172601616207 ) ) ;
#12157=CARTESIAN_POINT ( 'NONE',  ( 0.000000000000000000, 22.10000000618969906, 0.000000000000000000 ) ) ;
#12168=CARTESIAN_POINT ( 'NONE',  ( 0.000000000000000000, 16.89999999999999858, 0.000000000000000000 ) ) ;
#12170=EDGE_CURVE ( 'NONE', #4287, #6758, #19505, .T. ) ;
#12182=CARTESIAN_POINT ( 'NONE',  ( -1.908738021986881250, 30.14178492054505298, -1.010896472074411578 ) ) ;
#12184=FACE_OUTER_BOUND ( 'NONE', #9655, .T. ) ;
#12189=VERTEX_POINT ( 'NONE', #18699 ) ;
#12193=ORIENTED_EDGE ( 'NONE', *, *, #19338, .T. ) ;
#12196=CARTESIAN_POINT ( 'NONE',  ( -3.999996093277206732, 24.62756664670158102, -1.519951541552794883 ) ) ;
#12197=CIRCLE ( 'NONE', #7543, 0.09999999999999982514 ) ;
#12198=CARTESIAN_POINT ( 'NONE',  ( 2.167090447363087868, 26.42307332155113642, 0.1133437460621688486 ) ) ;
#12206=CARTESIAN_POINT ( 'NONE',  ( 0.000000000000000000, 13.10000000000000142, 0.000000000000000000 ) ) ;
#12212=ORIENTED_EDGE ( 'NONE', *, *, #22531, .F. ) ;
#12214=CARTESIAN_POINT ( 'NONE',  ( -1.538852087555999892, 27.04869850837999934, 1.664720809480999986 ) ) ;
#12218=CARTESIAN_POINT ( 'NONE',  ( 2.036706090186000129, 28.28937716036000083, -1.360883606431000148 ) ) ;
#12226=PLANE ( 'NONE',  #14228 ) ;
#12228=AXIS2_PLACEMENT_3D ( 'NONE', #19286, #8022, #15394 ) ;
#12229=EDGE_CURVE ( 'NONE', #12844, #20964, #9852, .T. ) ;
#12230=CARTESIAN_POINT ( 'NONE',  ( -1.425617094341268931, 30.52806882488800966, -2.032309464588828885 ) ) ;
#12234=CARTESIAN_POINT ( 'NONE',  ( -0.3272492347489287523, 27.38333333333333997, 2.500000000000001332 ) ) ;
#12238=CARTESIAN_POINT ( 'NONE',  ( -2.108931671552999987, 29.74725334348999795, 1.723862884677999974 ) ) ;
#12242=CARTESIAN_POINT ( 'NONE',  ( 2.100000000000000089, 18.89999999999999858, 1.955007544740999697E-10 ) ) ;
#12246=CARTESIAN_POINT ( 'NONE',  ( 0.6590036730604669213, 24.50443762530719027, -2.307010909781515906 ) ) ;
#12252=CARTESIAN_POINT ( 'NONE',  ( -1.767766952966000060, 30.50000000000000000, 1.767766952966000060 ) ) ;
#12255=VECTOR ( 'NONE', #10460, 1000.000000000000114 ) ;
#12257=CARTESIAN_POINT ( 'NONE',  ( -2.535357900355000194, 24.74337675623999999, -0.2234184053773999867 ) ) ;
#12263=ORIENTED_EDGE ( 'NONE', *, *, #23322, .F. ) ;
#12266=CARTESIAN_POINT ( 'NONE',  ( -4.000000000000056843, 24.75094615492120553, 2.107036910272268582 ) ) ;
#12267=ORIENTED_EDGE ( 'NONE', *, *, #20319, .T. ) ;
#12269=AXIS2_PLACEMENT_3D ( 'NONE', #12519, #8640, #4772 ) ;
#12273=CARTESIAN_POINT ( 'NONE',  ( 1.672509921849822945, 24.50639765414753768, 3.652834497693414839 ) ) ;
#12276=VERTEX_POINT ( 'NONE', #515 ) ;
#12278=CARTESIAN_POINT ( 'NONE',  ( -1.619012473651841422, 29.49616192514975666, 1.435411994078731990 ) ) ;
#12282=ORIENTED_EDGE ( 'NONE', *, *, #12322, .T. ) ;
#12291=DIRECTION ( 'NONE',  ( 0.7071067811881966980, 0.7071067811848966711, 4.825990873454977813E-08 ) ) ;
#12294=CARTESIAN_POINT ( 'NONE',  ( 0.000000000000000000, -1.550000000000000044, 0.000000000000000000 ) ) ;
#12295=CARTESIAN_POINT ( 'NONE',  ( 2.500000000000000000, 28.63419673618999894, 0.000000000000000000 ) ) ;
#12296=CARTESIAN_POINT ( 'NONE',  ( 0.000000000000000000, 9.000000000000000000, 0.000000000000000000 ) ) ;
#12301=DIRECTION ( 'NONE',  ( 1.000000000000000000, 0.000000000000000000, 0.000000000000000000 ) ) ;
#12303=CARTESIAN_POINT ( 'NONE',  ( -1.631621777345116708, 30.11277217328136402, -1.415534461727001814 ) ) ;
#12308=CARTESIAN_POINT ( 'NONE',  ( -1.391452274478730544, 23.61431841429077494, -1.593469617572546682 ) ) ;
#12309=ORIENTED_EDGE ( 'NONE', *, *, #21686, .F. ) ;
#12310=EDGE_CURVE ( 'NONE', #1169, #9922, #19326, .T. ) ;
#12315=VERTEX_POINT ( 'NONE', #2221 ) ;
#12317=DIRECTION ( 'NONE',  ( -1.000000000000000000, 0.000000000000000000, 0.000000000000000000 ) ) ;
#12321=DIRECTION ( 'NONE',  ( 0.000000000000000000, 1.000000000000000000, 0.000000000000000000 ) ) ;
#12322=EDGE_CURVE ( 'NONE', #8075, #6193, #20822, .T. ) ;
#12329=DIRECTION ( 'NONE',  ( 0.000000000000000000, -1.000000000000000000, 0.000000000000000000 ) ) ;
#12331=CARTESIAN_POINT ( 'NONE',  ( -4.000000000000000888, 26.43562577624027554, -1.040161751118715117 ) ) ;
#12338=CARTESIAN_POINT ( 'NONE',  ( -0.2419425476019000099, 26.86163313895000115, -2.456483904114000083 ) ) ;
#12339=CARTESIAN_POINT ( 'NONE',  ( 3.025523437588009568, 26.41693820796410463, 2.872015382385962656 ) ) ;
#12347=CARTESIAN_POINT ( 'NONE',  ( 0.000000000000000000, 16.89999999999999858, 0.000000000000000000 ) ) ;
#12351=CARTESIAN_POINT ( 'NONE',  ( -1.103611694251628084, 30.16587371767807824, 1.992807635840708302 ) ) ;
#12352=ADVANCED_FACE ( 'NONE', ( #5251 ), #16164, .F. ) ;
#12353=DIRECTION ( 'NONE',  ( 0.000000000000000000, 0.000000000000000000, -1.000000000000000000 ) ) ;
#12359=CARTESIAN_POINT ( 'NONE',  ( 2.500000000000000000, 28.41666666666666430, -0.3272492347489370235 ) ) ;
#12360=CARTESIAN_POINT ( 'NONE',  ( 2.675621865512000319, 29.28399530016000085, -0.5102467047576000336 ) ) ;
#12363=AXIS2_PLACEMENT_3D ( 'NONE', #13168, #15333, #7961 ) ;
#12364=ORIENTED_EDGE ( 'NONE', *, *, #14673, .T. ) ;
#12366=LINE ( 'NONE', #19753, #8723 ) ;
#12368=LINE ( 'NONE', #14721, #3040 ) ;
#12374=DIRECTION ( 'NONE',  ( 1.000000000000000000, 0.000000000000000000, 0.000000000000000000 ) ) ;
#12375=ORIENTED_EDGE ( 'NONE', *, *, #17739, .T. ) ;
#12378=CARTESIAN_POINT ( 'NONE',  ( 2.500000000000000000, 27.83419673618999823, 0.000000000000000000 ) ) ;
#12379=VERTEX_POINT ( 'NONE', #14785 ) ;
#12381=CARTESIAN_POINT ( 'NONE',  ( -2.550975086816000381, 24.01276803249999858, -0.9922851024814999255 ) ) ;
#12385=PLANE ( 'NONE',  #21550 ) ;
#12389=VERTEX_POINT ( 'NONE', #1615 ) ;
#12390=EDGE_CURVE ( 'NONE', #16342, #20086, #12407, .T. ) ;
#12394=VERTEX_POINT ( 'NONE', #7283 ) ;
#12399=CARTESIAN_POINT ( 'NONE',  ( 1.699986957659999964, 9.000014576061998284, -0.8485216275457999613 ) ) ;
#12402=ORIENTED_EDGE ( 'NONE', *, *, #18866, .F. ) ;
#12403=CARTESIAN_POINT ( 'NONE',  ( -1.852637453037785153, 26.30370469418262047, 1.202693574547283983 ) ) ;
#12404=CARTESIAN_POINT ( 'NONE',  ( -0.2347037422651374605, 29.21777112581033364, -2.147026567374833661 ) ) ;
#12407=LINE ( 'NONE', #17971, #10393 ) ;
#12409=ORIENTED_EDGE ( 'NONE', *, *, #12057, .F. ) ;
#12411=CARTESIAN_POINT ( 'NONE',  ( 0.2857557581101721755, 30.80642105250836238, -2.193578937681244678 ) ) ;
#12413=CARTESIAN_POINT ( 'NONE',  ( 0.000000000000000000, 15.00000000000000000, 0.000000000000000000 ) ) ;
#12415=ADVANCED_FACE ( 'NONE', ( #3202 ), #14557, .T. ) ;
#12416=ORIENTED_EDGE ( 'NONE', *, *, #12950, .F. ) ;
#12420=VERTEX_POINT ( 'NONE', #8765 ) ;
#12426=CARTESIAN_POINT ( 'NONE',  ( 2.243942538766000361, 29.77722651399999876, 0.6739745749383999618 ) ) ;
#12427=CIRCLE ( 'NONE', #1968, 0.1000000000000003525 ) ;
#12430=CARTESIAN_POINT ( 'NONE',  ( 0.4219218820329893593, 29.97882480414182638, -2.122083357744672494 ) ) ;
#12439=ORIENTED_EDGE ( 'NONE', *, *, #19335, .T. ) ;
#12440=DIRECTION ( 'NONE',  ( 0.000000000000000000, 0.000000000000000000, 1.000000000000000000 ) ) ;
#12443=PRODUCT_CONTEXT ( 'NONE', #4320, 'mechanical' ) ;
#12449=EDGE_CURVE ( 'NONE', #18916, #23321, #21950, .T. ) ;
#12453=CARTESIAN_POINT ( 'NONE',  ( 2.172046235086991128, 27.39994352002885236, 0.07647517823428454098 ) ) ;
#12459=CARTESIAN_POINT ( 'NONE',  ( 0.04846321314153999998, 27.25163313894999817, 2.467893978438000069 ) ) ;
#12462=ORIENTED_EDGE ( 'NONE', *, *, #1828, .T. ) ;
#12466=DIRECTION ( 'NONE',  ( -1.000000000000000000, 0.000000000000000000, 0.000000000000000000 ) ) ;
#12468=DIRECTION ( 'NONE',  ( 0.000000000000000000, 1.000000000000000000, 0.000000000000000000 ) ) ;
#12472=ADVANCED_FACE ( 'NONE', ( #19905 ), #5138, .T. ) ;
#12475=CARTESIAN_POINT ( 'NONE',  ( -2.156765450510000015, 30.19818128708999794, -0.9123105095192000080 ) ) ;
#12476=DIRECTION ( 'NONE',  ( -1.000000000000000000, 0.000000000000000000, 0.000000000000000000 ) ) ;
#12479=EDGE_LOOP ( 'NONE', ( #18621, #4690, #10726, #14121, #18323, #23429, #21752, #2640, #19263, #11924, #16876 ) ) ;
#12481=DIRECTION ( 'NONE',  ( 0.000000000000000000, 1.000000000000000000, 0.000000000000000000 ) ) ;
#12482=DIRECTION ( 'NONE',  ( 0.000000000000000000, -1.000000000000000000, 0.000000000000000000 ) ) ;
#12488=CARTESIAN_POINT ( 'NONE',  ( 2.500000000000000000, 30.23419673619000037, 0.000000000000000000 ) ) ;
#12489=ORIENTED_EDGE ( 'NONE', *, *, #10127, .F. ) ;
#12491=CARTESIAN_POINT ( 'NONE',  ( 0.1752525089982897022, 24.75094615491968852, -4.517620070270786492 ) ) ;
#12493=CARTESIAN_POINT ( 'NONE',  ( 1.848971201200000136, 25.85810122863999894, 1.749110969876999988 ) ) ;
#12502=CARTESIAN_POINT ( 'NONE',  ( -1.973459554958962414, 26.24813749873406010, 0.8485066749672629527 ) ) ;
#12504=EDGE_CURVE ( 'NONE', #20964, #11498, #21986, .T. ) ;
#12505=ORIENTED_EDGE ( 'NONE', *, *, #22074, .F. ) ;
#12507=FACE_OUTER_BOUND ( 'NONE', #9583, .T. ) ;
#12511=CARTESIAN_POINT ( 'NONE',  ( -3.000000000000000000, 19.09999999999999787, 0.000000000000000000 ) ) ;
#12514=ORIENTED_EDGE ( 'NONE', *, *, #10576, .F. ) ;
#12516=DIRECTION ( 'NONE',  ( 0.000000000000000000, 0.7071067811866525998, -0.7071067811864425456 ) ) ;
#12519=CARTESIAN_POINT ( 'NONE',  ( 0.000000000000000000, 15.00000000000000000, 0.000000000000000000 ) ) ;
#12520=CARTESIAN_POINT ( 'NONE',  ( 0.000000000000000000, -1.550000000000000044, 0.000000000000000000 ) ) ;
#12523=CARTESIAN_POINT ( 'NONE',  ( 6.356497079780072168E-07, 30.81706029784504963, -2.183072574220335849 ) ) ;
#12532=EDGE_CURVE ( 'NONE', #10909, #889, #5731, .T. ) ;
#12534=AXIS2_PLACEMENT_3D ( 'NONE', #22573, #406, #22456 ) ;
#12541=CARTESIAN_POINT ( 'NONE',  ( 1.679203100328423570, 29.89047614560958976, -1.358641863343548639 ) ) ;
#12543=ORIENTED_EDGE ( 'NONE', *, *, #6558, .F. ) ;
#12545=EDGE_CURVE ( 'NONE', #8305, #6675, #14626, .T. ) ;
#12550=CARTESIAN_POINT ( 'NONE',  ( 0.8007553318486925198, 23.87661134863360246, 2.106186139113426226 ) ) ;
#12554=CARTESIAN_POINT ( 'NONE',  ( 4.649999999999999467, 17.00000000000000000, 0.000000000000000000 ) ) ;
#12556=CARTESIAN_POINT ( 'NONE',  ( 0.9536831490418160584, 27.37231439908301311, -1.970019352804785795 ) ) ;
#12557=DIRECTION ( 'NONE',  ( -0.7071067811880967779, 0.7071067811849969242, 4.142943916964978477E-08 ) ) ;
#12566=CARTESIAN_POINT ( 'NONE',  ( -1.766837003731960287, 26.92292278627816415, -1.325251963590689197 ) ) ;
#12567=FACE_OUTER_BOUND ( 'NONE', #12479, .T. ) ;
#12568=CARTESIAN_POINT ( 'NONE',  ( 2.093630357446228718, 30.63581803265235592, -0.5390189978566096718 ) ) ;
#12571=DIRECTION ( 'NONE',  ( 1.000000000000000000, 0.000000000000000000, 0.000000000000000000 ) ) ;
#12572=CARTESIAN_POINT ( 'NONE',  ( 0.4339301335947999827, 26.47163313894999703, 2.429928970624000151 ) ) ;
#12574=CARTESIAN_POINT ( 'NONE',  ( 1.906085653762000121, 28.06364211382000207, -1.273605814386999713 ) ) ;
#12575=AXIS2_PLACEMENT_3D ( 'NONE', #6653, #21441, #10663 ) ;
#12579=DIRECTION ( 'NONE',  ( 0.000000000000000000, -1.000000000000000000, 0.000000000000000000 ) ) ;
#12580=DIRECTION ( 'NONE',  ( 1.000000000000000000, 0.000000000000000000, 0.000000000000000000 ) ) ;
#12581=B_SPLINE_CURVE_WITH_KNOTS ( 'NONE', 3,
 ( #15463, #20927, #4333, #4455, #6262, #19225 ),
 .UNSPECIFIED., .F., .F.,
 ( 4, 2, 4 ),
 ( 0.000000000000000000, 0.1676274590533611553, 0.3352549181067223105 ),
 .UNSPECIFIED. ) ;
#12582=B_SPLINE_CURVE_WITH_KNOTS ( 'NONE', 3,
 ( #9946, #2690, #7894, #2438, #8141, #8011 ),
 .UNSPECIFIED., .F., .F.,
 ( 4, 2, 4 ),
 ( 4.972458724030523193E-05, 0.0005957450933333919684, 0.001141765599426478820 ),
 .UNSPECIFIED. ) ;
#12585=CARTESIAN_POINT ( 'NONE',  ( -1.536366799937239458, 24.11666666666666359, 1.999167105995485860 ) ) ;
#12596=ORIENTED_EDGE ( 'NONE', *, *, #12532, .T. ) ;
#12597=DIRECTION ( 'NONE',  ( 0.000000000000000000, 1.000000000000000000, 0.000000000000000000 ) ) ;
#12599=CARTESIAN_POINT ( 'NONE',  ( 2.402140947178999647E-14, 29.00000000000000000, 2.500000000000000000 ) ) ;
#12606=CARTESIAN_POINT ( 'NONE',  ( -4.000000000000000000, 26.50000000000000711, 0.3708744353061897980 ) ) ;
#12608=EDGE_CURVE ( 'NONE', #16051, #8097, #92, .T. ) ;
#12609=CARTESIAN_POINT ( 'NONE',  ( 2.478485849303000421, 24.32535507907999772, 0.5788465350207999682 ) ) ;
#12611=CONICAL_SURFACE ( 'NONE', #12228, 2.154903751016000069, 0.7853981633972997312 ) ;
#12615=CARTESIAN_POINT ( 'NONE',  ( 2.053005267516999902E-14, 28.63049582772000079, 2.160000000000000142 ) ) ;
#12616=DIRECTION ( 'NONE',  ( 0.000000000000000000, -1.000000000000000000, 0.000000000000000000 ) ) ;
#12619=CARTESIAN_POINT ( 'NONE',  ( -1.972981379884462871, 26.24919170867575602, 0.8522811625499435717 ) ) ;
#12620=FACE_BOUND ( 'NONE', #10336, .T. ) ;
#12622=EDGE_CURVE ( 'NONE', #15489, #13137, #19017, .T. ) ;
#12624=CARTESIAN_POINT ( 'NONE',  ( 1.048523528441000163, 25.02545588595999959, -1.870813874093000040 ) ) ;
#12626=DIRECTION ( 'NONE',  ( -0.9947502446910230223, 0.000000000000000000, 0.1023325494999024060 ) ) ;
#12630=DIRECTION ( 'NONE',  ( 0.000000000000000000, 1.000000000000000000, 0.000000000000000000 ) ) ;
#12633=CARTESIAN_POINT ( 'NONE',  ( 0.2691697527663042266, 24.02083186604081888, -2.518926031034142810 ) ) ;
#12634=DIRECTION ( 'NONE',  ( 0.000000000000000000, -1.000000000000000000, -1.745863169774000102E-14 ) ) ;
#12636=ADVANCED_FACE ( 'NONE', ( #17202 ), #4012, .T. ) ;
#12643=VECTOR ( 'NONE', #9116, 1000.000000000000000 ) ;
#12651=CARTESIAN_POINT ( 'NONE',  ( -2.404489386789158356, 26.49040384242090695, 3.230569558791225315 ) ) ;
#12654=CARTESIAN_POINT ( 'NONE',  ( 2.256069968103000090, 29.84916353467000150, -0.6321931223507000208 ) ) ;
#12657=CIRCLE ( 'NONE', #11495, 2.399999999999999911 ) ;
#12659=CARTESIAN_POINT ( 'NONE',  ( 1.973751245779984620, 29.85710109731691020, -0.8775164263322219327 ) ) ;
#12663=CIRCLE ( 'NONE', #8796, 4.625000000000000000 ) ;
#12664=CARTESIAN_POINT ( 'NONE',  ( -0.9357423685147192582, 23.62724388030657252, -1.910385039341345736 ) ) ;
#12665=ORIENTED_EDGE ( 'NONE', *, *, #9505, .T. ) ;
#12669=EDGE_CURVE ( 'NONE', #18419, #18500, #15093, .T. ) ;
#12671=ORIENTED_EDGE ( 'NONE', *, *, #22955, .F. ) ;
#12672=DIRECTION ( 'NONE',  ( 1.000000000000000000, 0.000000000000000000, 0.000000000000000000 ) ) ;
#12677=ORIENTED_EDGE ( 'NONE', *, *, #1870, .F. ) ;
#12681=ADVANCED_FACE ( 'NONE', ( #7031 ), #22743, .T. ) ;
#12686=CARTESIAN_POINT ( 'NONE',  ( 2.172617890951596298, 26.60490896355391754, -0.008667336465691470940 ) ) ;
#12688=CARTESIAN_POINT ( 'NONE',  ( 1.756867461946528763, 30.68286621462199193, -1.256417070536908653 ) ) ;
#12693=AXIS2_PLACEMENT_3D ( 'NONE', #13630, #17273, #19462 ) ;
#12695=CARTESIAN_POINT ( 'NONE',  ( 1.347456777940000183, 27.86864211382000178, 1.854615231836999945 ) ) ;
#12702=CARTESIAN_POINT ( 'NONE',  ( 2.434931691670793263, 24.36666666666667425, 0.6543697108981854083 ) ) ;
#12704=B_SPLINE_CURVE_WITH_KNOTS ( 'NONE', 3,
 ( #20425, #10872, #14609, #5418, #1428, #21774, #20078, #11102, #16186, #23933, #9048, #5639, #3375, #12908, #3834, #14495, #20190, #1898, #3599, #19956, #8825, #12688, #22120, #10982, #18367, #14724, #20306, #7104, #1658, #3710, #11230, #3492, #9165, #16541, #14381, #12568, #23588, #9288, #5528, #16662, #1553, #6991, #8937, #11581, #181, #19070, #2242, #17021, #297, #7820, #9516, #9637, #6236, #420, #17261, #22346, #15073, #2485, #5765, #20657, #4068, #20778, #17140, #20903, #4307, #15190, #22587, #4185, #20543, #11461, #3954, #18838, #18957, #11698, #5992, #2364, #13150, #13376, #11345, #9400, #9754, #9874, #18717, #536, #659, #7942, #15307, #8064, #6110, #22701, #15435, #7703, #13617, #22822, #13504, #21016, #4427, #18608, #2014, #16772, #7571, #14951, #16894, #2127, #22468, #5879, #13264, #2858, #8553, #19693, #17388, #14110, #17509, #17877, #10367, #11944, #23302, #17631, #13739, #16029, #13989, #784, #21137, #2609, #6718, #10241, #8185, #3109, #23188, #902, #6485, #4551, #6606, #4679, #8429, #14233, #19195, #15797, #15911, #6357, #4917, #1028, #21381, #19329, #4797, #10493, #12182, #15669, #13867, #21505, #2738, #19450, #19571, #2976, #12303, #1279, #10119, #8664, #8304, #23422, #17756, #11818, #12065, #23058, #6839, #21629, #21271, #1160, #9998, #15553, #22940, #6963, #18341, #5048, #21976, #12430, #10725, #23671, #11074, #21860, #19813, #7311, #14355, #14582, #16278, #1399, #1523, #7425, #7190, #14808, #9138, #3227, #10610, #20280, #3684, #14467, #17994, #5159, #16153, #18458, #21746, #5390, #23555, #8791, #12541, #19929, #3347, #10955, #18117, #16393, #12775, #1633, #8912, #5271, #1869, #7080, #12659, #14700, #20048, #3464, #10849, #20166, #3572, #18231, #9022, #23784, #1751, #23903, #16514, #22091, #5501, #12879, #9258, #16634, #43, #16865, #5616, #268, #2455, #16743, #4283, #9371, #7674, #15049, #11434, #22442, #18808, #155, #11199, #7546, #12998, #17113, #13237, #18582, #6080, #9607, #3925, #5852, #14924, #16994, #20629, #628, #20399, #2216, #18933, #22319, #15279, #1986, #4040, #510, #22558, #394, #11671, #9728, #7792, #13473, #11318, #17228, #22671, #15162, #19045, #2340, #20519, #20875, #5736, #7912, #20748, #13124, #11552, #8030, #9846, #22202, #5964, #3805, #18693, #2100, #9490, #13349, #4157, #13960, #15524, #15403, #21108, #10091, #21476, #8277, #22793, #15639, #17352, #23277, #3080, #873, #21236, #13836, #6206, #11790, #17478, #1129, #13591, #21354, #23032, #6449, #4400, #22911, #2575, #14082, #755, #12278, #13711, #6691, #20988, #4519, #12155, #2831, #12036, #4770, #10338, #6329, #4649, #17728, #17853, #11912, #19295, #8527, #2708, #19419, #9966, #19667, #10211, #19544, #17604, #999, #19164, #8399, #8157, #15886, #15767, #23156, #6576, #2951, #4891, #10466, #1248, #3631, #13180, #3523, #14986, #14206, #3983, #5020, #11015, #18639, #23395, #7486, #16576, #20569, #10907, #20458, #11377, #22041, #23966, #5797, #7252, #214, #6814, #5450, #5675, #20337, #5563, #14871, #3869, #23842, #18400, #11261, #18749, #12833, #1810, #7372, #21603, #12404, #20115, #8638, #3745, #13062, #14643, #12940, #18291, #1930, #1691, #9435, #14756, #22152, #20227, #11134, #9198, #18520, #16001, #9317, #7609, #9081, #16692, #16452, #101, #22258, #2045, #16806, #22383, #4461, #11851, #15344, #9785, #11730, #4099, #18985, #11496, #4222, #19104, #19231, #17171, #9906, #13292, #9552, #22733, #22855, #20691, #2644, #5906, #11616, #10040, #2516, #6148, #8219, #13651, #2396, #17424, #7852, #21173, #818, #4338, #22972, #15586, #449, #6389, #2279, #21048, #695, #17052, #15469, #4585, #13772, #11978, #566, #6269 ),
 .UNSPECIFIED., .F., .F.,
 ( 4, 2, 2, 2, 1, 1, 1, 2, 2, 2, 2, 1, 2, 2, 2, 2, 1, 1, 1, 2, 2, 2, 2, 1, 1, 1, 2, 2, 2, 2, 1, 2, 2, 2, 2, 2, 2, 1, 1, 1, 1, 2, 2, 2, 2, 2, 1, 1, 1, 2, 2, 2, 2, 1, 2, 2, 2, 2, 1, 1, 1, 2, 2, 2, 2, 2, 2, 2, 2, 2, 2, 1, 1, 1, 2, 2, 2, 1, 1, 2, 2, 2, 2, 2, 2, 2, 1, 1, 2, 2, 2, 1, 1, 1, 2, 2, 2, 2, 1, 2, 2, 2, 2, 2, 2, 2, 1, 1, 1, 2, 2, 2, 1, 1, 1, 2, 2, 2, 2, 2, 2, 2, 2, 2, 2, 2, 2, 2, 2, 2, 2, 1, 1, 1, 2, 2, 2, 2, 2, 2, 2, 1, 1, 1, 1, 2, 2, 2, 2, 1, 2, 2, 2, 2, 1, 2, 2, 2, 2, 2, 1, 1, 1, 2, 2, 2, 1, 1, 2, 2, 2, 2, 1, 2, 2, 2, 2, 1, 1, 2, 2, 2, 2, 1, 1, 1, 2, 2, 2, 2, 1, 1, 1, 2, 2, 2, 2, 1, 1, 1, 2, 2, 2, 2, 1, 1, 1, 1, 2, 2, 2, 2, 2, 2, 2, 1, 1, 1, 1, 2, 2, 2, 2, 1, 1, 1, 2, 2, 2, 2, 1, 1, 1, 2, 2, 2, 2, 1, 1, 1, 2, 2, 2, 2, 2, 1, 1, 2, 2, 2, 2, 1, 1, 1, 1, 1, 2, 2, 2, 2, 2, 1, 2, 2, 2, 2, 1, 1, 1, 2, 2, 2, 2, 2, 1, 1, 2, 2, 2, 2, 2, 2, 2, 4 ),
 ( 0.000000000000000000, 0.03124999999998551853, 0.04687499999997828126, 0.05468749999997467304, 0.05859374999997287586, 0.06054687499997197381, 0.06152343749997152278, 0.06201171874997130767, 0.06249999999997109257, 0.07031249999996704025, 0.07421874999996501410, 0.07617187499996398714, 0.07714843749996350142, 0.07812499999996300182, 0.08593749999995900501, 0.08984374999995702049, 0.09179687499995603517, 0.09277343749995553557, 0.09326171874995527189, 0.09350585937495514699, 0.09374999999995502209, 0.1015624999999509143, 0.1054687499999488465, 0.1074218749999478195, 0.1083984374999472783, 0.1088867187499470285, 0.1091308593749469175, 0.1093749999999468064, 0.1171874999999435313, 0.1210937499999418798, 0.1230468749999410749, 0.1240234374999406586, 0.1249999999999402284, 0.1562499999999271139, 0.1718749999999205358, 0.1796874999999172606, 0.1835937499999156231, 0.1855468749999147904, 0.1865234374999143740, 0.1870117187499141798, 0.1872558593749140965, 0.1873779296874140410, 0.1874999999999139577, 0.1953124999999100719, 0.1992187499999081290, 0.2011718749999071298, 0.2021484374999066580, 0.2026367187499064082, 0.2028808593749062972, 0.2030029296874062417, 0.2031249999999061862, 0.2109374999999031886, 0.2148437499999016898, 0.2167968749999009404, 0.2177734374999005795, 0.2187499999999002187, 0.2265624999998971656, 0.2304687499998956390, 0.2324218749998948619, 0.2333984374998944733, 0.2338867187498942513, 0.2341308593748941680, 0.2343749999998940847, 0.2421874999998911981, 0.2460937499998897549, 0.2499999999998883116, 0.2656249999998824829, 0.2812499999998765987, 0.2968749999998707700, 0.3046874999998678279, 0.3085937499998663847, 0.3105468749998656630, 0.3115234374998652744, 0.3120117187498651079, 0.3122558593748649969, 0.3124999999998648859, 0.3164062499998635536, 0.3183593749998628319, 0.3193359374998624989, 0.3198242187498623323, 0.3203124999998621658, 0.3242187499998608335, 0.3281249999998595568, 0.3359374999998568923, 0.3398437499998555600, 0.3417968749998548939, 0.3427734374998545608, 0.3432617187498543387, 0.3435058593748542277, 0.3437499999998541167, 0.3515624999998508415, 0.3554687499998492317, 0.3574218749998483990, 0.3583984374998480105, 0.3588867187498478439, 0.3593749999998476774, 0.3671874999998447908, 0.3710937499998433475, 0.3730468749998426814, 0.3740234374998423483, 0.3749999999998419598, 0.3906249999998364641, 0.4062499999998309685, 0.4218749999998254174, 0.4296874999998226419, 0.4335937499998212541, 0.4355468749998205880, 0.4365234374998202549, 0.4370117187498200884, 0.4372558593748200328, 0.4374999999998199773, 0.4453124999998176459, 0.4492187499998164246, 0.4511718749998158695, 0.4521484374998155364, 0.4526367187498153699, 0.4531249999998152034, 0.4570312499998141487, 0.4589843749998135936, 0.4599609374998133715, 0.4609374999998131495, 0.4648437499998120948, 0.4667968749998115952, 0.4677734374998113176, 0.4687499999998110400, 0.4765624999998089861, 0.4804687499998079314, 0.4824218749998074318, 0.4843749999998068767, 0.4921874999998047673, 0.4960937499998037681, 0.4980468749998032130, 0.4990234374998029909, 0.4995117187498028799, 0.4997558593748028244, 0.4999999999998027134, 0.5156249999997973843, 0.5312499999997920552, 0.5468749999997866151, 0.5546874999997840616, 0.5585937499997826183, 0.5605468749997819522, 0.5615234374997816191, 0.5620117187497813971, 0.5622558593747812861, 0.5623779296872812861, 0.5624999999997811750, 0.5664062499997789546, 0.5683593749997778444, 0.5693359374997772893, 0.5698242187497769562, 0.5703124999997766231, 0.5742187499997741806, 0.5761718749997730704, 0.5771484374997725153, 0.5776367187497721822, 0.5781249999997718492, 0.5859374999997716271, 0.5898437499997716271, 0.5917968749997716271, 0.5927734374997716271, 0.5932617187497716271, 0.5935058593747716271, 0.5936279296872716271, 0.5937499999997717381, 0.5976562499997720712, 0.5996093749997722933, 0.6005859374997724043, 0.6010742187497725153, 0.6015624999997726263, 0.6054687499997730704, 0.6074218749997732925, 0.6083984374997734035, 0.6088867187497735145, 0.6093749999997735145, 0.6171874999997747357, 0.6210937499997752909, 0.6230468749997755129, 0.6240234374997756239, 0.6245117187497757349, 0.6249999999997758460, 0.6328124999997768452, 0.6367187499997772893, 0.6386718749997775113, 0.6396484374997776223, 0.6401367187497777334, 0.6403808593747777334, 0.6406249999997777334, 0.6484374999997783995, 0.6523437499997787326, 0.6542968749997789546, 0.6552734374997790656, 0.6557617187497790656, 0.6560058593747790656, 0.6562499999997790656, 0.6640624999997800648, 0.6679687499997806199, 0.6699218749997808420, 0.6708984374997809530, 0.6713867187497810640, 0.6716308593747810640, 0.6718749999997810640, 0.6796874999997818412, 0.6835937499997822853, 0.6855468749997825073, 0.6865234374997825073, 0.6870117187497826183, 0.6872558593747827294, 0.6873779296872828404, 0.6874999999997828404, 0.7031249999997902789, 0.7187499999997977174, 0.7343749999998051559, 0.7421874999998088196, 0.7460937499998107070, 0.7480468749998115952, 0.7490234374998120392, 0.7495117187498122613, 0.7497558593748123723, 0.7498779296873123723, 0.7499999999998123723, 0.7578124999998175904, 0.7617187499998201439, 0.7636718749998213651, 0.7646484374998220312, 0.7651367187498223643, 0.7653808593748225864, 0.7656249999998228084, 0.7734374999998279154, 0.7773437499998303579, 0.7792968749998316902, 0.7802734374998323563, 0.7807617187498326894, 0.7810058593748329114, 0.7812499999998331335, 0.7890624999998387956, 0.7929687499998416822, 0.7949218749998431255, 0.7958984374998437916, 0.7963867187498441247, 0.7966308593748443467, 0.7968749999998445688, 0.8046874999998504530, 0.8085937499998534506, 0.8105468749998550049, 0.8115234374998557820, 0.8120117187498561151, 0.8122558593748563371, 0.8124999999998565592, 0.8437499999998797628, 0.8593749999998914202, 0.8671874999998971933, 0.8710937499999001910, 0.8730468749999016342, 0.8740234374999024114, 0.8745117187499027445, 0.8747558593749029665, 0.8749999999999031886, 0.8828124999999086286, 0.8867187499999114042, 0.8886718749999128475, 0.8896484374999135136, 0.8901367187499138467, 0.8906249999999141798, 0.8984374999999198419, 0.9023437499999227285, 0.9042968749999240607, 0.9052734374999248379, 0.9057617187499251710, 0.9060058593749253930, 0.9062499999999256151, 0.9140624999999314992, 0.9179687499999342748, 0.9199218749999357181, 0.9208984374999364952, 0.9213867187499368283, 0.9216308593749370504, 0.9218749999999372724, 0.9296874999999434896, 0.9335937499999467093, 0.9374999999999499289, 0.9687499999999749090, 0.9843749999999874545, 1.000000000000000000 ),
 .UNSPECIFIED. ) ;
#12708=CARTESIAN_POINT ( 'NONE',  ( 2.500000000000000000, 29.43419673618999965, 0.000000000000000000 ) ) ;
#12709=CARTESIAN_POINT ( 'NONE',  ( -0.1830351089131000142, 30.75454386126000017, -2.142918224942000016 ) ) ;
#12712=ORIENTED_EDGE ( 'NONE', *, *, #12918, .T. ) ;
#12713=DIRECTION ( 'NONE',  ( 0.000000000000000000, 1.000000000000000000, 0.000000000000000000 ) ) ;
#12716=DIRECTION ( 'NONE',  ( 0.000000000000000000, -1.000000000000000000, 0.000000000000000000 ) ) ;
#12724=LINE ( 'NONE', #12378, #8044 ) ;
#12726=CARTESIAN_POINT ( 'NONE',  ( 1.541590903664999956, 24.04481553841000263, 1.514776262644000004 ) ) ;
#12728=FACE_OUTER_BOUND ( 'NONE', #11085, .T. ) ;
#12730=CARTESIAN_POINT ( 'NONE',  ( 2.434931691670788823, 27.63333333333332931, -0.6543697108982009514 ) ) ;
#12732=ORIENTED_EDGE ( 'NONE', *, *, #12808, .T. ) ;
#12739=CARTESIAN_POINT ( 'NONE',  ( 0.8474240257066999460, 25.43235017058999858, 2.175890254930000101 ) ) ;
#12744=EDGE_CURVE ( 'NONE', #14191, #9876, #7910, .T. ) ;
#12747=DIRECTION ( 'NONE',  ( 1.000000000000000000, 0.000000000000000000, 0.000000000000000000 ) ) ;
#12748=DIRECTION ( 'NONE',  ( 0.000000000000000000, 1.000000000000000000, 0.000000000000000000 ) ) ;
#12750=ORIENTED_EDGE ( 'NONE', *, *, #16515, .T. ) ;
#12755=ORIENTED_EDGE ( 'NONE', *, *, #14686, .F. ) ;
#12757=CARTESIAN_POINT ( 'NONE',  ( 2.299241366213215620, 30.70075862423665569, -0.3023531701502548130 ) ) ;
#12758=EDGE_CURVE ( 'NONE', #13776, #5466, #10502, .T. ) ;
#12773=CARTESIAN_POINT ( 'NONE',  ( -2.031444841857999783, 30.28078565870999839, 1.167369564227999978 ) ) ;
#12775=CARTESIAN_POINT ( 'NONE',  ( 1.769171358304295394, 29.88179273471633124, -1.240663272628178770 ) ) ;
#12777=CARTESIAN_POINT ( 'NONE',  ( -1.792464842300000027, 23.90299219745999793, 1.497497242616000257 ) ) ;
#12779=CARTESIAN_POINT ( 'NONE',  ( -0.8632614635461032249, 23.63695097697195280, -1.954829944972962696 ) ) ;
#12780=ORIENTED_EDGE ( 'NONE', *, *, #11278, .F. ) ;
#12782=DIRECTION ( 'NONE',  ( 0.000000000000000000, 0.000000000000000000, -1.000000000000000000 ) ) ;
#12786=EDGE_LOOP ( 'NONE', ( #22240, #3200, #21840, #15359, #9439, #22365, #18797, #4563 ) ) ;
#12789=DIRECTION ( 'NONE',  ( 0.000000000000000000, 1.000000000000000000, 0.000000000000000000 ) ) ;
#12800=CARTESIAN_POINT ( 'NONE',  ( -1.940745759242866963, 27.86371367745754668, 0.9740794332273453593 ) ) ;
#12805=CYLINDRICAL_SURFACE ( 'NONE', #16571, 3.000000000000000000 ) ;
#12807=CARTESIAN_POINT ( 'NONE',  ( -2.234660536879999881, 26.26021896306000158, 0.4903019467995999303 ) ) ;
#12808=EDGE_CURVE ( 'NONE', #15539, #13137, #20603, .T. ) ;
#12815=ORIENTED_EDGE ( 'NONE', *, *, #14578, .T. ) ;
#12822=CARTESIAN_POINT ( 'NONE',  ( -2.309787837468000316, 29.47020436186999959, 0.3857820856266000464 ) ) ;
#12823=EDGE_CURVE ( 'NONE', #10102, #18875, #12724, .T. ) ;
#12827=CARTESIAN_POINT ( 'NONE',  ( 0.000000000000000000, 26.35000000000000142, 0.000000000000000000 ) ) ;
#12833=CARTESIAN_POINT ( 'NONE',  ( -0.2898344006641048187, 29.22106918680644938, -2.140405143612640337 ) ) ;
#12834=CARTESIAN_POINT ( 'NONE',  ( 0.000000000000000000, 23.50000000000000000, 0.000000000000000000 ) ) ;
#12835=EDGE_LOOP ( 'NONE', ( #10522, #20505, #801, #9063 ) ) ;
#12836=EDGE_CURVE ( 'NONE', #8097, #367, #16566, .T. ) ;
#12837=DIRECTION ( 'NONE',  ( 0.000000000000000000, -1.000000000000000000, 1.493818482293000218E-14 ) ) ;
#12839=CARTESIAN_POINT ( 'NONE',  ( 3.099999999996000177, 22.00000000000000000, 5.570939916054706312E-07 ) ) ;
#12841=LINE ( 'NONE', #18411, #8409 ) ;
#12844=VERTEX_POINT ( 'NONE', #7855 ) ;
#12848=ORIENTED_EDGE ( 'NONE', *, *, #13164, .F. ) ;
#12850=CARTESIAN_POINT ( 'NONE',  ( -0.8096296179201000198, 24.64120919954999778, 1.985911886929999870 ) ) ;
#12854=CARTESIAN_POINT ( 'NONE',  ( 1.474730788452000008, 29.79525031396000045, -1.589135993989999829 ) ) ;
#12856=DIRECTION ( 'NONE',  ( 0.000000000000000000, 1.000000000000000000, 0.000000000000000000 ) ) ;
#12859=DIRECTION ( 'NONE',  ( 0.000000000000000000, 0.000000000000000000, -1.000000000000000000 ) ) ;
#12866=CARTESIAN_POINT ( 'NONE',  ( -1.812210406530999851, 26.78462896666999882, 1.960438172911999954 ) ) ;
#12867=VERTEX_POINT ( 'NONE', #7613 ) ;
#12871=ORIENTED_EDGE ( 'NONE', *, *, #13758, .F. ) ;
#12873=VECTOR ( 'NONE', #4874, 1000.000000000000000 ) ;
#12879=CARTESIAN_POINT ( 'NONE',  ( 2.161923304883017760, 29.80033983020846478, 0.05993981612989816160 ) ) ;
#12880=VERTEX_POINT ( 'NONE', #4225 ) ;
#12881=CARTESIAN_POINT ( 'NONE',  ( -0.1642833103220000257, 23.62380113545999905, -2.215518340065000036 ) ) ;
#12885=CARTESIAN_POINT ( 'NONE',  ( -0.7409725061051504191, 24.55264775341515104, -2.232429595175999371 ) ) ;
#12888=VERTEX_POINT ( 'NONE', #22156 ) ;
#12899=EDGE_CURVE ( 'NONE', #6008, #15539, #2987, .T. ) ;
#12903=CARTESIAN_POINT ( 'NONE',  ( -2.146066666875728668, 27.82396194969284409, 0.3297587073040745276 ) ) ;
#12906=AXIS2_PLACEMENT_3D ( 'NONE', #2932, #4380, #13942 ) ;
#12908=CARTESIAN_POINT ( 'NONE',  ( 1.412639476726861298, 30.71297323210350072, -1.633891639758391801 ) ) ;
#12909=ORIENTED_EDGE ( 'NONE', *, *, #7191, .T. ) ;
#12911=FACE_OUTER_BOUND ( 'NONE', #22235, .T. ) ;
#12914=CARTESIAN_POINT ( 'NONE',  ( 0.4903019467994999547, 28.40521896306000116, -2.234660536879999881 ) ) ;
#12915=AXIS2_PLACEMENT_3D ( 'NONE', #13823, #21223, #17716 ) ;
#12917=ORIENTED_EDGE ( 'NONE', *, *, #4184, .F. ) ;
#12918=EDGE_CURVE ( 'NONE', #7342, #21878, #9556, .T. ) ;
#12921=CARTESIAN_POINT ( 'NONE',  ( 1.603553703893112470, 28.72969600569719617, 1.618016667675826525 ) ) ;
#12922=ORIENTED_EDGE ( 'NONE', *, *, #19169, .F. ) ;
#12926=ADVANCED_FACE ( 'NONE', ( #22620 ), #23126, .T. ) ;
#12928=CARTESIAN_POINT ( 'NONE',  ( 0.4649696821386000156, 28.87458687759999876, 2.295119936837000107 ) ) ;
#12934=LINE ( 'NONE', #5328, #10828 ) ;
#12936=CARTESIAN_POINT ( 'NONE',  ( 0.000000000000000000, 26.34999999328000087, 0.000000000000000000 ) ) ;
#12940=CARTESIAN_POINT ( 'NONE',  ( 0.2397730383284118749, 29.18954072692674018, -2.146720939784232840 ) ) ;
#12944=AXIS2_PLACEMENT_3D ( 'NONE', #7763, #127, #5823 ) ;
#12945=ORIENTED_EDGE ( 'NONE', *, *, #4039, .F. ) ;
#12946=CARTESIAN_POINT ( 'NONE',  ( -2.109346313336999845, 24.70761240519000168, 1.043221774710999972 ) ) ;
#12949=CARTESIAN_POINT ( 'NONE',  ( 0.000000000000000000, -1.550000000000000044, 0.000000000000000000 ) ) ;
#12950=EDGE_CURVE ( 'NONE', #7342, #20095, #17055, .T. ) ;
#12956=AXIS2_PLACEMENT_3D ( 'NONE', #3736, #16334, #18741 ) ;
#12957=DIRECTION ( 'NONE',  ( 0.000000000000000000, -1.000000000000000000, 0.000000000000000000 ) ) ;
#12958=DIRECTION ( 'NONE',  ( -0.9967542221350019771, 0.000000000000000000, -0.08050478654122018851 ) ) ;
#12962=EDGE_CURVE ( 'NONE', #1045, #19401, #13848, .T. ) ;
#12963=CARTESIAN_POINT ( 'NONE',  ( 1.354564830409000109, 24.66385679777999940, 1.902051882269999883 ) ) ;
#12967=CARTESIAN_POINT ( 'NONE',  ( -2.209175327471999850, 30.73332322239999925, 0.9911013963042000219 ) ) ;
#12969=FACE_OUTER_BOUND ( 'NONE', #9152, .T. ) ;
#12974=AXIS2_PLACEMENT_3D ( 'NONE', #4254, #11758, #2543 ) ;
#12976=ORIENTED_EDGE ( 'NONE', *, *, #20520, .T. ) ;
#12982=CARTESIAN_POINT ( 'NONE',  ( -1.733846816785000078, 27.36962896666999967, -2.030073792688000367 ) ) ;
#12987=AXIS2_PLACEMENT_3D ( 'NONE', #10084, #10689, #21714 ) ;
#12991=AXIS2_PLACEMENT_3D ( 'NONE', #14588, #14240, #12782 ) ;
#12995=CARTESIAN_POINT ( 'NONE',  ( 1.319569304714000024, 30.27086167420000251, 1.751203780500999896 ) ) ;
#12998=CARTESIAN_POINT ( 'NONE',  ( 1.284731885223538095, 29.68481603961470228, 1.736443197320483911 ) ) ;
#13000=CARTESIAN_POINT ( 'NONE',  ( 1.625542394206999974, 24.11238549395999797, 1.677209909501000240 ) ) ;
#13007=DIRECTION ( 'NONE',  ( 0.000000000000000000, 0.000000000000000000, -1.000000000000000000 ) ) ;
#13013=CONICAL_SURFACE ( 'NONE', #2577, 4.309401076758999416, 1.119376321708719590 ) ;
#13019=CARTESIAN_POINT ( 'NONE',  ( 0.000000000000000000, 22.00131761696259503, -2.948682383037075194 ) ) ;
#13021=CYLINDRICAL_SURFACE ( 'NONE', #9669, 2.500000000000000000 ) ;
#13030=CARTESIAN_POINT ( 'NONE',  ( 1.670812126161404620, 24.75820121222832526, 1.340034817297290903 ) ) ;
#13032=CARTESIAN_POINT ( 'NONE',  ( 1.902247796447000150, 28.30771896306000102, -1.271041439915000071 ) ) ;
#13034=VECTOR ( 'NONE', #14995, 999.9999999999998863 ) ;
#13039=CARTESIAN_POINT ( 'NONE',  ( 0.000000000000000000, 18.72912878474779319, 0.000000000000000000 ) ) ;
#13040=AXIS2_PLACEMENT_3D ( 'NONE', #15954, #23348, #12353 ) ;
#13041=CARTESIAN_POINT ( 'NONE',  ( -2.277683716954383986, 29.23235820488807946, 0.03738910628819932386 ) ) ;
#13042=VERTEX_POINT ( 'NONE', #20572 ) ;
#13043=DIRECTION ( 'NONE',  ( 0.000000000000000000, 1.000000000000000000, 0.000000000000000000 ) ) ;
#13046=CARTESIAN_POINT ( 'NONE',  ( -2.500000000000000000, 29.03419673619000108, 0.000000000000000000 ) ) ;
#13047=CARTESIAN_POINT ( 'NONE',  ( -0.8763272250956999354, 30.79866367490999934, -1.893775765471000128 ) ) ;
#13048=CARTESIAN_POINT ( 'NONE',  ( 0.000000000000000000, 17.95000004008999994, -2.949999959913000236 ) ) ;
#13049=CARTESIAN_POINT ( 'NONE',  ( -1.713868625172748850, 30.87793769366716035, -1.251725348822291251 ) ) ;
#13050=CIRCLE ( 'NONE', #8027, 4.750000000000000000 ) ;
#13053=DIRECTION ( 'NONE',  ( 0.000000000000000000, -1.000000000000000000, 0.000000000000000000 ) ) ;
#13056=B_SPLINE_SURFACE_WITH_KNOTS ( 'NONE', 3, 3, ( 
 ( #2978, #17758, #23304, #6841, #6721, #14112, #19695, #21507, #3111, #10495, #1281, #8666, #16032, #14235, #20522, #5855, #4042, #7548, #11202, #22093, #3686, #2219, #14926, #16745, #18343, #9492, #13000, #3807, #157, #12777, #5503, #18584, #16867, #21978, #12881 ),
 ( #15051, #7676, #5618, #270, #13127, #22444, #3574, #22322, #1988, #11076, #5738, #5392, #9140, #16996, #18811, #2102, #3927, #20401, #14810, #20168, #9373, #16517, #396, #11320, #18694, #1753, #13239, #14702, #23905, #20631, #9609, #9260, #14584, #10957, #7313 ),
 ( #20282, #18460, #1872, #16636, #45, #7427, #22204, #21238, #4161, #4651, #7914, #12038, #11554, #19421, #15281, #19047, #2457, #875, #9731, #15165, #6331, #2833, #18935, #6208, #22674, #10093, #10213, #513, #13593, #15526, #2342, #6083, #20990, #20877, #19168 ),
 ( #2578, #2710, #22560, #13475, #8032, #17115, #23034, #17480, #17230, #4285, #11674, #15405, #631, #17606, #9849, #8279, #22795, #7794, #8159, #5966, #9968, #17354, #13839, #758, #22913, #13713, #21110, #4523, #11914, #19297, #15641, #6452, #10341, #17731, #1497 ) ),
 .UNSPECIFIED., .F., .F., .F.,
 ( 4, 4 ),
 ( 4, 1, 1, 1, 1, 1, 1, 1, 1, 1, 1, 1, 1, 1, 1, 1, 1, 1, 1, 1, 1, 1, 1, 1, 1, 1, 1, 1, 1, 1, 1, 1, 4 ),
 ( -0.2678694646895999898, 1.311704223562000005 ),
 ( -0.01431749035882000018, 0.008948431474262000945, 0.03221435330733999486, 0.05548027514042999653, 0.07874619697350999925, 0.1020121188065999940, 0.1252780406396999946, 0.1485439624727999952, 0.1718098843057999925, 0.1950758061388999931, 0.2183417279720000215, 0.2416076498050999943, 0.2648735716381999672, 0.2881394934712000477, 0.3114054153042999928, 0.3346713371373999935, 0.3579372589704999941, 0.3812031808035999947, 0.4044691026366000197, 0.4277350244697000203, 0.4510009463028000209, 0.4742668681359000216, 0.4975327899689999667, 0.5207987118021000228, 0.5440646336350999368, 0.5673305554681999929, 0.5905964773012999380, 0.6138623991343999942, 0.6371283209674999393, 0.6603942428004999643, 0.6836601646335999094, 0.7069260864666999655, 0.7301920082997999106 ),
 .UNSPECIFIED. ) ;
#13057=DIRECTION ( 'NONE',  ( 0.000000000000000000, 0.000000000000000000, 1.000000000000000000 ) ) ;
#13062=CARTESIAN_POINT ( 'NONE',  ( 0.1497631068246060015, 29.19488348412568968, -2.155278165456777195 ) ) ;
#13064=ORIENTED_EDGE ( 'NONE', *, *, #20646, .F. ) ;
#13066=ORIENTED_EDGE ( 'NONE', *, *, #20816, .T. ) ;
#13067=CARTESIAN_POINT ( 'NONE',  ( -1.592552173163000129, 25.43822112891999510, 1.461104491376000070 ) ) ;
#13068=FACE_OUTER_BOUND ( 'NONE', #18942, .T. ) ;
#13071=CARTESIAN_POINT ( 'NONE',  ( 4.625000000000000000, 15.00000000000000000, 0.000000000000000000 ) ) ;
#13072=CARTESIAN_POINT ( 'NONE',  ( 0.000000000000000000, 17.89999999999999858, 0.000000000000000000 ) ) ;
#13073=DIRECTION ( 'NONE',  ( -0.5000000000000169864, 0.000000000000000000, -0.8660254037844289376 ) ) ;
#13075=CARTESIAN_POINT ( 'NONE',  ( 4.549999999999999822, 24.49999999999999645, 0.000000000000000000 ) ) ;
#13077=COLOUR_RGB ( '', 0.31764706, 0.68627451, 0.89019608) ;
#13081=CARTESIAN_POINT ( 'NONE',  ( -2.076645445633999998, 23.70193952168000351, 0.1838767006059000009 ) ) ;
#13083=AXIS2_PLACEMENT_3D ( 'NONE', #2474, #2593, #11686 ) ;
#13087=CARTESIAN_POINT ( 'NONE',  ( -0.7558401036728000788, 30.51789656560000097, -2.438651476941999796 ) ) ;
#13092=LINE ( 'NONE', #18664, #19131 ) ;
#13101=CONICAL_SURFACE ( 'NONE', #17753, 4.309401076758999416, 1.119376321708719590 ) ;
#13105=CARTESIAN_POINT ( 'NONE',  ( 2.554499528901000183, 25.51712896667000052, -0.7744564004552999537 ) ) ;
#13110=VECTOR ( 'NONE', #11880, 1000.000000000000000 ) ;
#13112=DIRECTION ( 'NONE',  ( -0.7071067811873956721, 0.7071067811856958096, 7.036629202178957517E-08 ) ) ;
#13113=VERTEX_POINT ( 'NONE', #698 ) ;
#13119=AXIS2_PLACEMENT_3D ( 'NONE', #19636, #724, #2923 ) ;
#13120=CARTESIAN_POINT ( 'NONE',  ( -0.8842211952242999828, 29.57975725467000316, 2.001696468556000141 ) ) ;
#13121=CIRCLE ( 'NONE', #8100, 3.000000000000000000 ) ;
#13122=AXIS2_PLACEMENT_3D ( 'NONE', #1925, #16336, #13057 ) ;
#13124=CARTESIAN_POINT ( 'NONE',  ( 0.07326045961678868956, 29.60812239200971874, 2.159155182468644352 ) ) ;
#13127=CARTESIAN_POINT ( 'NONE',  ( 0.5683451982577000239, 25.66627813763999910, 2.106144784215999710 ) ) ;
#13131=ORIENTED_EDGE ( 'NONE', *, *, #17878, .T. ) ;
#13137=VERTEX_POINT ( 'NONE', #9909 ) ;
#13139=CARTESIAN_POINT ( 'NONE',  ( -2.500000000000000000, 29.60000000000000142, 0.000000000000000000 ) ) ;
#13146=LINE ( 'NONE', #6106, #16195 ) ;
#13147=DIRECTION ( 'NONE',  ( 0.000000000000000000, 1.000000000000000000, 0.000000000000000000 ) ) ;
#13150=CARTESIAN_POINT ( 'NONE',  ( 0.4694942836120984397, 30.43170351587815503, 2.108251680744269940 ) ) ;
#13157=CARTESIAN_POINT ( 'NONE',  ( 1.620993131148000144, 27.08864211382000065, 1.620993131147000055 ) ) ;
#13162=LINE ( 'NONE', #15084, #14942 ) ;
#13164=EDGE_CURVE ( 'NONE', #17309, #8412, #21229, .T. ) ;
#13168=CARTESIAN_POINT ( 'NONE',  ( 0.000000000000000000, -1.550000000000000044, 0.000000000000000000 ) ) ;
#13170=CARTESIAN_POINT ( 'NONE',  ( -1.491631619277377085, 30.87136588096693046, -1.523986932099241853 ) ) ;
#13171=ORIENTED_EDGE ( 'NONE', *, *, #9544, .F. ) ;
#13176=CARTESIAN_POINT ( 'NONE',  ( -2.100000000000000089, 18.10000000000000142, -2.368343299253000103E-10 ) ) ;
#13178=AXIS2_PLACEMENT_3D ( 'NONE', #23737, #18193, #3417 ) ;
#13180=CARTESIAN_POINT ( 'NONE',  ( -1.633777111905726498, 29.31308647643173870, -1.412695173303529339 ) ) ;
#13182=EDGE_LOOP ( 'NONE', ( #16967, #3335, #20291, #2186 ) ) ;
#13184=VERTEX_POINT ( 'NONE', #11853 ) ;
#13185=CARTESIAN_POINT ( 'NONE',  ( -0.03700557815484000618, 24.74151833367000108, 2.160944269522000027 ) ) ;
#13187=CARTESIAN_POINT ( 'NONE',  ( 0.04450989311250999614, 27.09299822780999989, 2.266578917753999889 ) ) ;
#13192=ADVANCED_FACE ( 'NONE', ( #6391 ), #16580, .T. ) ;
#13196=VERTEX_POINT ( 'NONE', #17174 ) ;
#13198=CARTESIAN_POINT ( 'NONE',  ( -0.3313809864660999804, 25.26287442561999796, 2.503738740189999756 ) ) ;
#13202=CARTESIAN_POINT ( 'NONE',  ( 2.251425272252999488, 29.54619791218000202, 0.7094205924024000742 ) ) ;
#13206=CARTESIAN_POINT ( 'NONE',  ( -1.999167105995446780, 26.71753006952333109, 1.536366799937292305 ) ) ;
#13212=ORIENTED_EDGE ( 'NONE', *, *, #21060, .F. ) ;
#13213=AXIS2_PLACEMENT_3D ( 'NONE', #3098, #10483, #17870 ) ;
#13219=CARTESIAN_POINT ( 'NONE',  ( -0.3933730402102999513, 27.55669433610000141, 2.844001364980000002 ) ) ;
#13225=DIRECTION ( 'NONE',  ( 0.7071067811905932254, 0.7071067811824932603, 1.099460927037990408E-07 ) ) ;
#13233=CARTESIAN_POINT ( 'NONE',  ( -0.9845628394066999745, 29.04793232273999948, -1.959238121737999716 ) ) ;
#13237=CARTESIAN_POINT ( 'NONE',  ( 1.238547465960351257, 29.68149730498098293, 1.769554945797824796 ) ) ;
#13238=EDGE_LOOP ( 'NONE', ( #9083, #16270, #5146, #6450, #14086 ) ) ;
#13239=CARTESIAN_POINT ( 'NONE',  ( 1.518228109745999976, 24.13072729665000082, 1.566484663595000049 ) ) ;
#13248=EDGE_CURVE ( 'NONE', #8533, #11568, #14731, .T. ) ;
#13249=ORIENTED_EDGE ( 'NONE', *, *, #792, .F. ) ;
#13254=CARTESIAN_POINT ( 'NONE',  ( 0.000000000000000000, 21.89999999999999858, -3.000000000000013323 ) ) ;
#13259=CARTESIAN_POINT ( 'NONE',  ( 0.000000000000000000, 15.00000000000000000, -3.100000000000386002 ) ) ;
#13262=CARTESIAN_POINT ( 'NONE',  ( 0.3056909699690598115, 26.48398052701158178, -2.383980527013956685 ) ) ;
#13264=CARTESIAN_POINT ( 'NONE',  ( -1.051908427655785516, 30.33894127233460125, 1.886895527404444328 ) ) ;
#13271=CARTESIAN_POINT ( 'NONE',  ( 1.852511768836999861, 25.52864211381999837, 0.9439018917105000961 ) ) ;
#13276=CARTESIAN_POINT ( 'NONE',  ( 1.549555853195504929, 29.73502040408345337, -1.669765763550722815 ) ) ;
#13278=CARTESIAN_POINT ( 'NONE',  ( -1.771853452025566655, 26.49970565133012101, 1.763679972769350623 ) ) ;
#13283=CARTESIAN_POINT ( 'NONE',  ( -1.617838176641581693, 30.87517387167590499, -1.378981570155497272 ) ) ;
#13287=CARTESIAN_POINT ( 'NONE',  ( 4.000000000000117240, 24.49999999999976907, -0.3805779584833442475 ) ) ;
#13288=ORIENTED_EDGE ( 'NONE', *, *, #13333, .F. ) ;
#13289=DIRECTION ( 'NONE',  ( 1.345655357976046922E-09, -1.000000000000000000, 0.000000000000000000 ) ) ;
#13292=CARTESIAN_POINT ( 'NONE',  ( 2.160193564748952966, 29.00404398936455763, -0.001994679732726410866 ) ) ;
#13295=CARTESIAN_POINT ( 'NONE',  ( 1.699999998870999951, 12.90000000000000036, 1.053565372968999991 ) ) ;
#13297=VECTOR ( 'NONE', #14424, 1000.000000000000000 ) ;
#13299=CARTESIAN_POINT ( 'NONE',  ( -1.723852419406000092, 26.80049822781000302, -1.472309056329999866 ) ) ;
#13306=CARTESIAN_POINT ( 'NONE',  ( 0.000000000000000000, 26.50000000000000355, 0.000000000000000000 ) ) ;
#13310=CARTESIAN_POINT ( 'NONE',  ( 2.143849369842000030, 24.75054551040999939, -1.335074848179999885 ) ) ;
#13312=CIRCLE ( 'NONE', #20671, 2.000000000000000000 ) ;
#13315=CARTESIAN_POINT ( 'NONE',  ( 2.281976920270999631, 29.61800679778000145, -0.6039657844537000830 ) ) ;
#13318=TOROIDAL_SURFACE ( 'NONE', #13720, 2.500000000000000000, 0.5500000000000000444 ) ;
#13319=CARTESIAN_POINT ( 'NONE',  ( -4.749999920006001020, 24.30000007999099765, -4.227385599170000255E-08 ) ) ;
#13320=ADVANCED_FACE ( 'NONE', ( #3718 ), #10989, .T. ) ;
#13321=CARTESIAN_POINT ( 'NONE',  ( 1.999167105995449445, 29.51753006952333180, -1.536366799937288530 ) ) ;
#13325=CARTESIAN_POINT ( 'NONE',  ( 2.257767744500999818, 25.33650334349000133, -1.547397860518000101 ) ) ;
#13326=CARTESIAN_POINT ( 'NONE',  ( 0.000000000000000000, 24.39999999221199900, 0.000000000000000000 ) ) ;
#13332=CARTESIAN_POINT ( 'NONE',  ( 2.219793368323999871, 27.95462896667000052, -1.483218624018999954 ) ) ;
#13333=EDGE_CURVE ( 'NONE', #15998, #10829, #8071, .T. ) ;
#13334=ORIENTED_EDGE ( 'NONE', *, *, #12608, .F. ) ;
#13340=VERTEX_POINT ( 'NONE', #16781 ) ;
#13345=CARTESIAN_POINT ( 'NONE',  ( -2.341484834389000014, 30.80774310834999952, -0.2625247487647999756 ) ) ;
#13348=EDGE_CURVE ( 'NONE', #20885, #17972, #7304, .T. ) ;
#13349=CARTESIAN_POINT ( 'NONE',  ( -0.3788180770592776692, 29.58146988764027085, 2.126762119974988430 ) ) ;
#13358=ORIENTED_EDGE ( 'NONE', *, *, #18141, .T. ) ;
#13361=FACE_OUTER_BOUND ( 'NONE', #254, .T. ) ;
#13376=CARTESIAN_POINT ( 'NONE',  ( 0.4444477064986781523, 30.43018009420528003, 2.113756326305517685 ) ) ;
#13377=EDGE_LOOP ( 'NONE', ( #13212, #4384, #1634 ) ) ;
#13385=CARTESIAN_POINT ( 'NONE',  ( -2.149413090608000232, 28.48696440326000001, 1.203722632180999952 ) ) ;
#13393=CARTESIAN_POINT ( 'NONE',  ( 1.981941605402921525, 27.97637690296692980, 0.8825957265570513188 ) ) ;
#13394=DIRECTION ( 'NONE',  ( 0.000000000000000000, -1.000000000000000000, 0.000000000000000000 ) ) ;
#13396=DIRECTION ( 'NONE',  ( 5.702240835238999409E-10, 0.9999999999999997780, -2.283934685009999534E-08 ) ) ;
#13397=AXIS2_PLACEMENT_3D ( 'NONE', #402, #4166, #7434 ) ;
#13402=CARTESIAN_POINT ( 'NONE',  ( 0.000000000000000000, 21.94999982584599962, 0.000000000000000000 ) ) ;
#13406=VERTEX_POINT ( 'NONE', #14449 ) ;
#13407=CIRCLE ( 'NONE', #4439, 0.5500000000000001554 ) ;
#13409=CARTESIAN_POINT ( 'NONE',  ( 2.437990915149000237, 25.92706776952000070, 0.5485649090615000167 ) ) ;
#13415=AXIS2_PLACEMENT_3D ( 'NONE', #12157, #19904, #21838 ) ;
#13419=DIRECTION ( 'NONE',  ( 0.7071067811864980568, -0.7071067811865969777, -1.093189995836995798E-08 ) ) ;
#13420=CARTESIAN_POINT ( 'NONE',  ( -2.214344957515000267, 26.11799822780999847, 0.4858445502740000310 ) ) ;
#13429=CARTESIAN_POINT ( 'NONE',  ( -0.2318060435179999934, 31.07084775298000068, -2.713913184503999876 ) ) ;
#13431=CARTESIAN_POINT ( 'NONE',  ( -0.6445284140762999048, 24.00469973582999827, -2.638471611800000005 ) ) ;
#13436=CARTESIAN_POINT ( 'NONE',  ( -1.055980501909000058, 29.22533662481999883, 2.324492492552999945 ) ) ;
#13438=CARTESIAN_POINT ( 'NONE',  ( -2.729128784747790970, 18.00000000000000000, 0.000000000000000000 ) ) ;
#13439=CYLINDRICAL_SURFACE ( 'NONE', #23415, 2.500000000000000000 ) ;
#13440=CARTESIAN_POINT ( 'NONE',  ( 0.000000000000000000, 21.89999999999999858, 0.000000000000000000 ) ) ;
#13442=ORIENTED_EDGE ( 'NONE', *, *, #19155, .F. ) ;
#13448=CARTESIAN_POINT ( 'NONE',  ( 0.000000000000000000, 21.87500000000000000, 0.000000000000000000 ) ) ;
#13451=CARTESIAN_POINT ( 'NONE',  ( 1.699999998837999904, 12.90000000000000036, -1.053565373074999867 ) ) ;
#13454=CARTESIAN_POINT ( 'NONE',  ( -2.866097959738999723, 26.58169433609999999, 0.1690226414555000001 ) ) ;
#13455=ORIENTED_EDGE ( 'NONE', *, *, #23433, .F. ) ;
#13464=FACE_OUTER_BOUND ( 'NONE', #14152, .T. ) ;
#13468=CARTESIAN_POINT ( 'NONE',  ( 2.052109269678999759, 30.34279869486999814, 0.7725448515828999829 ) ) ;
#13473=CARTESIAN_POINT ( 'NONE',  ( 0.4691844297121841589, 29.63158630830557172, 2.108311878348199997 ) ) ;
#13474=ORIENTED_EDGE ( 'NONE', *, *, #3775, .F. ) ;
#13475=CARTESIAN_POINT ( 'NONE',  ( 1.704131630875000081, 25.52532134332999902, 1.616576773546999801 ) ) ;
#13477=CARTESIAN_POINT ( 'NONE',  ( 0.000000000000000000, 18.72912878474779319, 0.000000000000000000 ) ) ;
#13478=VECTOR ( 'NONE', #11930, 1000.000000000000000 ) ;
#13484=DIRECTION ( 'NONE',  ( 0.000000000000000000, -1.000000000000000000, 0.000000000000000000 ) ) ;
#13486=AXIS2_PLACEMENT_3D ( 'NONE', #14856, #21907, #14744 ) ;
#13489=CARTESIAN_POINT ( 'NONE',  ( 4.000000000000000000, 26.47444252552741872, -0.7494995952805646455 ) ) ;
#13498=B_SPLINE_CURVE_WITH_KNOTS ( 'NONE', 3,
 ( #23110, #12359, #10540, #5093, #10657, #18045, #1450, #23234, #13918, #21314, #1081, #8846, #6648, #23609, #17811, #13789, #14043, #21436 ),
 .UNSPECIFIED., .F., .F.,
 ( 4, 2, 2, 2, 2, 2, 2, 2, 4 ),
 ( 0.000000000000000000, 0.1250000000000000555, 0.2500000000000001110, 0.3750000000000000555, 0.5000000000000000000, 0.6249999999999998890, 0.7499999999999998890, 0.8749999999999998890, 1.000000000000000000 ),
 .UNSPECIFIED. ) ;
#13500=CIRCLE ( 'NONE', #16981, 2.000000000000000000 ) ;
#13501=FILL_AREA_STYLE ('',( #22343 ) ) ;
#13502=CARTESIAN_POINT ( 'NONE',  ( 1.699999998870999951, 12.90000000000000036, 1.053565372968999991 ) ) ;
#13504=CARTESIAN_POINT ( 'NONE',  ( -0.5044265879204176128, 30.37393115978347424, 2.100552943717841181 ) ) ;
#13509=TOROIDAL_SURFACE ( 'NONE', #10440, 2.500000000000000000, 0.5500000000000000444 ) ;
#13510=CARTESIAN_POINT ( 'NONE',  ( -1.672139866504000150, 26.92696440325999774, 1.808910716397999829 ) ) ;
#13511=CIRCLE ( 'NONE', #21260, 4.625000000000000000 ) ;
#13512=DIRECTION ( 'NONE',  ( 1.000000000000000000, 0.000000000000000000, 0.000000000000000000 ) ) ;
#13514=EDGE_CURVE ( 'NONE', #12420, #14786, #1119, .T. ) ;
#13517=CARTESIAN_POINT ( 'NONE',  ( 2.000000000000000000, 24.50000000000000000, 3.464101615137999968 ) ) ;
#13520=ORIENTED_EDGE ( 'NONE', *, *, #20509, .T. ) ;
#13528=CARTESIAN_POINT ( 'NONE',  ( 1.999167105995457216, 26.95086340285667248, 1.536366799937278760 ) ) ;
#13531=CARTESIAN_POINT ( 'NONE',  ( 3.999878274658703159, 24.63336607547242707, -1.519686587934146127 ) ) ;
#13532=ORIENTED_EDGE ( 'NONE', *, *, #9911, .T. ) ;
#13534=CARTESIAN_POINT ( 'NONE',  ( -0.2616786785208999877, 26.96706776951999984, -2.656868203660999850 ) ) ;
#13539=ORIENTED_EDGE ( 'NONE', *, *, #20646, .T. ) ;
#13543=CARTESIAN_POINT ( 'NONE',  ( -1.472309056329999866, 27.58049822781000060, -1.723852419406000092 ) ) ;
#13545=CARTESIAN_POINT ( 'NONE',  ( -0.4126679282215456324, 30.83232909844395309, -2.137904739592160652 ) ) ;
#13553=CARTESIAN_POINT ( 'NONE',  ( 2.696211895155999905, 30.07815194586000018, -0.3869592438285999747 ) ) ;
#13554=CARTESIAN_POINT ( 'NONE',  ( -1.290484346291000062, 24.83723422303999939, -2.389895288096000048 ) ) ;
#13556=AXIS2_PLACEMENT_3D ( 'NONE', #20104, #3733, #1452 ) ;
#13561=CARTESIAN_POINT ( 'NONE',  ( 0.3765435872583000054, 29.19171087983999868, 2.719724165663000015 ) ) ;
#13564=ADVANCED_FACE ( 'NONE', ( #23882 ), #14648, .T. ) ;
#13571=ORIENTED_EDGE ( 'NONE', *, *, #13997, .T. ) ;
#13572=DIRECTION ( 'NONE',  ( 0.000000000000000000, -1.000000000000000000, 0.000000000000000000 ) ) ;
#13573=CARTESIAN_POINT ( 'NONE',  ( -2.102266727616999731, 23.66000000000000014, 0.4960590750638999569 ) ) ;
#13584=CARTESIAN_POINT ( 'NONE',  ( 1.702253152602459796, 12.92476687935645074, -1.054244267527355117 ) ) ;
#13588=CARTESIAN_POINT ( 'NONE',  ( -0.9118897615661000211, 29.87256183959000211, -2.172606093380000214 ) ) ;
#13591=CARTESIAN_POINT ( 'NONE',  ( -1.391465838797818266, 29.51483024477171213, 1.652436496091826745 ) ) ;
#13593=CARTESIAN_POINT ( 'NONE',  ( -0.7013385995965000230, 23.74705491642000155, 2.070322660781999780 ) ) ;
#13595=ORIENTED_EDGE ( 'NONE', *, *, #12918, .F. ) ;
#13600=EDGE_LOOP ( 'NONE', ( #18922, #246, #2189, #15387, #5707 ) ) ;
#13603=CARTESIAN_POINT ( 'NONE',  ( -1.346439123299411733, 24.53198827073828880, -3.841100253456362523 ) ) ;
#13606=CARTESIAN_POINT ( 'NONE',  ( 3.999999999999999112, 26.41068681084913194, -1.228746328088897721 ) ) ;
#13611=CARTESIAN_POINT ( 'NONE',  ( 2.500000000000000000, 27.03419673618999752, 0.000000000000000000 ) ) ;
#13615=CARTESIAN_POINT ( 'NONE',  ( -0.6543697108982035049, 28.86753006952333678, -2.434931691670788823 ) ) ;
#13617=CARTESIAN_POINT ( 'NONE',  ( -0.2706287508702177047, 30.38790270302602892, 2.145884556181206548 ) ) ;
#13625=CARTESIAN_POINT ( 'NONE',  ( -1.873164014766999896, 26.73196440325999745, -1.599833206071999969 ) ) ;
#13626=TOROIDAL_SURFACE ( 'NONE', #3221, 2.100000000000000089, 0.1000000000000000056 ) ;
#13630=CARTESIAN_POINT ( 'NONE',  ( 0.000000000000000000, 15.00000000000000000, 0.000000000000000000 ) ) ;
#13631=CARTESIAN_POINT ( 'NONE',  ( -0.9079114435473193412, 28.28457205800976126, -1.972232025669313105 ) ) ;
#13639=FACE_BOUND ( 'NONE', #9788, .T. ) ;
#13649=CARTESIAN_POINT ( 'NONE',  ( -0.6741018852137999895, 26.18706776952000226, -2.583184600869000036 ) ) ;
#13651=CARTESIAN_POINT ( 'NONE',  ( 2.070949786996742148, 28.96702299132843805, 0.6137957092266852488 ) ) ;
#13657=DIRECTION ( 'NONE',  ( 0.000000000000000000, -1.000000000000000000, 0.000000000000000000 ) ) ;
#13660=PRODUCT_DEFINITION_FORMATION_WITH_SPECIFIED_SOURCE ( 'ANY', '', #11128, .NOT_KNOWN. ) ;
#13664=CIRCLE ( 'NONE', #22948, 4.649999999999999467 ) ;
#13668=ORIENTED_EDGE ( 'NONE', *, *, #10409, .T. ) ;
#13671=CARTESIAN_POINT ( 'NONE',  ( -2.445536200447000041, 23.49107026052999814, 0.2165401555166999725 ) ) ;
#13676=DIRECTION ( 'NONE',  ( 1.000000000000000000, 0.000000000000000000, 0.000000000000000000 ) ) ;
#13679=CARTESIAN_POINT ( 'NONE',  ( 2.500000000000000000, 29.19999999999999929, 0.000000000000000000 ) ) ;
#13680=CIRCLE ( 'NONE', #16771, 1.500000000000000000 ) ;
#13688=CARTESIAN_POINT ( 'NONE',  ( 0.000000000000000000, 26.35000000000000142, 4.309401076758999416 ) ) ;
#13691=TOROIDAL_SURFACE ( 'NONE', #16779, 2.100000000000000089, 0.1000000000000000056 ) ;
#13692=VECTOR ( 'NONE', #6093, 1000.000000000000114 ) ;
#13695=CARTESIAN_POINT ( 'NONE',  ( 2.030158388880999976, 26.87419433610000397, 2.030158388880999976 ) ) ;
#13699=EDGE_CURVE ( 'NONE', #5650, #4259, #15353, .T. ) ;
#13701=CARTESIAN_POINT ( 'NONE',  ( 3.316026328257057010, 24.63336607546882817, 2.704152903937933061 ) ) ;
#13702=DIRECTION ( 'NONE',  ( -0.7071067811823850136, -0.7071067811898851252, -1.080116769369976149E-06 ) ) ;
#13708=CARTESIAN_POINT ( 'NONE',  ( 0.6836813991273753555, 24.62756664670378015, 4.224074002598932509 ) ) ;
#13711=CARTESIAN_POINT ( 'NONE',  ( -1.688436697687023758, 29.48963661612821596, 1.350056256019540157 ) ) ;
#13713=CARTESIAN_POINT ( 'NONE',  ( 2.274201110986000085, 23.98977050234999808, 0.5876087361756999750 ) ) ;
#13714=VECTOR ( 'NONE', #1020, 1000.000000000000000 ) ;
#13716=VERTEX_POINT ( 'NONE', #15026 ) ;
#13720=AXIS2_PLACEMENT_3D ( 'NONE', #9964, #754, #1495 ) ;
#13721=FACE_OUTER_BOUND ( 'NONE', #21733, .T. ) ;
#13723=ORIENTED_EDGE ( 'NONE', *, *, #14008, .F. ) ;
#13726=DIRECTION ( 'NONE',  ( -1.000000000000000000, 0.000000000000000000, 0.000000000000000000 ) ) ;
#13727=ORIENTED_EDGE ( 'NONE', *, *, #9120, .T. ) ;
#13728=CARTESIAN_POINT ( 'NONE',  ( -1.382592897918908825, 24.72515053741216562, 1.690066663980638983 ) ) ;
#13730=DIRECTION ( 'NONE',  ( 1.000000000000000000, 0.000000000000000000, 0.000000000000000000 ) ) ;
#13732=CARTESIAN_POINT ( 'NONE',  ( 4.000000000000000888, 26.44682129341587995, 0.9440428258623110302 ) ) ;
#13734=DIRECTION ( 'NONE',  ( 0.000000000000000000, -1.000000000000000000, 0.000000000000000000 ) ) ;
#13737=LINE ( 'NONE', #4304, #10470 ) ;
#13739=CARTESIAN_POINT ( 'NONE',  ( -2.147910637137995682, 30.21755022053942241, 0.2331351799471601260 ) ) ;
#13743=CARTESIAN_POINT ( 'NONE',  ( 1.259047450927257339, 27.70086340285666893, 2.184465970885639763 ) ) ;
#13747=VECTOR ( 'NONE', #8732, 1000.000000000000114 ) ;
#13748=DIRECTION ( 'NONE',  ( 0.000000000000000000, 1.000000000000000000, 0.000000000000000000 ) ) ;
#13749=ORIENTED_EDGE ( 'NONE', *, *, #9479, .F. ) ;
#13751=CARTESIAN_POINT ( 'NONE',  ( 0.5458742448588185248, 26.26180390196785908, 2.091772243866166114 ) ) ;
#13752=CARTESIAN_POINT ( 'NONE',  ( -2.089563112090822017, 27.66818174792411611, 0.6513645842518486218 ) ) ;
#13758=EDGE_CURVE ( 'NONE', #23625, #16342, #4264, .T. ) ;
#13762=CARTESIAN_POINT ( 'NONE',  ( 2.063594504837999888E-14, 28.80370090847999975, 2.160000000000000142 ) ) ;
#13763=AXIS2_PLACEMENT_3D ( 'NONE', #161, #4164, #11558 ) ;
#13764=CARTESIAN_POINT ( 'NONE',  ( 0.3272492347489454056, 26.85086340285666751, 2.499999999999998668 ) ) ;
#13766=CARTESIAN_POINT ( 'NONE',  ( 0.000000000000000000, 14.95000002005000006, 0.000000000000000000 ) ) ;
#13769=CARTESIAN_POINT ( 'NONE',  ( 0.5047246425491000998, 26.68250240009999885, 2.826365205286999860 ) ) ;
#13770=AXIS2_PLACEMENT_3D ( 'NONE', #11566, #18944, #4535 ) ;
#13772=CARTESIAN_POINT ( 'NONE',  ( 0.8066938640923024817, 28.85226775220604623, 2.013103552383532335 ) ) ;
#13776=VERTEX_POINT ( 'NONE', #17329 ) ;
#13783=CARTESIAN_POINT ( 'NONE',  ( -0.6543697108982035049, 27.26753006952333891, -2.434931691670788823 ) ) ;
#13787=ADVANCED_FACE ( 'NONE', ( #6791 ), #18092, .T. ) ;
#13788=ORIENTED_EDGE ( 'NONE', *, *, #22451, .F. ) ;
#13789=CARTESIAN_POINT ( 'NONE',  ( -2.434931691670790155, 28.76666666666667282, -0.6543697108981958444 ) ) ;
#13790=CARTESIAN_POINT ( 'NONE',  ( 1.066440661507000121, 30.89923340193000101, -2.297374585629999633 ) ) ;
#13792=CARTESIAN_POINT ( 'NONE',  ( -2.596050696748999798, 23.36428859183000029, -0.2023800179719000003 ) ) ;
#13795=AXIS2_PLACEMENT_3D ( 'NONE', #13072, #22396, #22162 ) ;
#13796=DIRECTION ( 'NONE',  ( 1.000000000000000000, 0.000000000000000000, 0.000000000000000000 ) ) ;
#13801=AXIS2_PLACEMENT_3D ( 'NONE', #9326, #16463, #20470 ) ;
#13807=CARTESIAN_POINT ( 'NONE',  ( 0.000000000000000000, 19.00000000000000000, -2.899999999999999911 ) ) ;
#13809=ORIENTED_EDGE ( 'NONE', *, *, #3934, .T. ) ;
#13811=CARTESIAN_POINT ( 'NONE',  ( 0.2737217042541190692, 24.02003154414986597, 2.176099354324680490 ) ) ;
#13819=CIRCLE ( 'NONE', #3406, 4.649999999999999467 ) ;
#13821=CARTESIAN_POINT ( 'NONE',  ( 2.434931691670791487, 30.20086340285667958, 0.6543697108981911814 ) ) ;
#13822=CARTESIAN_POINT ( 'NONE',  ( -0.05078100571018644843, 26.49647344481827815, -2.396473444817840637 ) ) ;
#13823=CARTESIAN_POINT ( 'NONE',  ( 0.000000000000000000, 16.94999982584599962, 0.000000000000000000 ) ) ;
#13826=ORIENTED_EDGE ( 'NONE', *, *, #2587, .F. ) ;
#13834=AXIS2_PLACEMENT_3D ( 'NONE', #344, #5687, #13073 ) ;
#13836=CARTESIAN_POINT ( 'NONE',  ( -1.095779270870209654, 29.53601415047671352, 1.861248250499890844 ) ) ;
#13838=ORIENTED_EDGE ( 'NONE', *, *, #18866, .T. ) ;
#13839=CARTESIAN_POINT ( 'NONE',  ( 0.4183838372234000014, 24.19916379885000168, -2.311326400246999757 ) ) ;
#13847=CARTESIAN_POINT ( 'NONE',  ( 1.346883420029665982E-05, 28.56481971072916792, 2.273192963938693190 ) ) ;
#13848=CIRCLE ( 'NONE', #16941, 2.000000000000000000 ) ;
#13853=CARTESIAN_POINT ( 'NONE',  ( -2.246347731941017223, 24.65365226805931087, -5.222125272214524731E-08 ) ) ;
#13855=DIRECTION ( 'NONE',  ( 1.000000000000000000, 0.000000000000000000, 0.000000000000000000 ) ) ;
#13858=DIRECTION ( 'NONE',  ( -1.000000000000000000, 0.000000000000000000, 0.000000000000000000 ) ) ;
#13859=AXIS2_PLACEMENT_3D ( 'NONE', #13176, #17168, #13289 ) ;
#13867=CARTESIAN_POINT ( 'NONE',  ( -1.899230582703691272, 30.14058891630886450, -1.028631790195981388 ) ) ;
#13872=CARTESIAN_POINT ( 'NONE',  ( 0.000000000000000000, 26.50000000000000355, 0.000000000000000000 ) ) ;
#13878=CIRCLE ( 'NONE', #5770, 2.750000000000000000 ) ;
#13881=CARTESIAN_POINT ( 'NONE',  ( -0.8183426631040646715, 28.58043940685084294, 2.011287406255212851 ) ) ;
#13882=CARTESIAN_POINT ( 'NONE',  ( 0.000000000000000000, 24.49999999999999645, 0.000000000000000000 ) ) ;
#13885=AXIS2_PLACEMENT_3D ( 'NONE', #5509, #8920, #1406 ) ;
#13894=DIRECTION ( 'NONE',  ( 0.000000000000000000, 0.000000000000000000, -1.000000000000000000 ) ) ;
#13895=VERTEX_POINT ( 'NONE', #14534 ) ;
#13897=CARTESIAN_POINT ( 'NONE',  ( -0.06321855798620600042, 24.77054417338800718, 2.143747832292392186 ) ) ;
#13898=CIRCLE ( 'NONE', #9646, 4.549999999999999822 ) ;
#13901=CARTESIAN_POINT ( 'NONE',  ( 3.064125534931650296, 26.41068681084918524, 2.849728451093326953 ) ) ;
#13904=ORIENTED_EDGE ( 'NONE', *, *, #2730, .T. ) ;
#13905=ADVANCED_FACE ( 'NONE', ( #12728 ), #20234, .T. ) ;
#13908=FACE_OUTER_BOUND ( 'NONE', #19858, .T. ) ;
#13911=CARTESIAN_POINT ( 'NONE',  ( 0.000000000000000000, 17.95000004008999994, 0.000000000000000000 ) ) ;
#13912=AXIS2_PLACEMENT_3D ( 'NONE', #21515, #13748, #8676 ) ;
#13918=CARTESIAN_POINT ( 'NONE',  ( 0.3272492347489343589, 28.58333333333333570, -2.500000000000000444 ) ) ;
#13919=CARTESIAN_POINT ( 'NONE',  ( 1.580360580230000034, 29.84035787434000042, 1.979290453440999853 ) ) ;
#13921=DIRECTION ( 'NONE',  ( 0.000000000000000000, -1.000000000000000000, 0.000000000000000000 ) ) ;
#13923=ORIENTED_EDGE ( 'NONE', *, *, #14522, .T. ) ;
#13925=CARTESIAN_POINT ( 'NONE',  ( 0.000000000000000000, 13.00000000000000000, 0.000000000000000000 ) ) ;
#13926=CARTESIAN_POINT ( 'NONE',  ( 0.5907988678278000005, 28.40181313824999876, 2.681278056231000129 ) ) ;
#13929=CARTESIAN_POINT ( 'NONE',  ( 0.000000000000000000, -1.550000000000000044, 0.000000000000000000 ) ) ;
#13930=DIRECTION ( 'NONE',  ( 0.7071067811868960717, 0.7071067811861969643, 5.329912238617969693E-08 ) ) ;
#13938=CARTESIAN_POINT ( 'NONE',  ( -0.6531029714935000507, 25.61332603901999860, 2.260778022581000357 ) ) ;
#13942=DIRECTION ( 'NONE',  ( 1.000000000000000000, 0.000000000000000000, 0.000000000000000000 ) ) ;
#13946=CARTESIAN_POINT ( 'NONE',  ( 0.000000000000000000, 22.00000000000000000, 0.000000000000000000 ) ) ;
#13948=EDGE_LOOP ( 'NONE', ( #1400, #1416, #16154, #18877 ) ) ;
#13949=ADVANCED_FACE ( 'NONE', ( #22268 ), #22624, .T. ) ;
#13955=CARTESIAN_POINT ( 'NONE',  ( -4.000000000000000000, 24.80000000000000426, 2.309401076759000304 ) ) ;
#13958=PLANE ( 'NONE',  #2900 ) ;
#13960=CARTESIAN_POINT ( 'NONE',  ( -0.4927160651647209955, 29.57458059066297196, 2.103003212775674147 ) ) ;
#13961=ORIENTED_EDGE ( 'NONE', *, *, #1439, .T. ) ;
#13962=CARTESIAN_POINT ( 'NONE',  ( 2.500000000000000000, 29.21666666666666856, -0.3272492347489370235 ) ) ;
#13965=CONICAL_SURFACE ( 'NONE', #7774, 4.674999969225999585, 0.7853981633972997312 ) ;
#13973=ORIENTED_EDGE ( 'NONE', *, *, #12808, .F. ) ;
#13976=CARTESIAN_POINT ( 'NONE',  ( 4.000000000000000000, 24.80000000000000426, -2.309401076759000304 ) ) ;
#13980=DIRECTION ( 'NONE',  ( 0.000000000000000000, 1.000000000000000000, 0.000000000000000000 ) ) ;
#13984=B_SPLINE_CURVE_WITH_KNOTS ( 'NONE', 3,
 ( #13853, #8417, #647, #17372, #19060, #8049, #4414, #13728, #11806, #21256 ),
 .UNSPECIFIED., .F., .F.,
 ( 4, 2, 2, 2, 4 ),
 ( 0.000000000000000000, 0.0005867848385660769540, 0.001173569677132153908, 0.001760354515698231296, 0.002347139354264308683 ),
 .UNSPECIFIED. ) ;
#13986=CARTESIAN_POINT ( 'NONE',  ( -0.8545932710616224171, 26.39685207198635553, 4.125402498422513276 ) ) ;
#13989=CARTESIAN_POINT ( 'NONE',  ( -2.157756447954014334, 30.20979554246039456, 0.1029187449844319868 ) ) ;
#13993=DIRECTION ( 'NONE',  ( 1.000000000000000000, 0.000000000000000000, 0.000000000000000000 ) ) ;
#13997=EDGE_CURVE ( 'NONE', #8124, #1589, #6474, .T. ) ;
#13999=EDGE_LOOP ( 'NONE', ( #16995, #5946, #2003, #20693 ) ) ;
#14003=CARTESIAN_POINT ( 'NONE',  ( 2.141488944079684931, 27.19972511225902423, 0.5077517406370575248 ) ) ;
#14008=EDGE_CURVE ( 'NONE', #11502, #23288, #19646, .T. ) ;
#14009=CARTESIAN_POINT ( 'NONE',  ( -1.420784056250328886, 26.52499303979539391, 2.114791243013953270 ) ) ;
#14010=EDGE_CURVE ( 'NONE', #15589, #889, #15352, .T. ) ;
#14015=DIRECTION ( 'NONE',  ( 1.000000000000000000, 0.000000000000000000, 0.000000000000000000 ) ) ;
#14017=CARTESIAN_POINT ( 'NONE',  ( 2.184057253797768272, 28.22147922721521240, -0.2997864855702207509 ) ) ;
#14023=CARTESIAN_POINT ( 'NONE',  ( 2.070238309910999774, 25.71619850837999977, 0.4658180156273000194 ) ) ;
#14027=CARTESIAN_POINT ( 'NONE',  ( -1.279883260171999826, 28.48437716036000111, -2.088559871480999419 ) ) ;
#14028=DIRECTION ( 'NONE',  ( 1.000000000000000000, 0.000000000000000000, 0.000000000000000000 ) ) ;
#14036=CARTESIAN_POINT ( 'NONE',  ( 0.000000000000000000, 24.50000000000000000, 0.000000000000000000 ) ) ;
#14042=ORIENTED_EDGE ( 'NONE', *, *, #275, .F. ) ;
#14043=CARTESIAN_POINT ( 'NONE',  ( -2.500000000000000444, 28.78333333333333144, -0.3272492347489320275 ) ) ;
#14044=CARTESIAN_POINT ( 'NONE',  ( -0.4458865764599000414, 29.37709983102000066, -2.493253997570000102 ) ) ;
#14051=CARTESIAN_POINT ( 'NONE',  ( 0.000000000000000000, 24.49999999999999645, 0.000000000000000000 ) ) ;
#14054=FACE_OUTER_BOUND ( 'NONE', #9200, .T. ) ;
#14056=ORIENTED_EDGE ( 'NONE', *, *, #12669, .T. ) ;
#14057=CARTESIAN_POINT ( 'NONE',  ( 2.424643331163519964E-11, 24.52694564545263844, -2.373054354547839306 ) ) ;
#14060=CARTESIAN_POINT ( 'NONE',  ( -1.662092656101999966, 23.94309775297999821, -2.174644641551999769 ) ) ;
#14061=DIRECTION ( 'NONE',  ( -1.000000000000000000, 0.000000000000000000, 0.000000000000000000 ) ) ;
#14067=EDGE_LOOP ( 'NONE', ( #6129, #18059, #13571 ) ) ;
#14069=CARTESIAN_POINT ( 'NONE',  ( 0.000000000000000000, 18.89999999999999858, 0.000000000000000000 ) ) ;
#14082=CARTESIAN_POINT ( 'NONE',  ( -1.524685720705258207, 29.50411617716720514, 1.529777632466581050 ) ) ;
#14084=CARTESIAN_POINT ( 'NONE',  ( 1.999167105995449889, 29.28333333333333499, -1.536366799937288086 ) ) ;
#14086=ORIENTED_EDGE ( 'NONE', *, *, #1963, .F. ) ;
#14091=CARTESIAN_POINT ( 'NONE',  ( -1.938452583514000072, 27.67006359724000220, 1.528152797339000113 ) ) ;
#14093=ORIENTED_EDGE ( 'NONE', *, *, #1695, .T. ) ;
#14100=CONICAL_SURFACE ( 'NONE', #21044, 3.049999825846000157, 0.7853981633972997312 ) ;
#14105=ADVANCED_FACE ( 'NONE', ( #13908 ), #17292, .T. ) ;
#14106=DIRECTION ( 'NONE',  ( -1.000000000000000000, 0.000000000000000000, 0.000000000000000000 ) ) ;
#14108=CARTESIAN_POINT ( 'NONE',  ( 0.000000000000000000, -1.550000000000000044, 0.000000000000000000 ) ) ;
#14109=CARTESIAN_POINT ( 'NONE',  ( 2.267779804951839839, 26.36777980495183726, 5.387954023152814032E-08 ) ) ;
#14110=CARTESIAN_POINT ( 'NONE',  ( -1.597028793744863506, 30.29838184876847151, 1.461961021377746972 ) ) ;
#14112=CARTESIAN_POINT ( 'NONE',  ( -0.6558363950912000639, 25.57813856944000008, 2.241719613464999927 ) ) ;
#14115=CARTESIAN_POINT ( 'NONE',  ( 0.000000000000000000, 15.05000017415440006, -3.049999825846000157 ) ) ;
#14119=EDGE_CURVE ( 'NONE', #19360, #22068, #19240, .T. ) ;
#14121=ORIENTED_EDGE ( 'NONE', *, *, #19488, .F. ) ;
#14123=CARTESIAN_POINT ( 'NONE',  ( 2.500000000000000000, 18.50000000000000000, 0.000000000000000000 ) ) ;
#14126=CARTESIAN_POINT ( 'NONE',  ( 2.049260319077078840, 26.47238454635797922, -0.7136609902301204178 ) ) ;
#14128=ADVANCED_FACE ( 'NONE', ( #8589 ), #16128, .T. ) ;
#14139=DIRECTION ( 'NONE',  ( 0.000000000000000000, -1.000000000000000000, 0.000000000000000000 ) ) ;
#14145=CARTESIAN_POINT ( 'NONE',  ( -1.780325977227999790, 27.82869850838000048, 1.403495832404999977 ) ) ;
#14146=CIRCLE ( 'NONE', #6001, 3.100000000000000089 ) ;
#14152=EDGE_LOOP ( 'NONE', ( #16320, #10991, #8496, #10811 ) ) ;
#14158=CARTESIAN_POINT ( 'NONE',  ( 2.184465970885655306, 24.33333333333333570, 1.259047450927230027 ) ) ;
#14165=CARTESIAN_POINT ( 'NONE',  ( -0.3904964477860000116, 29.04133632509000051, 2.613711361504000408 ) ) ;
#14169=CARTESIAN_POINT ( 'NONE',  ( -1.236362846991004183, 26.50000008335574719, -2.171602059085420589 ) ) ;
#14170=FACE_OUTER_BOUND ( 'NONE', #22405, .T. ) ;
#14177=EDGE_LOOP ( 'NONE', ( #13923, #14925, #10242, #22292 ) ) ;
#14179=FACE_OUTER_BOUND ( 'NONE', #2592, .T. ) ;
#14181=CARTESIAN_POINT ( 'NONE',  ( 1.699999994525651204, 12.91209873359414217, 1.053565370275990620 ) ) ;
#14184=CARTESIAN_POINT ( 'NONE',  ( 2.247878665003999910, 25.86878373060999792, -0.3542756539240000668 ) ) ;
#14187=CARTESIAN_POINT ( 'NONE',  ( 4.750000000000000000, 16.89999999999999858, 0.000000000000000000 ) ) ;
#14189=CARTESIAN_POINT ( 'NONE',  ( 0.000000000000000000, 15.05000017415440006, 0.000000000000000000 ) ) ;
#14191=VERTEX_POINT ( 'NONE', #23819 ) ;
#14195=ORIENTED_EDGE ( 'NONE', *, *, #13699, .T. ) ;
#14197=CIRCLE ( 'NONE', #13397, 3.000000000000000000 ) ;
#14198=LINE ( 'NONE', #21595, #20743 ) ;
#14200=CARTESIAN_POINT ( 'NONE',  ( 4.000000000000000000, 24.80000000000000426, 2.309401076759000304 ) ) ;
#14204=EDGE_LOOP ( 'NONE', ( #12021, #6091, #13961, #17816, #2456, #12041 ) ) ;
#14206=CARTESIAN_POINT ( 'NONE',  ( -1.633105399745039321, 29.31302638303034058, -1.413471024401691256 ) ) ;
#14207=VERTEX_POINT ( 'NONE', #1788 ) ;
#14208=CARTESIAN_POINT ( 'NONE',  ( 2.184465970885645092, 29.26666666666667993, -1.259047450927249123 ) ) ;
#14216=DIRECTION ( 'NONE',  ( -1.000000000000000000, 0.000000000000000000, 0.000000000000000000 ) ) ;
#14217=ADVANCED_FACE ( 'NONE', ( #7229 ), #16555, .T. ) ;
#14218=CARTESIAN_POINT ( 'NONE',  ( -2.456483904114000083, 27.57256359724000205, -0.2419425476017999788 ) ) ;
#14221=DIRECTION ( 'NONE',  ( 0.000000000000000000, 1.000000000000000000, 0.000000000000000000 ) ) ;
#14224=ORIENTED_EDGE ( 'NONE', *, *, #21707, .T. ) ;
#14228=AXIS2_PLACEMENT_3D ( 'NONE', #14036, #11986, #6399 ) ;
#14231=CARTESIAN_POINT ( 'NONE',  ( 0.2323400247800999907, 29.20173034859999817, -2.331423980350999958 ) ) ;
#14233=CARTESIAN_POINT ( 'NONE',  ( -2.124536007966489670, 30.18061194770063338, -0.3918411660969223775 ) ) ;
#14235=CARTESIAN_POINT ( 'NONE',  ( 2.333600034839999893, 25.01975644544999966, -0.09865051850806999534 ) ) ;
#14240=DIRECTION ( 'NONE',  ( 0.000000000000000000, 1.000000000000000000, 0.000000000000000000 ) ) ;
#14248=ORIENTED_EDGE ( 'NONE', *, *, #23093, .F. ) ;
#14256=EDGE_CURVE ( 'NONE', #6193, #8075, #1454, .T. ) ;
#14257=CARTESIAN_POINT ( 'NONE',  ( -0.3463667137703017040, 24.70780860099542764, 4.418706525546099328 ) ) ;
#14259=CARTESIAN_POINT ( 'NONE',  ( 2.125092041327180326, 26.63141011545438985, -0.4551239170173230764 ) ) ;
#14263=ORIENTED_EDGE ( 'NONE', *, *, #15278, .F. ) ;
#14264=CARTESIAN_POINT ( 'NONE',  ( -0.3564538054804341494, 26.29977277844468020, -4.413003452969197049 ) ) ;
#14266=CARTESIAN_POINT ( 'NONE',  ( 1.107772814030999919, 25.87869850838000119, -1.978081431919000099 ) ) ;
#14269=CARTESIAN_POINT ( 'NONE',  ( 0.5249584007626000304, 28.38687716036000097, -2.392615059649000120 ) ) ;
#14270=AXIS2_PLACEMENT_3D ( 'NONE', #23457, #1308, #3251 ) ;
#14281=CARTESIAN_POINT ( 'NONE',  ( -2.434931691670770171, 24.03333333333333499, 0.6543697108982720057 ) ) ;
#14285=VECTOR ( 'NONE', #17159, 1000.000000000000114 ) ;
#14289=CARTESIAN_POINT ( 'NONE',  ( -1.879209721347999906, 30.33054072803999901, 1.397325483377999999 ) ) ;
#14290=CARTESIAN_POINT ( 'NONE',  ( 0.5271288625574210851, 26.26111511314614688, 2.095841999210956264 ) ) ;
#14295=FACE_OUTER_BOUND ( 'NONE', #8538, .T. ) ;
#14305=CARTESIAN_POINT ( 'NONE',  ( -4.000000000000000000, 26.50000000000000355, 0.000000000000000000 ) ) ;
#14306=EDGE_LOOP ( 'NONE', ( #7367, #21460, #2713 ) ) ;
#14307=AXIS2_PLACEMENT_3D ( 'NONE', #13326, #7887, #2079 ) ;
#14308=CARTESIAN_POINT ( 'NONE',  ( 0.4324689435440000063, 24.63980054822999932, -2.702762649533999806 ) ) ;
#14312=EDGE_CURVE ( 'NONE', #8412, #6193, #7585, .T. ) ;
#14318=CARTESIAN_POINT ( 'NONE',  ( -1.536366799937282313, 29.95086340285667603, 1.999167105995454552 ) ) ;
#14319=B_SPLINE_CURVE_WITH_KNOTS ( 'NONE', 3,
 ( #19650, #21590, #13821, #16110, #19403, #23261, #2935, #19887, #8511, #15987, #1479, #21461, #14318, #23379, #6797, #5004, #10197, #2817 ),
 .UNSPECIFIED., .F., .F.,
 ( 4, 2, 2, 2, 2, 2, 2, 2, 4 ),
 ( 0.000000000000000000, 0.1250000000000000000, 0.2500000000000000000, 0.3750000000000000000, 0.5000000000000000000, 0.6250000000000000000, 0.7500000000000000000, 0.8750000000000000000, 1.000000000000000000 ),
 .UNSPECIFIED. ) ;
#14321=CARTESIAN_POINT ( 'NONE',  ( 0.000000000000000000, 9.100092063578999912, -1.999999999999988676 ) ) ;
#14322=VERTEX_POINT ( 'NONE', #7464 ) ;
#14330=CARTESIAN_POINT ( 'NONE',  ( 1.375818737057000085, 30.26428676817999985, 1.918154343084000013 ) ) ;
#14339=DIRECTION ( 'NONE',  ( 0.000000000000000000, -1.000000000000000000, 0.000000000000000000 ) ) ;
#14342=ORIENTED_EDGE ( 'NONE', *, *, #10548, .F. ) ;
#14345=CARTESIAN_POINT ( 'NONE',  ( 2.000000000000198508, 24.49999999999999645, -3.464101615138341028 ) ) ;
#14352=CARTESIAN_POINT ( 'NONE',  ( -2.340764093348000063, 30.20884863804000275, -0.1017020371176000082 ) ) ;
#14353=AXIS2_PLACEMENT_3D ( 'NONE', #1800, #7361, #11123 ) ;
#14355=CARTESIAN_POINT ( 'NONE',  ( 0.8827757939797101772, 29.95033105760662906, -1.971174946009011553 ) ) ;
#14360=CARTESIAN_POINT ( 'NONE',  ( -0.9262738205379743572, 23.62802189508158790, -1.915861982203995284 ) ) ;
#14363=CARTESIAN_POINT ( 'NONE',  ( 2.500000000000000000, 18.50000000000000000, 0.000000000000000000 ) ) ;
#14368=CARTESIAN_POINT ( 'NONE',  ( 1.890284010598150877, 26.36143429054256870, 1.130219607317671127 ) ) ;
#14378=CARTESIAN_POINT ( 'NONE',  ( 1.767919490126756310, 26.52540550784508611, 1.264046928454615193 ) ) ;
#14381=CARTESIAN_POINT ( 'NONE',  ( 2.066176616758256035, 30.64207483863886594, -0.6409079810234022956 ) ) ;
#14383=FACE_OUTER_BOUND ( 'NONE', #10595, .T. ) ;
#14384=CARTESIAN_POINT ( 'NONE',  ( -2.104626470933999904, 26.17913313895000016, -1.289728978252000058 ) ) ;
#14387=CARTESIAN_POINT ( 'NONE',  ( -1.796659635434000091, 27.91771896306000045, 1.416372250270000022 ) ) ;
#14394=CARTESIAN_POINT ( 'NONE',  ( -2.153985071724999756, 30.83999999999999986, 0.1610847937796999751 ) ) ;
#14400=ORIENTED_EDGE ( 'NONE', *, *, #7702, .F. ) ;
#14401=DIRECTION ( 'NONE',  ( 0.000000000000000000, 0.7071067811866525998, -0.7071067811864425456 ) ) ;
#14416=CARTESIAN_POINT ( 'NONE',  ( 1.709378212513718687, 12.94272856688811046, 1.056191457993780114 ) ) ;
#14418=CARTESIAN_POINT ( 'NONE',  ( 2.301266907105999682, 25.82233687760000151, 0.4915126353211999866 ) ) ;
#14420=EDGE_CURVE ( 'NONE', #23795, #6008, #22709, .T. ) ;
#14424=DIRECTION ( 'NONE',  ( 0.000000000000000000, 0.7071067811866525998, -0.7071067811864425456 ) ) ;
#14426=CARTESIAN_POINT ( 'NONE',  ( 0.000000000000000000, 24.50000000000000000, 0.000000000000000000 ) ) ;
#14431=CARTESIAN_POINT ( 'NONE',  ( 0.7621399210758000864, 23.93675694115000141, 2.004617982535000120 ) ) ;
#14435=EDGE_CURVE ( 'NONE', #21280, #1169, #4954, .T. ) ;
#14436=CARTESIAN_POINT ( 'NONE',  ( 0.5645359770996000170, 30.65695694114999981, -2.093200898226000195 ) ) ;
#14442=VERTEX_POINT ( 'NONE', #19082 ) ;
#14443=FACE_OUTER_BOUND ( 'NONE', #15464, .T. ) ;
#14446=FACE_OUTER_BOUND ( 'NONE', #2231, .T. ) ;
#14448=EDGE_CURVE ( 'NONE', #21878, #22057, #22725, .T. ) ;
#14449=CARTESIAN_POINT ( 'NONE',  ( 2.750000000000000000, 24.29999999999999716, 0.000000000000000000 ) ) ;
#14455=LINE ( 'NONE', #20271, #10970 ) ;
#14459=CARTESIAN_POINT ( 'NONE',  ( -2.944270284434495899, 26.42936170367566362, 2.918926912232258530 ) ) ;
#14461=B_SPLINE_CURVE_WITH_KNOTS ( 'NONE', 3,
 ( #17018, #6234, #20654, #9996, #15433, #22698, #11816, #13615, #21013, #17385, #782, #11579, #11459, #17259, #14949, #18955, #9513, #4425 ),
 .UNSPECIFIED., .F., .F.,
 ( 4, 2, 2, 2, 2, 2, 2, 2, 4 ),
 ( 0.000000000000000000, 0.1250000000000000555, 0.2500000000000000555, 0.3750000000000000555, 0.5000000000000000000, 0.6249999999999998890, 0.7499999999999998890, 0.8749999999999998890, 1.000000000000000000 ),
 .UNSPECIFIED. ) ;
#14464=CARTESIAN_POINT ( 'NONE',  ( 1.463530596214999813, 29.93944235804000087, -1.626872480619000028 ) ) ;
#14465=UNCERTAINTY_MEASURE_WITH_UNIT (LENGTH_MEASURE( 1.000000000000000082E-05 ), #11147, 'distance_accuracy_value', 'NONE');
#14467=CARTESIAN_POINT ( 'NONE',  ( 1.411316182247830175, 29.91300950840242479, -1.635672673209419559 ) ) ;
#14484=CARTESIAN_POINT ( 'NONE',  ( -1.536366799937282090, 29.71666666666667211, 1.999167105995454552 ) ) ;
#14485=ORIENTED_EDGE ( 'NONE', *, *, #9923, .F. ) ;
#14487=AXIS2_PLACEMENT_3D ( 'NONE', #8423, #13734, #13858 ) ;
#14489=DIRECTION ( 'NONE',  ( 0.000000000000000000, -1.000000000000000000, 0.000000000000000000 ) ) ;
#14492=CARTESIAN_POINT ( 'NONE',  ( 0.6990180580869200799, 26.44590205212557521, 2.094941974207407132 ) ) ;
#14493=VECTOR ( 'NONE', #12516, 1000.000000000000000 ) ;
#14495=CARTESIAN_POINT ( 'NONE',  ( 1.509965525092430205, 30.70526206248454670, -1.547206845526075236 ) ) ;
#14498=CARTESIAN_POINT ( 'NONE',  ( 2.258737362907614621, 26.35873736869804773, 0.2437184634590501553 ) ) ;
#14499=CARTESIAN_POINT ( 'NONE',  ( 1.350549796471707253, 24.78453005107567009, 1.633252776670135908 ) ) ;
#14500=CARTESIAN_POINT ( 'NONE',  ( 1.416372250270000022, 26.74771896305999874, -1.796659635434000091 ) ) ;
#14507=ORIENTED_EDGE ( 'NONE', *, *, #12143, .F. ) ;
#14508=EDGE_CURVE ( 'NONE', #5518, #7680, #19087, .T. ) ;
#14509=CARTESIAN_POINT ( 'NONE',  ( 1.999167105995466764, 24.31666666666666643, 1.536366799937266325 ) ) ;
#14510=DIRECTION ( 'NONE',  ( 0.000000000000000000, -1.000000000000000000, 0.000000000000000000 ) ) ;
#14514=DIRECTION ( 'NONE',  ( 0.000000000000000000, -1.000000000000000000, 0.000000000000000000 ) ) ;
#14515=CARTESIAN_POINT ( 'NONE',  ( -1.169337612399999893, 30.82072358173000381, -1.691178548922000147 ) ) ;
#14519=VERTEX_POINT ( 'NONE', #15565 ) ;
#14520=CARTESIAN_POINT ( 'NONE',  ( 0.000000000000000000, 31.00000000000000000, -2.000000000000000000 ) ) ;
#14522=EDGE_CURVE ( 'NONE', #11598, #10311, #11711, .T. ) ;
#14529=CARTESIAN_POINT ( 'NONE',  ( 2.325656998026726541, 30.67434301629538851, 0.4535295980105740199 ) ) ;
#14530=CARTESIAN_POINT ( 'NONE',  ( -4.000000000000000000, 26.41693820796410108, 1.184172465503444904 ) ) ;
#14532=CARTESIAN_POINT ( 'NONE',  ( -0.8187353038599000099, 24.39316693604000008, -2.000180504622000033 ) ) ;
#14534=CARTESIAN_POINT ( 'NONE',  ( 2.000000000000000000, 23.00000000000000000, 0.000000000000000000 ) ) ;
#14536=CARTESIAN_POINT ( 'NONE',  ( -0.6543697108982037269, 27.83333333333333925, -2.434931691670788823 ) ) ;
#14540=DIRECTION ( 'NONE',  ( 0.000000000000000000, -1.000000000000000000, 0.000000000000000000 ) ) ;
#14541=CARTESIAN_POINT ( 'NONE',  ( -1.842949095694737638, 26.21789781124859786, 1.045490242349867982 ) ) ;
#14542=DIRECTION ( 'NONE',  ( 1.000000000000000000, 0.000000000000000000, 0.000000000000000000 ) ) ;
#14543=ORIENTED_EDGE ( 'NONE', *, *, #4962, .T. ) ;
#14545=CARTESIAN_POINT ( 'NONE',  ( 2.291512794585000012, 25.56043239939999978, 0.4488570629504000098 ) ) ;
#14549=CARTESIAN_POINT ( 'NONE',  ( -1.795908923730999751, 30.69514008176999909, -1.532003524410999962 ) ) ;
#14552=FACE_OUTER_BOUND ( 'NONE', #1467, .T. ) ;
#14554=LINE ( 'NONE', #21947, #15247 ) ;
#14555=EDGE_LOOP ( 'NONE', ( #14224, #17632, #1176, #13532 ) ) ;
#14557=CYLINDRICAL_SURFACE ( 'NONE', #4576, 3.000000000000000000 ) ;
#14560=VERTEX_POINT ( 'NONE', #8079 ) ;
#14565=EDGE_CURVE ( 'NONE', #22702, #13196, #21427, .T. ) ;
#14567=ORIENTED_EDGE ( 'NONE', *, *, #21326, .F. ) ;
#14576=DIRECTION ( 'NONE',  ( 1.127781618093000070E-10, -1.517612146120235195E-19, -1.000000000000000000 ) ) ;
#14577=CARTESIAN_POINT ( 'NONE',  ( 1.571106264104000116, 30.73074958545000257, -1.523240044125999892 ) ) ;
#14578=EDGE_CURVE ( 'NONE', #953, #8305, #20914, .T. ) ;
#14582=CARTESIAN_POINT ( 'NONE',  ( 0.8902908324380954808, 29.94984802629786813, -1.967793501657690403 ) ) ;
#14583=ORIENTED_EDGE ( 'NONE', *, *, #5938, .F. ) ;
#14584=CARTESIAN_POINT ( 'NONE',  ( -1.271343851483999865, 23.71194070365999806, -1.772672411470999965 ) ) ;
#14586=CARTESIAN_POINT ( 'NONE',  ( -0.8942398442040443429, 23.65531290036175704, -1.961072913851835242 ) ) ;
#14588=CARTESIAN_POINT ( 'NONE',  ( 0.000000000000000000, 7.049999902385000183, 0.000000000000000000 ) ) ;
#14592=EDGE_CURVE ( 'NONE', #14519, #20964, #10761, .T. ) ;
#14593=CARTESIAN_POINT ( 'NONE',  ( 0.000000000000000000, 15.09999999999999964, 0.000000000000000000 ) ) ;
#14596=VECTOR ( 'NONE', #825, 1000.000000000000000 ) ;
#14597=CARTESIAN_POINT ( 'NONE',  ( -2.499999999999999556, 28.25086340285665543, 0.3272492347489435738 ) ) ;
#14599=ORIENTED_EDGE ( 'NONE', *, *, #17364, .T. ) ;
#14600=AXIS2_PLACEMENT_3D ( 'NONE', #10997, #1791, #20209 ) ;
#14603=CARTESIAN_POINT ( 'NONE',  ( -2.500000000000000000, 29.60000000000000142, 0.000000000000000000 ) ) ;
#14607=CARTESIAN_POINT ( 'NONE',  ( -2.098987933218289914, 27.83721252561470649, 0.5526953750194446568 ) ) ;
#14608=DIRECTION ( 'NONE',  ( 0.000000000000000000, -1.000000000000000000, 0.000000000000000000 ) ) ;
#14609=CARTESIAN_POINT ( 'NONE',  ( 0.1386669981692911224, 30.79610789710345742, -2.185737362969716546 ) ) ;
#14611=CARTESIAN_POINT ( 'NONE',  ( 0.000000000000000000, 26.20000000000000284, -4.618802153517000519 ) ) ;
#14615=CARTESIAN_POINT ( 'NONE',  ( 4.000000000000000000, 24.80000000000000426, -2.309401076759000304 ) ) ;
#14616=CARTESIAN_POINT ( 'NONE',  ( -2.088559871480999419, 26.14437716036000126, -1.279883260171999826 ) ) ;
#14618=EDGE_LOOP ( 'NONE', ( #5829, #18431, #3822 ) ) ;
#14621=CARTESIAN_POINT ( 'NONE',  ( 0.000000000000000000, -1.550000000000000044, 0.000000000000000000 ) ) ;
#14623=ORIENTED_EDGE ( 'NONE', *, *, #6288, .F. ) ;
#14624=CARTESIAN_POINT ( 'NONE',  ( -2.729128784747790970, 19.00000000000000000, 0.000000000000000000 ) ) ;
#14626=CIRCLE ( 'NONE', #686, 3.000000000000000000 ) ;
#14630=CARTESIAN_POINT ( 'NONE',  ( -0.6465006763629999043, 28.70297252654999909, 1.951786927810000183 ) ) ;
#14634=DIRECTION ( 'NONE',  ( 0.000000000000000000, 0.000000000000000000, 1.000000000000000000 ) ) ;
#14637=LINE ( 'NONE', #19985, #19732 ) ;
#14639=AXIS2_PLACEMENT_3D ( 'NONE', #10268, #16061, #21296 ) ;
#14640=CARTESIAN_POINT ( 'NONE',  ( 0.000000000000000000, -1.550000000000000044, 0.000000000000000000 ) ) ;
#14643=CARTESIAN_POINT ( 'NONE',  ( 0.1891046077859345476, 29.19254760244434976, -2.151987026392503832 ) ) ;
#14648=CONICAL_SURFACE ( 'NONE', #6913, 4.699999872533999756, 0.7853981633972997312 ) ;
#14650=CARTESIAN_POINT ( 'NONE',  ( 2.235419194099999896, 24.28959072804000030, -0.7352241695104999586 ) ) ;
#14654=CARTESIAN_POINT ( 'NONE',  ( -4.624999963076000142, 12.99999996307999872, -4.214403009264000636E-08 ) ) ;
#14656=AXIS2_PLACEMENT_3D ( 'NONE', #5220, #20226, #5449 ) ;
#14657=ORIENTED_EDGE ( 'NONE', *, *, #7332, .F. ) ;
#14664=CARTESIAN_POINT ( 'NONE',  ( -0.2985486204943000321, 23.87271582673999859, 2.123722402587000069 ) ) ;
#14666=AXIS2_PLACEMENT_3D ( 'NONE', #18845, #22593, #18614 ) ;
#14673=EDGE_CURVE ( 'NONE', #16342, #9790, #4560, .T. ) ;
#14680=DIRECTION ( 'NONE',  ( 0.000000000000000000, 1.000000000000000000, 0.000000000000000000 ) ) ;
#14685=CARTESIAN_POINT ( 'NONE',  ( -2.464088664829000130, 26.79256359724000092, 0.1453149127352000025 ) ) ;
#14686=EDGE_CURVE ( 'NONE', #12867, #21635, #17727, .T. ) ;
#14696=CARTESIAN_POINT ( 'NONE',  ( -1.826717418791999892, 30.92821884477999816, -1.467226286860000117 ) ) ;
#14700=CARTESIAN_POINT ( 'NONE',  ( 1.985433307355395360, 29.85536931078693001, -0.8508083005501347884 ) ) ;
#14702=CARTESIAN_POINT ( 'NONE',  ( 0.4793969798898999879, 24.06092953115000199, 2.128160979441000134 ) ) ;
#14706=DIRECTION ( 'NONE',  ( 0.000000000000000000, 0.000000000000000000, -1.000000000000000000 ) ) ;
#14713=DIRECTION ( 'NONE',  ( 0.000000000000000000, 0.000000000000000000, -1.000000000000000000 ) ) ;
#14715=CARTESIAN_POINT ( 'NONE',  ( 2.500000000000000000, 24.41665956134495730, -0.3271097220832465124 ) ) ;
#14720=CARTESIAN_POINT ( 'NONE',  ( 2.151176768373039838, 27.38669294409674393, 0.3026932924341791398 ) ) ;
#14721=CARTESIAN_POINT ( 'NONE',  ( 1.399999855176999874, 6.999999855177000185, -5.700011344538000517E-07 ) ) ;
#14722=CARTESIAN_POINT ( 'NONE',  ( -0.8328668639932000906, 29.02250240009999871, 2.747163055864000114 ) ) ;
#14723=EDGE_CURVE ( 'NONE', #9190, #1429, #21872, .T. ) ;
#14724=CARTESIAN_POINT ( 'NONE',  ( 1.949611214030006812, 30.66062952581684087, -0.9304744684606878202 ) ) ;
#14725=ORIENTED_EDGE ( 'NONE', *, *, #16379, .F. ) ;
#14726=EDGE_CURVE ( 'NONE', #11568, #10983, #3028, .T. ) ;
#14730=CARTESIAN_POINT ( 'NONE',  ( -2.218121370661999769, 28.35614211381999894, -0.5788358281067000899 ) ) ;
#14731=LINE ( 'NONE', #22799, #20075 ) ;
#14733=EDGE_LOOP ( 'NONE', ( #12712, #17826, #13064, #5225 ) ) ;
#14744=DIRECTION ( 'NONE',  ( -1.000000000000000000, 0.000000000000000000, 0.000000000000000000 ) ) ;
#14745=CARTESIAN_POINT ( 'NONE',  ( 1.263454500199000075, 30.42364525888999793, 1.740526072561999982 ) ) ;
#14748=VERTEX_POINT ( 'NONE', #12554 ) ;
#14751=FACE_OUTER_BOUND ( 'NONE', #7441, .T. ) ;
#14756=CARTESIAN_POINT ( 'NONE',  ( 0.3018188377541565215, 29.18586512010584855, -2.138794871149622967 ) ) ;
#14758=VERTEX_POINT ( 'NONE', #1535 ) ;
#14760=CARTESIAN_POINT ( 'NONE',  ( -0.8914544781580999722, 24.49860156660999877, -2.177834349592000063 ) ) ;
#14771=DIRECTION ( 'NONE',  ( -0.000000000000000000, 1.000000000000000000, 0.000000000000000000 ) ) ;
#14772=EDGE_LOOP ( 'NONE', ( #23651, #10739, #3795, #14342 ) ) ;
#14774=CARTESIAN_POINT ( 'NONE',  ( 2.331686743179000043, 24.79193902659000059, -0.1260324335329000012 ) ) ;
#14778=CARTESIAN_POINT ( 'NONE',  ( -1.046351349501999817, 29.04353571299000336, -2.115973140337000125 ) ) ;
#14785=CARTESIAN_POINT ( 'NONE',  ( 2.899999999999999911, 19.00000000000000000, 0.000000000000000000 ) ) ;
#14786=VERTEX_POINT ( 'NONE', #23794 ) ;
#14787=B_SPLINE_SURFACE_WITH_KNOTS ( 'NONE', 3, 3, ( 
 ( #17797, #8584, #3144, #938, #12100, #14027, #14269, #12218, #19486, #21667, #5079, #19844, #10275, #2893, #15587, #17665, #18031, #19608, #8220, #19962, #7458, #6998, #20431, #16426, #23595, #3605, #23939, #3717, #11107, #14616, #9055, #10988, #3381, #5534, #11236 ),
 ( #18156, #20197, #18265, #22012, #14840, #22125, #12914, #13032, #1559, #5425, #20312, #14387, #18492, #10764, #22232, #16547, #18372, #8944, #1665, #23815, #7223, #1904, #9293, #14500, #16667, #73, #3840, #1434, #12807, #5647, #5304, #21780, #1783, #16312, #8832 ),
 ( #9171, #5193, #7346, #23703, #14730, #16193, #7110, #12574, #21893, #12695, #20084, #3497, #10877, #16777, #22828, #20909, #22708, #13157, #16900, #9408, #9760, #2371, #5772, #4314, #6118, #22354, #543, #3960, #18724, #15442, #20549, #6242, #2134, #5885, #13271 ),
 ( #21021, #17028, #9880, #13385, #20785, #4192, #11353, #186, #426, #11588, #7826, #7578, #18964, #17147, #17269, #20665, #305, #2019, #9523, #13510, #4075, #13625, #7711, #667, #14957, #4434, #9645, #15079, #7948, #15317, #11704, #19078, #15197, #2250, #2491 ) ),
 .UNSPECIFIED., .F., .F., .F.,
 ( 4, 4 ),
 ( 4, 1, 1, 1, 1, 1, 1, 1, 1, 1, 1, 1, 1, 1, 1, 1, 1, 1, 1, 1, 1, 1, 1, 1, 1, 1, 1, 1, 1, 1, 1, 1, 4 ),
 ( -0.2678694646895999898, 1.311704223562000005 ),
 ( -0.02000000000000000042, 0.01250000000000000069, 0.04499999999999999833, 0.07749999999999999944, 0.1100000000000000006, 0.1424999999999999878, 0.1749999999999999889, 0.2074999999999999900, 0.2399999999999999911, 0.2725000000000000200, 0.3049999999999999933, 0.3375000000000000222, 0.3699999999999999956, 0.4025000000000000244, 0.4349999999999999978, 0.4675000000000000266, 0.5000000000000000000, 0.5324999999999999734, 0.5649999999999999467, 0.5975000000000000311, 0.6300000000000000044, 0.6624999999999999778, 0.6949999999999999512, 0.7275000000000000355, 0.7600000000000000089, 0.7924999999999999822, 0.8249999999999999556, 0.8575000000000000400, 0.8900000000000000133, 0.9224999999999999867, 0.9549999999999999600, 0.9875000000000000444, 1.020000000000000018 ),
 .UNSPECIFIED. ) ;
#14788=DIRECTION ( 'NONE',  ( 0.000000000000000000, -1.000000000000000000, 0.000000000000000000 ) ) ;
#14792=CARTESIAN_POINT ( 'NONE',  ( 1.528152797339000113, 26.50006359724000049, -1.938452583514000072 ) ) ;
#14795=DIRECTION ( 'NONE',  ( -0.8660254037844288266, 0.000000000000000000, 0.5000000000000169864 ) ) ;
#14801=AXIS2_PLACEMENT_3D ( 'NONE', #7627, #3762, #349 ) ;
#14805=CARTESIAN_POINT ( 'NONE',  ( -0.7087001424027000729, 30.63054677757000022, -2.075015324932000027 ) ) ;
#14807=EDGE_CURVE ( 'NONE', #14786, #8812, #16147, .T. ) ;
#14808=CARTESIAN_POINT ( 'NONE',  ( 1.293847722389922739, 29.92197960974256432, -1.729741070547694104 ) ) ;
#14810=CARTESIAN_POINT ( 'NONE',  ( -1.971011845997999945, 24.68910942064999858, 0.9348812773489000305 ) ) ;
#14812=CARTESIAN_POINT ( 'NONE',  ( -1.070116364160798250, 23.62009658023850633, -1.830887543399779993 ) ) ;
#14819=CYLINDRICAL_SURFACE ( 'NONE', #5210, 4.750000000000000000 ) ;
#14820=CARTESIAN_POINT ( 'NONE',  ( 0.6543697108982093891, 29.83333333333333570, 2.434931691670787046 ) ) ;
#14821=EDGE_CURVE ( 'NONE', #14758, #9876, #2228, .T. ) ;
#14822=ORIENTED_EDGE ( 'NONE', *, *, #2148, .T. ) ;
#14830=DIRECTION ( 'NONE',  ( 0.000000000000000000, 0.000000000000000000, 1.000000000000000000 ) ) ;
#14832=AXIS2_PLACEMENT_3D ( 'NONE', #11416, #16975, #376 ) ;
#14833=EDGE_CURVE ( 'NONE', #1589, #16783, #1474, .T. ) ;
#14835=VERTEX_POINT ( 'NONE', #11273 ) ;
#14840=CARTESIAN_POINT ( 'NONE',  ( -2.213655236985999863, 28.60021896306000144, -0.5776703561810999643 ) ) ;
#14841=AXIS2_PLACEMENT_3D ( 'NONE', #5314, #12468, #3269 ) ;
#14842=CARTESIAN_POINT ( 'NONE',  ( -2.124682394174019162, 30.86598673310974661, 0.1994363584945500478 ) ) ;
#14849=CARTESIAN_POINT ( 'NONE',  ( 2.172683023327428575, 29.59140263288345807, 0.6846090325570640678 ) ) ;
#14853=CARTESIAN_POINT ( 'NONE',  ( -1.767805011140364924, 26.50018596745192312, 1.767686163102024643 ) ) ;
#14856=CARTESIAN_POINT ( 'NONE',  ( 0.000000000000000000, 22.00000000000000000, 0.000000000000000000 ) ) ;
#14857=CARTESIAN_POINT ( 'NONE',  ( 1.461167822581999953, 29.73492324375999729, 1.830009909314999961 ) ) ;
#14861=DIRECTION ( 'NONE',  ( -1.000000000000000000, 0.000000000000000000, 0.000000000000000000 ) ) ;
#14871=CARTESIAN_POINT ( 'NONE',  ( -0.7579255142056604555, 29.24940332731515014, -2.022519581349923712 ) ) ;
#14873=ORIENTED_EDGE ( 'NONE', *, *, #22155, .F. ) ;
#14874=B_SPLINE_CURVE_WITH_KNOTS ( 'NONE', 3,
 ( #12599, #3405, #3739, #23727, #11254, #10788, #11010, #9430, #7366, #1583 ),
 .UNSPECIFIED., .F., .F.,
 ( 4, 2, 2, 2, 4 ),
 ( 0.000000000000000000, 0.2500000000000000555, 0.5000000000000001110, 0.7500000000000002220, 1.000000000000000000 ),
 .UNSPECIFIED. ) ;
#14875=DIRECTION ( 'NONE',  ( -0.7071067811867974839, 0.7071067811862974395, 5.435105086405977277E-09 ) ) ;
#14876=CIRCLE ( 'NONE', #177, 1.500000000000000000 ) ;
#14878=CARTESIAN_POINT ( 'NONE',  ( -1.428961511897999914, 23.73222849182999639, -1.869621096888999912 ) ) ;
#14880=CARTESIAN_POINT ( 'NONE',  ( 1.884954223019000175, 28.16549822781000145, -1.259486242684000112 ) ) ;
#14883=CARTESIAN_POINT ( 'NONE',  ( 0.000000000000000000, 20.10000000000000142, 0.000000000000000000 ) ) ;
#14890=CARTESIAN_POINT ( 'NONE',  ( -1.962499827145000042, 25.11214459858999959, -1.265401773453000089 ) ) ;
#14894=CARTESIAN_POINT ( 'NONE',  ( 2.468126052364000067, 29.51257216720999921, -0.6532334635400000034 ) ) ;
#14898=CARTESIAN_POINT ( 'NONE',  ( -2.184465970885641983, 26.70086340285666893, 1.259047450927253564 ) ) ;
#14899=DIRECTION ( 'NONE',  ( 0.000000000000000000, -1.000000000000000000, 0.000000000000000000 ) ) ;
#14901=ORIENTED_EDGE ( 'NONE', *, *, #4236, .T. ) ;
#14902=CARTESIAN_POINT ( 'NONE',  ( -1.486213254096201197, 24.35414964709700669, 2.050825213284277915 ) ) ;
#14903=CARTESIAN_POINT ( 'NONE',  ( 0.000000000000000000, 19.09999999999999787, 0.000000000000000000 ) ) ;
#14909=CARTESIAN_POINT ( 'NONE',  ( -0.2419425476019000099, 26.59756359724000063, -2.456483904114000083 ) ) ;
#14910=EDGE_LOOP ( 'NONE', ( #13358, #18587, #7001, #5133, #5324, #19678, #2925 ) ) ;
#14922=CARTESIAN_POINT ( 'NONE',  ( 2.138161440418999693, 28.76018424004000096, 0.4860145525067000039 ) ) ;
#14924=CARTESIAN_POINT ( 'NONE',  ( 1.030379110807799314, 29.66722595074598701, 1.898321818861515187 ) ) ;
#14925=ORIENTED_EDGE ( 'NONE', *, *, #2737, .T. ) ;
#14926=CARTESIAN_POINT ( 'NONE',  ( 0.4160319935711000450, 24.39157655595000307, -2.298333837344000319 ) ) ;
#14930=EDGE_CURVE ( 'NONE', #22357, #903, #13050, .T. ) ;
#14935=ORIENTED_EDGE ( 'NONE', *, *, #15284, .T. ) ;
#14937=CARTESIAN_POINT ( 'NONE',  ( 2.434931691670791931, 29.96666666666666856, 0.6543697108981911814 ) ) ;
#14939=CIRCLE ( 'NONE', #17666, 2.399999999999999911 ) ;
#14942=VECTOR ( 'NONE', #22364, 1000.000000000000000 ) ;
#14945=CARTESIAN_POINT ( 'NONE',  ( 2.063594504837999888E-14, 28.80370090847999975, 2.160000000000000142 ) ) ;
#14947=CARTESIAN_POINT ( 'NONE',  ( -3.145406728938546781, 26.39685207198636618, -2.802800731853388516 ) ) ;
#14949=CARTESIAN_POINT ( 'NONE',  ( 2.184465970885644648, 28.70086340285666537, -1.259047450927249345 ) ) ;
#14950=CARTESIAN_POINT ( 'NONE',  ( -1.536366799937290084, 28.11753006952332967, -1.999167105995447669 ) ) ;
#14951=CARTESIAN_POINT ( 'NONE',  ( -0.6790912232653096847, 30.36316110238290022, 2.050354341998521512 ) ) ;
#14955=ADVANCED_FACE ( 'NONE', ( #10167, #2781 ), #12226, .F. ) ;
#14957=CARTESIAN_POINT ( 'NONE',  ( 2.440142399906000126, 26.43946440326000058, -0.3375125786566000041 ) ) ;
#14958=CARTESIAN_POINT ( 'NONE',  ( -2.127018241980240365, 30.86165161360391807, 0.2199161313900584724 ) ) ;
#14961=VERTEX_POINT ( 'NONE', #15596 ) ;
#14964=AXIS2_PLACEMENT_3D ( 'NONE', #3506, #22022, #15086 ) ;
#14967=CIRCLE ( 'NONE', #18100, 2.000000000000000000 ) ;
#14971=CARTESIAN_POINT ( 'NONE',  ( 0.000000000000000000, 13.00000000000000000, -4.625000000000000000 ) ) ;
#14972=DIRECTION ( 'NONE',  ( 1.000000000000000000, 0.000000000000000000, 0.000000000000000000 ) ) ;
#14976=ORIENTED_EDGE ( 'NONE', *, *, #1934, .F. ) ;
#14982=ORIENTED_EDGE ( 'NONE', *, *, #8976, .F. ) ;
#14986=CARTESIAN_POINT ( 'NONE',  ( -1.632592650705358972, 29.31298059332072370, -1.414061715089352633 ) ) ;
#14987=EDGE_CURVE ( 'NONE', #5602, #13406, #12108, .T. ) ;
#14989=ORIENTED_EDGE ( 'NONE', *, *, #20883, .T. ) ;
#14991=ORIENTED_EDGE ( 'NONE', *, *, #15166, .T. ) ;
#14992=CARTESIAN_POINT ( 'NONE',  ( 2.158151686652000301, 24.95052917223999955, -0.1158915279824000027 ) ) ;
#14994=CARTESIAN_POINT ( 'NONE',  ( 0.1334610483750000021, 27.48299822781000046, -2.263084017374999757 ) ) ;
#14995=DIRECTION ( 'NONE',  ( 6.465317307631811410E-08, 0.9999999999999703570, 2.351119573244930785E-07 ) ) ;
#15001=EDGE_CURVE ( 'NONE', #16783, #8812, #15711, .T. ) ;
#15006=AXIS2_PLACEMENT_3D ( 'NONE', #18635, #17290, #7849 ) ;
#15009=CARTESIAN_POINT ( 'NONE',  ( -2.292223709382000152, 25.13479219682000121, 1.060295004442999955 ) ) ;
#15012=DIRECTION ( 'NONE',  ( -1.000000000000000000, 0.000000000000000000, 0.000000000000000000 ) ) ;
#15013=CARTESIAN_POINT ( 'NONE',  ( 0.3501359026391999696, 29.29714551040999737, 2.528984977829000336 ) ) ;
#15016=AXIS2_PLACEMENT_3D ( 'NONE', #7288, #10705, #19910 ) ;
#15017=ADVANCED_FACE ( 'NONE', ( #6526 ), #8829, .T. ) ;
#15019=VERTEX_POINT ( 'NONE', #11586 ) ;
#15021=CARTESIAN_POINT ( 'NONE',  ( 1.602306253747700415, 23.96496164759273739, -1.892277031798197395 ) ) ;
#15023=CIRCLE ( 'NONE', #22398, 2.899999999999999911 ) ;
#15024=LINE ( 'NONE', #1729, #12643 ) ;
#15026=CARTESIAN_POINT ( 'NONE',  ( 2.500000000000000000, 28.40000000000000213, 0.000000000000000000 ) ) ;
#15027=AXIS2_PLACEMENT_3D ( 'NONE', #15574, #3005, #15933 ) ;
#15030=CARTESIAN_POINT ( 'NONE',  ( -2.778011591584000239, 28.14169433609999871, -0.7249434865795999494 ) ) ;
#15041=DIRECTION ( 'NONE',  ( 0.7071067811867999264, 0.7071067811862000729, -3.665336548266999286E-07 ) ) ;
#15044=CIRCLE ( 'NONE', #325, 2.270871215252209030 ) ;
#15045=CARTESIAN_POINT ( 'NONE',  ( 2.061941880494999602, 29.07619810994999909, -0.7328290969762999429 ) ) ;
#15046=CONICAL_SURFACE ( 'NONE', #18537, 3.049999825846000157, 0.7853981633972997312 ) ;
#15049=CARTESIAN_POINT ( 'NONE',  ( 1.426790630978265417, 29.69555823242072989, 1.621662507842850154 ) ) ;
#15051=CARTESIAN_POINT ( 'NONE',  ( 1.957984142568000241, 25.87567143413000181, -0.6867741620196999852 ) ) ;
#15058=CIRCLE ( 'NONE', #11987, 1.899912543625999373 ) ;
#15071=CARTESIAN_POINT ( 'NONE',  ( -2.649085689637681096, 26.47444252552742228, -3.089351817498231068 ) ) ;
#15072=CARTESIAN_POINT ( 'NONE',  ( -1.999167105995453442, 28.15086340285666466, -1.536366799937283645 ) ) ;
#15073=CARTESIAN_POINT ( 'NONE',  ( 1.735737918923996981, 30.52199503463014452, 1.297044354150451273 ) ) ;
#15074=ORIENTED_EDGE ( 'NONE', *, *, #20816, .F. ) ;
#15079=CARTESIAN_POINT ( 'NONE',  ( -1.368576729846999962, 26.14696440326000015, 2.048219662131999907 ) ) ;
#15083=DIRECTION ( 'NONE',  ( 0.000000000000000000, 0.000000000000000000, -1.000000000000000000 ) ) ;
#15084=CARTESIAN_POINT ( 'NONE',  ( 0.000000000000000000, 21.94999982584599962, -3.049999825846000157 ) ) ;
#15086=DIRECTION ( 'NONE',  ( 0.8947368421052591669, 0.000000000000000000, 0.4465937565388801156 ) ) ;
#15093=B_SPLINE_CURVE_WITH_KNOTS ( 'NONE', 3,
 ( #17578, #2806, #15739, #8251, #19265, #2680 ),
 .UNSPECIFIED., .F., .F.,
 ( 4, 2, 4 ),
 ( 3.686902641442823701E-05, 0.0005902785358939091793, 0.001143688045373390067 ),
 .UNSPECIFIED. ) ;
#15094=CARTESIAN_POINT ( 'NONE',  ( -0.3272492347489120990, 28.98333333333332718, 2.500000000000003109 ) ) ;
#15097=VERTEX_POINT ( 'NONE', #9879 ) ;
#15100=CIRCLE ( 'NONE', #14353, 4.724999999999999645 ) ;
#15109=CARTESIAN_POINT ( 'NONE',  ( -1.999167105995447224, 28.08333333333333570, 1.536366799937292305 ) ) ;
#15110=CARTESIAN_POINT ( 'NONE',  ( 1.664720809480999986, 27.38549822781000032, -1.538852087555999892 ) ) ;
#15113=CARTESIAN_POINT ( 'NONE',  ( 0.000000000000000000, 20.00000000000000000, -2.704938617610999654E-14 ) ) ;
#15119=CARTESIAN_POINT ( 'NONE',  ( -2.000000000000000000, 23.00000000000000000, 0.000000000000000000 ) ) ;
#15122=CARTESIAN_POINT ( 'NONE',  ( -2.282676281439000032, 24.90127533745000221, -1.471848595755000044 ) ) ;
#15124=LINE ( 'NONE', #11282, #17208 ) ;
#15125=CARTESIAN_POINT ( 'NONE',  ( 0.5493650718401000832, 28.50724776881999745, 2.493235163772000273 ) ) ;
#15130=CARTESIAN_POINT ( 'NONE',  ( 0.000000000000000000, 22.19999999999999574, -4.749999999999798383 ) ) ;
#15138=CARTESIAN_POINT ( 'NONE',  ( 0.000000000000000000, 21.95000012746600149, 0.000000000000000000 ) ) ;
#15141=DIRECTION ( 'NONE',  ( 0.000000000000000000, -1.000000000000000000, 0.000000000000000000 ) ) ;
#15142=ADVANCED_FACE ( 'NONE', ( #10003 ), #3382, .F. ) ;
#15143=CARTESIAN_POINT ( 'NONE',  ( -1.483218624018999954, 26.00462896666999768, 2.219793368323999871 ) ) ;
#15144=ORIENTED_EDGE ( 'NONE', *, *, #6527, .F. ) ;
#15152=EDGE_LOOP ( 'NONE', ( #23893, #20604, #3573, #23878 ) ) ;
#15159=CARTESIAN_POINT ( 'NONE',  ( 0.4716927464761000444, 28.86038704793000065, 2.136794783675000087 ) ) ;
#15160=CIRCLE ( 'NONE', #18283, 0.09999999999999982514 ) ;
#15162=CARTESIAN_POINT ( 'NONE',  ( 0.3745806831042071683, 29.62585680761208806, 2.127681447449794039 ) ) ;
#15165=CARTESIAN_POINT ( 'NONE',  ( -2.173781772047999716, 24.37523480591000080, -0.2297506569266999921 ) ) ;
#15166=EDGE_CURVE ( 'NONE', #10102, #14442, #21268, .T. ) ;
#15170=DIRECTION ( 'NONE',  ( 0.000000000000000000, 1.000000000000000000, 0.000000000000000000 ) ) ;
#15171=DIRECTION ( 'NONE',  ( 0.000000000000000000, -1.000000000000000000, -2.441144892843000242E-14 ) ) ;
#15172=DIRECTION ( 'NONE',  ( 0.000000000000000000, -1.000000000000000000, 0.000000000000000000 ) ) ;
#15183=CARTESIAN_POINT ( 'NONE',  ( 3.999999999999999112, 26.49040384242090695, 0.4670641126941216248 ) ) ;
#15185=DIRECTION ( 'NONE',  ( 0.000000000000000000, 1.000000000000000000, 0.000000000000000000 ) ) ;
#15187=CARTESIAN_POINT ( 'NONE',  ( -3.268181200173221335, 26.37490599056235752, -2.731916857836431678 ) ) ;
#15189=CARTESIAN_POINT ( 'NONE',  ( -2.434931691670790155, 28.20086340285666893, -0.6543697108981963995 ) ) ;
#15190=CARTESIAN_POINT ( 'NONE',  ( 0.9202813454773431934, 30.45996977815284978, 1.954029222696366030 ) ) ;
#15191=ORIENTED_EDGE ( 'NONE', *, *, #20206, .T. ) ;
#15197=CARTESIAN_POINT ( 'NONE',  ( 2.357055497444999759, 25.65946440325999944, -0.7145966149424999303 ) ) ;
#15203=CARTESIAN_POINT ( 'NONE',  ( -2.147341988817836445, 28.45716134483373594, 0.4763078141162557788 ) ) ;
#15205=ORIENTED_EDGE ( 'NONE', *, *, #9772, .F. ) ;
#15216=FACE_OUTER_BOUND ( 'NONE', #5737, .T. ) ;
#15217=CARTESIAN_POINT ( 'NONE',  ( -2.276308483783000103, 26.28456776952000240, -1.394936847711000016 ) ) ;
#15222=CARTESIAN_POINT ( 'NONE',  ( -1.488573664845307620, 23.70893436307923707, 1.654057013544842025 ) ) ;
#15229=DIRECTION ( 'NONE',  ( 1.000000000000000000, 0.000000000000000000, 0.000000000000000000 ) ) ;
#15231=VECTOR ( 'NONE', #797, 1000.000000000000227 ) ;
#15238=CARTESIAN_POINT ( 'NONE',  ( -2.122588054292000148, 25.00670996802000090, -1.368625184603999845 ) ) ;
#15243=CARTESIAN_POINT ( 'NONE',  ( -2.717871120395999984, 30.55607970622999758, -0.3891938976568000697 ) ) ;
#15247=VECTOR ( 'NONE', #12748, 1000.000000000000000 ) ;
#15248=CARTESIAN_POINT ( 'NONE',  ( -4.649999849441000421, 14.99999984944626696, 6.648422602291999773E-08 ) ) ;
#15250=VERTEX_POINT ( 'NONE', #23193 ) ;
#15255=CYLINDRICAL_SURFACE ( 'NONE', #4622, 4.750000000000000000 ) ;
#15256=CARTESIAN_POINT ( 'NONE',  ( -0.7385364242858543093, 24.44737158853346770, -2.065887602175232818 ) ) ;
#15262=CARTESIAN_POINT ( 'NONE',  ( 0.000000000000000000, 26.35000000000000142, 0.000000000000000000 ) ) ;
#15268=DIRECTION ( 'NONE',  ( -0.7071067811881966980, 0.7071067811848966711, -4.825991045650978446E-08 ) ) ;
#15269=ORIENTED_EDGE ( 'NONE', *, *, #6886, .F. ) ;
#15270=ADVANCED_FACE ( 'NONE', ( #15673 ), #6845, .T. ) ;
#15276=CARTESIAN_POINT ( 'NONE',  ( -0.8486101488374000468, 29.83923955014999763, -2.021840421918000175 ) ) ;
#15278=EDGE_CURVE ( 'NONE', #12276, #16405, #14939, .T. ) ;
#15279=CARTESIAN_POINT ( 'NONE',  ( 0.9172437346412692927, 29.65973296616930810, 1.957376652516603421 ) ) ;
#15281=CARTESIAN_POINT ( 'NONE',  ( 1.912038027982999822, 24.72422363341000207, 1.059350336922000091 ) ) ;
#15283=ORIENTED_EDGE ( 'NONE', *, *, #8833, .T. ) ;
#15284=EDGE_CURVE ( 'NONE', #9790, #17141, #19576, .T. ) ;
#15288=AXIS2_PLACEMENT_3D ( 'NONE', #10203, #10330, #16249 ) ;
#15290=ORIENTED_EDGE ( 'NONE', *, *, #15630, .F. ) ;
#15299=CARTESIAN_POINT ( 'NONE',  ( 4.000000000000000000, 26.50000000000000355, 0.000000000000000000 ) ) ;
#15304=DIRECTION ( 'NONE',  ( 1.000000000000000000, 0.000000000000000000, 0.000000000000000000 ) ) ;
#15305=CARTESIAN_POINT ( 'NONE',  ( 0.4393762720424915225, 26.31534065533142552, -4.365128144578328317 ) ) ;
#15307=CARTESIAN_POINT ( 'NONE',  ( 0.04514251421120654695, 30.40639362649127975, 2.160055992278567150 ) ) ;
#15308=ORIENTED_EDGE ( 'NONE', *, *, #4252, .T. ) ;
#15311=CIRCLE ( 'NONE', #8371, 2.750000000000000000 ) ;
#15315=EDGE_CURVE ( 'NONE', #5021, #14322, #8263, .T. ) ;
#15316=CARTESIAN_POINT ( 'NONE',  ( 1.716841021922666632, 23.94065246303359729, 1.459342451765975879 ) ) ;
#15317=CARTESIAN_POINT ( 'NONE',  ( -2.100366574696000299, 25.95196440325999987, -1.287118485749000119 ) ) ;
#15324=CARTESIAN_POINT ( 'NONE',  ( -0.6458848329242314890, 27.79145980994124088, 2.105047925194707403 ) ) ;
#15326=ORIENTED_EDGE ( 'NONE', *, *, #2144, .F. ) ;
#15327=EDGE_CURVE ( 'NONE', #10853, #23711, #16909, .T. ) ;
#15330=CIRCLE ( 'NONE', #21939, 2.729128784747790970 ) ;
#15333=DIRECTION ( 'NONE',  ( 0.000000000000000000, 1.000000000000000000, 0.000000000000000000 ) ) ;
#15335=CARTESIAN_POINT ( 'NONE',  ( -1.095323197919201519, 30.85834471387956413, -1.858592797474962754 ) ) ;
#15336=CARTESIAN_POINT ( 'NONE',  ( 2.500000000000000000, 27.03419673618999752, 0.000000000000000000 ) ) ;
#15341=CARTESIAN_POINT ( 'NONE',  ( 2.322750540216000026, 26.78000240009999899, 1.687576972922000040 ) ) ;
#15342=AXIS2_PLACEMENT_3D ( 'NONE', #21425, #8225, #15952 ) ;
#15344=CARTESIAN_POINT ( 'NONE',  ( 2.069432874219926166, 29.04090307382888625, -0.6216230384549564780 ) ) ;
#15349=ORIENTED_EDGE ( 'NONE', *, *, #10633, .T. ) ;
#15352=LINE ( 'NONE', #4107, #13034 ) ;
#15353=B_SPLINE_CURVE_WITH_KNOTS ( 'NONE', 3,
 ( #487, #20852, #9470, #16846, #16724, #20727, #15382, #249 ),
 .UNSPECIFIED., .F., .F.,
 ( 4, 2, 2, 4 ),
 ( 1.477043467946315188E-05, 0.0004760515949908603051, 0.0009373327553022574006, 0.001859895075925053001 ),
 .UNSPECIFIED. ) ;
#15359=ORIENTED_EDGE ( 'NONE', *, *, #8989, .T. ) ;
#15360=CARTESIAN_POINT ( 'NONE',  ( 2.147930124081999903, 30.14433166633000027, -1.675020066154000231 ) ) ;
#15361=CARTESIAN_POINT ( 'NONE',  ( 0.3139855153997000436, 24.38894642224000009, 2.697844032124999902 ) ) ;
#15363=ORIENTED_EDGE ( 'NONE', *, *, #19725, .F. ) ;
#15364=FACE_OUTER_BOUND ( 'NONE', #1029, .T. ) ;
#15367=FACE_OUTER_BOUND ( 'NONE', #4932, .T. ) ;
#15370=FACE_OUTER_BOUND ( 'NONE', #20400, .T. ) ;
#15372=CARTESIAN_POINT ( 'NONE',  ( -2.500000000000000000, 26.50000000000000355, 0.000000000000000000 ) ) ;
#15373=ORIENTED_EDGE ( 'NONE', *, *, #8228, .T. ) ;
#15374=DIRECTION ( 'NONE',  ( 0.000000000000000000, 1.000000000000000000, 0.000000000000000000 ) ) ;
#15375=AXIS2_PLACEMENT_3D ( 'NONE', #9034, #21989, #12440 ) ;
#15379=CARTESIAN_POINT ( 'NONE',  ( -2.685167613138000231, 25.68485474111000144, 0.5308767225436000770 ) ) ;
#15382=CARTESIAN_POINT ( 'NONE',  ( 0.4554420578654839735, 24.53874986669016778, 2.337013420279270726 ) ) ;
#15385=DIRECTION ( 'NONE',  ( 0.000000000000000000, 0.000000000000000000, 1.000000000000000000 ) ) ;
#15387=ORIENTED_EDGE ( 'NONE', *, *, #1963, .T. ) ;
#15390=CARTESIAN_POINT ( 'NONE',  ( 3.000000000000000000, 20.10000000000000142, 0.000000000000000000 ) ) ;
#15393=CARTESIAN_POINT ( 'NONE',  ( 1.699999998837999904, 12.90000000000000036, -1.053565373074999867 ) ) ;
#15394=DIRECTION ( 'NONE',  ( 0.000000000000000000, 0.000000000000000000, -1.000000000000000000 ) ) ;
#15398=EDGE_CURVE ( 'NONE', #12379, #953, #17274, .T. ) ;
#15399=CARTESIAN_POINT ( 'NONE',  ( 2.220168113581999947, 28.86544355015000107, -0.7890638476296999437 ) ) ;
#15402=CONICAL_SURFACE ( 'NONE', #18136, 2.249999993279999888, 0.7853981633972997312 ) ;
#15403=CARTESIAN_POINT ( 'NONE',  ( -0.5680056327079126000, 29.56997042186494795, 2.083912535968097224 ) ) ;
#15405=CARTESIAN_POINT ( 'NONE',  ( 0.9838067277388000686, 24.96693921933999860, -2.132932039142000136 ) ) ;
#15411=CARTESIAN_POINT ( 'NONE',  ( -2.125654151014383153, 30.86397478161066843, 0.2102433260543445648 ) ) ;
#15417=CARTESIAN_POINT ( 'NONE',  ( -1.181632374603359237, 24.55137445130588958, -3.936586548166618460 ) ) ;
#15421=FACE_OUTER_BOUND ( 'NONE', #22645, .T. ) ;
#15423=DIRECTION ( 'NONE',  ( 0.000000000000000000, 0.000000000000000000, -1.000000000000000000 ) ) ;
#15431=DIRECTION ( 'NONE',  ( -1.000000000000000000, 0.000000000000000000, 0.000000000000000000 ) ) ;
#15432=AXIS2_PLACEMENT_3D ( 'NONE', #21390, #10248, #10007 ) ;
#15433=CARTESIAN_POINT ( 'NONE',  ( -1.999167105995453442, 28.95086340285666182, -1.536366799937283645 ) ) ;
#15434=CARTESIAN_POINT ( 'NONE',  ( 2.500000000000000000, 27.83419673618999823, 0.000000000000000000 ) ) ;
#15435=CARTESIAN_POINT ( 'NONE',  ( -0.1289249096770258562, 30.39619859440238159, 2.156031166653296971 ) ) ;
#15442=CARTESIAN_POINT ( 'NONE',  ( -1.954613887214999846, 25.91864211381999894, -1.197800277839999872 ) ) ;
#15444=VECTOR ( 'NONE', #6300, 1000.000000000000000 ) ;
#15449=CARTESIAN_POINT ( 'NONE',  ( 1.473293862388198594, 28.13663838358920088, -1.634089070379382891 ) ) ;
#15460=CARTESIAN_POINT ( 'NONE',  ( -0.8766499437396024774, 28.75150226347701476, 1.987951473063243935 ) ) ;
#15463=CARTESIAN_POINT ( 'NONE',  ( -2.500000000000000000, 26.63419673618999894, 0.000000000000000000 ) ) ;
#15464=EDGE_LOOP ( 'NONE', ( #19124, #14599, #14400, #4101 ) ) ;
#15466=CARTESIAN_POINT ( 'NONE',  ( 1.099251314038999894, 29.01456776952000283, 2.157402177123000087 ) ) ;
#15467=CIRCLE ( 'NONE', #5060, 0.5500000000000001554 ) ;
#15469=CARTESIAN_POINT ( 'NONE',  ( 1.439764776165384008, 28.89522456450965038, 1.649428253125927668 ) ) ;
#15472=EDGE_CURVE ( 'NONE', #9272, #12394, #20379, .T. ) ;
#15474=DIRECTION ( 'NONE',  ( 0.000000000000000000, 1.000000000000000000, 0.000000000000000000 ) ) ;
#15479=DIRECTION ( 'NONE',  ( 1.000000000000000000, 0.000000000000000000, 0.000000000000000000 ) ) ;
#15483=CARTESIAN_POINT ( 'NONE',  ( 2.500000000000001776, 27.58333333333333570, 0.3272492347489265874 ) ) ;
#15484=VERTEX_POINT ( 'NONE', #4183 ) ;
#15486=CARTESIAN_POINT ( 'NONE',  ( 0.01985994072882999936, 24.87862773921999704, -2.525494120218000127 ) ) ;
#15488=CIRCLE ( 'NONE', #8945, 3.100000000000000089 ) ;
#15489=VERTEX_POINT ( 'NONE', #21014 ) ;
#15492=CARTESIAN_POINT ( 'NONE',  ( 1.932766431522000117, 28.47362202384999819, 1.950198670200999906 ) ) ;
#15497=DIRECTION ( 'NONE',  ( -1.000000000000000000, 0.000000000000000000, 0.000000000000000000 ) ) ;
#15503=CARTESIAN_POINT ( 'NONE',  ( 2.031887307395044751, 24.15498103193775492, 0.8252474979483435114 ) ) ;
#15515=DIRECTION ( 'NONE',  ( 0.000000000000000000, -1.000000000000000000, 0.000000000000000000 ) ) ;
#15524=CARTESIAN_POINT ( 'NONE',  ( -0.5273013900716050362, 29.57247171166937605, 2.094731424541075526 ) ) ;
#15526=CARTESIAN_POINT ( 'NONE',  ( -1.677508373566000133, 23.67725715092000272, 1.401457983775999949 ) ) ;
#15528=ORIENTED_EDGE ( 'NONE', *, *, #9269, .F. ) ;
#15529=CARTESIAN_POINT ( 'NONE',  ( -2.191702116096594821, 24.63208194274876917, -0.6023946256753694994 ) ) ;
#15531=CARTESIAN_POINT ( 'NONE',  ( -2.123582770898495120, 30.87008440628623873, 0.1642131033563037079 ) ) ;
#15535=ORIENTED_EDGE ( 'NONE', *, *, #9210, .T. ) ;
#15536=FACE_OUTER_BOUND ( 'NONE', #6687, .T. ) ;
#15539=VERTEX_POINT ( 'NONE', #13502 ) ;
#15540=CARTESIAN_POINT ( 'NONE',  ( -4.549999999999999822, 24.49999999999999645, 0.000000000000000000 ) ) ;
#15542=DIRECTION ( 'NONE',  ( 0.000000000000000000, 1.000000000000000000, 0.000000000000000000 ) ) ;
#15544=CARTESIAN_POINT ( 'NONE',  ( 4.000000000000000888, 26.37418302490048561, 1.506880184559474811 ) ) ;
#15547=ADVANCED_FACE ( 'NONE', ( #2607, #2126 ), #3953, .F. ) ;
#15550=CARTESIAN_POINT ( 'NONE',  ( -1.350914310362234527, 26.47444252552741872, 3.838851412777818606 ) ) ;
#15553=CARTESIAN_POINT ( 'NONE',  ( -0.9850774032204228092, 30.06393871203397339, -1.927287055198054322 ) ) ;
#15557=CARTESIAN_POINT ( 'NONE',  ( 1.999167105995457216, 27.75086340285666608, 1.536366799937278760 ) ) ;
#15560=AXIS2_PLACEMENT_3D ( 'NONE', #2565, #15515, #19285 ) ;
#15562=ORIENTED_EDGE ( 'NONE', *, *, #17390, .F. ) ;
#15565=CARTESIAN_POINT ( 'NONE',  ( 4.750000000000000000, 22.19999999999999574, 0.000000000000000000 ) ) ;
#15566=CARTESIAN_POINT ( 'NONE',  ( -1.908614330669104797, 27.69283736032755172, 1.033640524002992667 ) ) ;
#15574=CARTESIAN_POINT ( 'NONE',  ( 0.000000000000000000, 24.50000000000000000, 0.000000000000000000 ) ) ;
#15577=CARTESIAN_POINT ( 'NONE',  ( 1.259047450927257339, 26.90086340285667177, 2.184465970885639763 ) ) ;
#15583=CARTESIAN_POINT ( 'NONE',  ( 1.304555153736000062, 26.08956776952000212, -2.329463490920999913 ) ) ;
#15586=CARTESIAN_POINT ( 'NONE',  ( 2.013606499909832426, 28.95625055469338349, 0.7894195048039055473 ) ) ;
#15587=CARTESIAN_POINT ( 'NONE',  ( 0.1442055869094999998, 27.60687716035999983, -2.445277951317000209 ) ) ;
#15589=VERTEX_POINT ( 'NONE', #8062 ) ;
#15594=EDGE_CURVE ( 'NONE', #20706, #10102, #18637, .T. ) ;
#15596=CARTESIAN_POINT ( 'NONE',  ( 0.000000000000000000, 26.20000000000000284, 4.618802153517000519 ) ) ;
#15597=AXIS2_PLACEMENT_3D ( 'NONE', #19311, #8541, #8652 ) ;
#15600=CARTESIAN_POINT ( 'NONE',  ( 1.999167105995457661, 27.51666666666667282, 1.536366799937278760 ) ) ;
#15601=ORIENTED_EDGE ( 'NONE', *, *, #6572, .T. ) ;
#15604=CARTESIAN_POINT ( 'NONE',  ( -2.185797623742999907, 30.54140998917999994, 1.625295296457000216 ) ) ;
#15605=CARTESIAN_POINT ( 'NONE',  ( 2.069451752920999699, 23.68449416383000283, 1.759067238232999930 ) ) ;
#15612=CARTESIAN_POINT ( 'NONE',  ( 0.000000000000000000, 17.00000000000000000, 0.000000000000000000 ) ) ;
#15613=AXIS2_PLACEMENT_3D ( 'NONE', #9710, #9472, #16617 ) ;
#15614=CARTESIAN_POINT ( 'NONE',  ( 0.000000000000000000, 18.50000000000000000, 0.000000000000000000 ) ) ;
#15616=DIRECTION ( 'NONE',  ( 0.000000000000000000, 0.000000000000000000, -1.000000000000000000 ) ) ;
#15619=DIRECTION ( 'NONE',  ( -0.9970458808888235103, 0.000000000000000000, -0.07680827691486176445 ) ) ;
#15620=CARTESIAN_POINT ( 'NONE',  ( -1.660235382367824641, 24.69477898227424006, 1.432877587170922284 ) ) ;
#15629=EDGE_LOOP ( 'NONE', ( #11491, #14991, #17757, #23439 ) ) ;
#15630=EDGE_CURVE ( 'NONE', #23948, #2047, #23466, .T. ) ;
#15632=LINE ( 'NONE', #15393, #20235 ) ;
#15639=CARTESIAN_POINT ( 'NONE',  ( -0.9423453617915489300, 29.54624551692468160, 1.944123615020682427 ) ) ;
#15640=EDGE_LOOP ( 'NONE', ( #2952, #3268, #18718 ) ) ;
#15641=CARTESIAN_POINT ( 'NONE',  ( -2.323275342901000240, 23.64078167485000037, 0.3458804795797000287 ) ) ;
#15642=AXIS2_PLACEMENT_3D ( 'NONE', #16220, #12597, #19983 ) ;
#15648=DIRECTION ( 'NONE',  ( 1.000000000000000000, 0.000000000000000000, 0.000000000000000000 ) ) ;
#15651=DIRECTION ( 'NONE',  ( 0.5000000000000169864, 0.000000000000000000, -0.8660254037844289376 ) ) ;
#15653=CARTESIAN_POINT ( 'NONE',  ( -2.184465970885646424, 27.13333333333333641, -1.259047450927245126 ) ) ;
#15654=CARTESIAN_POINT ( 'NONE',  ( 3.649794085728313320, 24.70197603011190068, -2.511592555635393964 ) ) ;
#15656=CARTESIAN_POINT ( 'NONE',  ( 4.000000000000000000, 26.24995697614769341, -2.103311180602513986 ) ) ;
#15669=CARTESIAN_POINT ( 'NONE',  ( -1.903056763539824114, 30.14106874054843033, -1.021523276054197904 ) ) ;
#15673=FACE_OUTER_BOUND ( 'NONE', #11599, .T. ) ;
#15675=CONICAL_SURFACE ( 'NONE', #12987, 2.949999944334000368, 0.7853981633972997312 ) ;
#15682=CARTESIAN_POINT ( 'NONE',  ( -2.059085180431123874, 28.38319450762345753, -0.7814348820212547730 ) ) ;
#15684=DIRECTION ( 'NONE',  ( -1.000000000000000000, 0.000000000000000000, 0.000000000000000000 ) ) ;
#15685=VERTEX_POINT ( 'NONE', #14109 ) ;
#15692=CARTESIAN_POINT ( 'NONE',  ( -3.999999999999999112, 26.49040384242090695, -0.4670641126940866528 ) ) ;
#15698=CARTESIAN_POINT ( 'NONE',  ( 0.000000000000000000, 22.09999988306815766, 0.000000000000000000 ) ) ;
#15699=CARTESIAN_POINT ( 'NONE',  ( 1.402946323589000066, 26.19500240010000169, -2.505154520421000175 ) ) ;
#15701=CARTESIAN_POINT ( 'NONE',  ( 2.000000000000000000, 26.50000000000000355, 3.464101615137999968 ) ) ;
#15711=LINE ( 'NONE', #704, #9963 ) ;
#15715=ADVANCED_FACE ( 'NONE', ( #10240 ), #13013, .T. ) ;
#15716=CARTESIAN_POINT ( 'NONE',  ( 2.184465970885649977, 27.53333333333333499, 1.259047450927240686 ) ) ;
#15719=CARTESIAN_POINT ( 'NONE',  ( -1.534530130794999891, 30.23743619718000275, -2.015030406789999784 ) ) ;
#15721=DIRECTION ( 'NONE',  ( 0.000000000000000000, -1.000000000000000000, 0.000000000000000000 ) ) ;
#15728=CARTESIAN_POINT ( 'NONE',  ( -2.745296661449999842, 28.97628422304000040, 0.04506516330758999350 ) ) ;
#15732=B_SPLINE_CURVE_WITH_KNOTS ( 'NONE', 3,
 ( #19885, #16241, #10565, #3423, #16354, #1477 ),
 .UNSPECIFIED., .F., .F.,
 ( 4, 2, 4 ),
 ( 0.000000000000000000, 0.5000000000000000000, 1.000000000000000000 ),
 .UNSPECIFIED. ) ;
#15735=DIRECTION ( 'NONE',  ( 0.000000000000000000, -1.000000000000000000, 0.000000000000000000 ) ) ;
#15737=EDGE_LOOP ( 'NONE', ( #12917, #14989, #10947, #22103 ) ) ;
#15739=CARTESIAN_POINT ( 'NONE',  ( 1.472141380057878868, 24.50000000000001421, -1.988599837602683218 ) ) ;
#15741=CARTESIAN_POINT ( 'NONE',  ( 2.112965035456999985, 25.89200715711999834, -0.7396727963457000454 ) ) ;
#15742=CARTESIAN_POINT ( 'NONE',  ( -1.568717858167619994, 23.70514940564993012, -1.532321819884336023 ) ) ;
#15756=DIRECTION ( 'NONE',  ( 1.552013396384999864E-11, 0.000000000000000000, 1.000000000000000000 ) ) ;
#15761=LINE ( 'NONE', #13955, #7267 ) ;
#15765=AXIS2_PLACEMENT_3D ( 'NONE', #13911, #664, #8070 ) ;
#15767=CARTESIAN_POINT ( 'NONE',  ( -1.745680696064461523, 29.32358447642451438, -1.273442031135304964 ) ) ;
#15768=EDGE_LOOP ( 'NONE', ( #16607, #5172, #10258, #11263 ) ) ;
#15772=ORIENTED_EDGE ( 'NONE', *, *, #436, .F. ) ;
#15773=DIRECTION ( 'NONE',  ( 0.7071067811867980391, 0.7071067811862969954, -5.435108384955979519E-09 ) ) ;
#15775=EDGE_CURVE ( 'NONE', #7466, #12844, #2992, .T. ) ;
#15778=CARTESIAN_POINT ( 'NONE',  ( 1.699999999999999956, 9.029776245285399128, -0.9151600407964531891 ) ) ;
#15780=ORIENTED_EDGE ( 'NONE', *, *, #2004, .F. ) ;
#15783=CARTESIAN_POINT ( 'NONE',  ( 0.000000000000000000, 18.00000000000000000, 0.000000000000000000 ) ) ;
#15786=DIRECTION ( 'NONE',  ( 0.000000000000000000, 0.000000000000000000, -1.000000000000000000 ) ) ;
#15788=CARTESIAN_POINT ( 'NONE',  ( -4.000000000000000000, 26.20000000000000284, 2.309401076759000304 ) ) ;
#15791=CONICAL_SURFACE ( 'NONE', #5365, 4.309401076758999416, 1.119376321708719590 ) ;
#15797=CARTESIAN_POINT ( 'NONE',  ( -2.098716048264661183, 30.17350835825882882, -0.5109231943707897017 ) ) ;
#15802=FACE_OUTER_BOUND ( 'NONE', #15152, .T. ) ;
#15807=CARTESIAN_POINT ( 'NONE',  ( 1.640193969998194001, 24.74015355458762144, 1.405240085690787843 ) ) ;
#15808=DIRECTION ( 'NONE',  ( 0.000000000000000000, -1.000000000000000000, 0.000000000000000000 ) ) ;
#15809=CONICAL_SURFACE ( 'NONE', #8484, 4.309401076758999416, 1.119376321708719590 ) ;
#15810=CARTESIAN_POINT ( 'NONE',  ( 0.5508124349485069571, 27.39697001148643807, -2.099160625523386781 ) ) ;
#15812=DIRECTION ( 'NONE',  ( -0.000000000000000000, -1.000000000000000000, -0.000000000000000000 ) ) ;
#15813=ORIENTED_EDGE ( 'NONE', *, *, #21985, .T. ) ;
#15815=CONICAL_SURFACE ( 'NONE', #15432, 2.849999992212000066, 0.7853981633972997312 ) ;
#15821=CARTESIAN_POINT ( 'NONE',  ( 1.852496879401591912, 28.27448153086328730, -1.136612110235776019 ) ) ;
#15824=CARTESIAN_POINT ( 'NONE',  ( 0.000000000000000000, 21.89999999999999858, -4.749999999999985789 ) ) ;
#15826=CARTESIAN_POINT ( 'NONE',  ( 2.504532394112000003E-14, 28.43419673618999965, 2.500000000000000000 ) ) ;
#15827=CARTESIAN_POINT ( 'NONE',  ( 1.834054417453000019, 26.46369850838000204, 1.332518472557000067 ) ) ;
#15828=CIRCLE ( 'NONE', #22400, 2.750000000000000000 ) ;
#15829=CIRCLE ( 'NONE', #13122, 2.948682383037074750 ) ;
#15830=FACE_OUTER_BOUND ( 'NONE', #3525, .T. ) ;
#15834=ORIENTED_EDGE ( 'NONE', *, *, #5231, .T. ) ;
#15840=CARTESIAN_POINT ( 'NONE',  ( -2.434931691670790155, 27.40086340285667532, -0.6543697108981963995 ) ) ;
#15846=CARTESIAN_POINT ( 'NONE',  ( -2.032503672545999951, 30.43597535861000125, 1.511310389916999952 ) ) ;
#15847=CARTESIAN_POINT ( 'NONE',  ( 2.661087342023999547, 23.74853527822999766, 0.5436575690810000472 ) ) ;
#15848=DIRECTION ( 'NONE',  ( 1.000000000000000000, 0.000000000000000000, 0.000000000000000000 ) ) ;
#15849=CIRCLE ( 'NONE', #22425, 4.649999999999999467 ) ;
#15851=DIRECTION ( 'NONE',  ( 1.000000000000000000, 0.000000000000000000, 0.000000000000000000 ) ) ;
#15853=CARTESIAN_POINT ( 'NONE',  ( -2.344225979797000203, 28.90447533745000186, -1.429436635564000024 ) ) ;
#15857=CARTESIAN_POINT ( 'NONE',  ( -4.000000000000000000, 24.80000000000000426, 2.309401076759000304 ) ) ;
#15860=EDGE_LOOP ( 'NONE', ( #4078, #794, #2341, #20437 ) ) ;
#15864=CARTESIAN_POINT ( 'NONE',  ( -0.7526554537551000124, 24.11634424051000281, 2.431350270797000057 ) ) ;
#15868=FACE_OUTER_BOUND ( 'NONE', #15640, .T. ) ;
#15871=EDGE_LOOP ( 'NONE', ( #23016, #21369, #20992, #17914 ) ) ;
#15873=DIRECTION ( 'NONE',  ( 0.000000000000000000, 0.000000000000000000, 1.000000000000000000 ) ) ;
#15879=DIRECTION ( 'NONE',  ( 1.000000000000000000, 0.000000000000000000, 0.000000000000000000 ) ) ;
#15880=DIRECTION ( 'NONE',  ( 0.000000000000000000, 1.000000000000000000, 0.000000000000000000 ) ) ;
#15886=CARTESIAN_POINT ( 'NONE',  ( -1.841895772823868960, 29.33354493891415160, -1.134390543764295822 ) ) ;
#15888=CARTESIAN_POINT ( 'NONE',  ( 0.6543697108981982868, 29.36666666666666359, -2.434931691670790155 ) ) ;
#15890=ADVANCED_FACE ( 'NONE', ( #1233 ), #23857, .F. ) ;
#15894=ADVANCED_FACE ( 'NONE', ( #12023 ), #17346, .F. ) ;
#15898=DIRECTION ( 'NONE',  ( 0.8866244295713172630, 0.000000000000000000, 0.4624901305837091359 ) ) ;
#15899=CARTESIAN_POINT ( 'NONE',  ( 1.259047450927246903, 26.93333333333332646, -2.184465970885645536 ) ) ;
#15900=CARTESIAN_POINT ( 'NONE',  ( 2.327192509895192885, 24.50639765414752702, -3.274853329251975698 ) ) ;
#15901=ORIENTED_EDGE ( 'NONE', *, *, #17390, .T. ) ;
#15903=DIRECTION ( 'NONE',  ( -0.000000000000000000, -1.000000000000000000, -0.000000000000000000 ) ) ;
#15904=CARTESIAN_POINT ( 'NONE',  ( -2.160826008357635164, 26.50000000000000355, 3.371248675920325955 ) ) ;
#15909=EDGE_CURVE ( 'NONE', #6758, #16136, #14319, .T. ) ;
#15910=CARTESIAN_POINT ( 'NONE',  ( 1.595510613210902928, 26.49040384242091761, 3.697633671484740425 ) ) ;
#15911=CARTESIAN_POINT ( 'NONE',  ( -2.080319161808850570, 30.16916080325708904, -0.5827450134709621921 ) ) ;
#15912=ORIENTED_EDGE ( 'NONE', *, *, #12322, .F. ) ;
#15915=CARTESIAN_POINT ( 'NONE',  ( 0.000000000000000000, 17.00000000000000000, -2.704938617610999654E-14 ) ) ;
#15916=CARTESIAN_POINT ( 'NONE',  ( -1.605639779780836829, 23.61395945400231611, -1.383350294238146372 ) ) ;
#15919=CARTESIAN_POINT ( 'NONE',  ( -3.100000000000000089, 22.00000000000000000, 0.000000000000000000 ) ) ;
#15926=CARTESIAN_POINT ( 'NONE',  ( -0.8667355603187372193, 26.97782460062819254, 2.020380412232955170 ) ) ;
#15929=DIRECTION ( 'NONE',  ( 0.8500000000000165201, 0.000000000000000000, -0.5267826876426102700 ) ) ;
#15933=DIRECTION ( 'NONE',  ( -0.5000000000000169864, 0.000000000000000000, -0.8660254037844289376 ) ) ;
#15936=CARTESIAN_POINT ( 'NONE',  ( -4.000000000000000888, 26.37418302490047850, -1.506880184559495017 ) ) ;
#15937=CARTESIAN_POINT ( 'NONE',  ( 2.000000000000000000, 26.50000000000000355, -3.464101615137999968 ) ) ;
#15943=CARTESIAN_POINT ( 'NONE',  ( 1.994688225595000253, 25.78913313894999959, 1.016344414748000080 ) ) ;
#15952=DIRECTION ( 'NONE',  ( 0.000000000000000000, 0.000000000000000000, -1.000000000000000000 ) ) ;
#15954=CARTESIAN_POINT ( 'NONE',  ( 0.000000000000000000, 9.050044887908999414, 0.000000000000000000 ) ) ;
#15958=CARTESIAN_POINT ( 'NONE',  ( 0.000000000000000000, 17.00000000000000000, 0.000000000000000000 ) ) ;
#15961=CARTESIAN_POINT ( 'NONE',  ( -1.747945498421000110, 29.54871418206000300, -2.089014728103999907 ) ) ;
#15964=ORIENTED_EDGE ( 'NONE', *, *, #18692, .F. ) ;
#15965=DIRECTION ( 'NONE',  ( 1.000000000000000000, 0.000000000000000000, 0.000000000000000000 ) ) ;
#15973=ORIENTED_EDGE ( 'NONE', *, *, #4818, .F. ) ;
#15974=CARTESIAN_POINT ( 'NONE',  ( 0.000000000000000000, 24.80000000000000426, 4.618802153517000519 ) ) ;
#15976=CARTESIAN_POINT ( 'NONE',  ( 1.317056079378642108, 23.81658996185279875, 1.926182033697757534 ) ) ;
#15977=EDGE_LOOP ( 'NONE', ( #15601, #17647 ) ) ;
#15978=CARTESIAN_POINT ( 'NONE',  ( -1.734000915526999975, 25.54365575949000089, 1.590878194398000156 ) ) ;
#15983=CONICAL_SURFACE ( 'NONE', #5922, 3.049999825846000157, 0.7853981633972997312 ) ;
#15987=CARTESIAN_POINT ( 'NONE',  ( -0.3272492347489284192, 30.01753006952332825, 2.500000000000001332 ) ) ;
#15988=DIRECTION ( 'NONE',  ( 0.9967542221350019771, 0.000000000000000000, 0.08050478654122018851 ) ) ;
#15990=VERTEX_POINT ( 'NONE', #23745 ) ;
#15992=DIRECTION ( 'NONE',  ( 1.000000000000000000, 0.000000000000000000, 0.000000000000000000 ) ) ;
#15994=DIRECTION ( 'NONE',  ( 0.000000000000000000, -1.000000000000000000, 0.000000000000000000 ) ) ;
#15995=CARTESIAN_POINT ( 'NONE',  ( 0.2973205334010999845, 29.50801477156000274, 2.147506602161000089 ) ) ;
#15998=VERTEX_POINT ( 'NONE', #11031 ) ;
#16001=CARTESIAN_POINT ( 'NONE',  ( 1.568686367319726882, 29.10097142498572964, -1.495817114762474809 ) ) ;
#16004=CARTESIAN_POINT ( 'NONE',  ( -2.434931691670790155, 29.56666666666666288, -0.6543697108981958444 ) ) ;
#16007=CARTESIAN_POINT ( 'NONE',  ( -1.767766952966000060, 30.50000000000000000, 1.767766952966000060 ) ) ;
#16011=EDGE_CURVE ( 'NONE', #3493, #1813, #8116, .T. ) ;
#16016=CARTESIAN_POINT ( 'NONE',  ( 2.653270836322024984, 24.53198827073824617, -3.086600612158302948 ) ) ;
#16017=VERTEX_POINT ( 'NONE', #3425 ) ;
#16023=ADVANCED_FACE ( 'NONE', ( #18536 ), #17398, .F. ) ;
#16025=CARTESIAN_POINT ( 'NONE',  ( 0.000000000000000000, 15.00000000000000000, 0.000000000000000000 ) ) ;
#16029=CARTESIAN_POINT ( 'NONE',  ( -2.155035702249775476, 30.21239445103314836, 0.1465990187513959708 ) ) ;
#16032=CARTESIAN_POINT ( 'NONE',  ( 1.940244192847000004, 25.08955421093999760, -1.300335925705000006 ) ) ;
#16036=CARTESIAN_POINT ( 'NONE',  ( -1.189123363982122816, 23.61714873636219636, -1.751662368594682162 ) ) ;
#16037=CIRCLE ( 'NONE', #5603, 3.000000000000000000 ) ;
#16039=FACE_OUTER_BOUND ( 'NONE', #6897, .T. ) ;
#16042=ORIENTED_EDGE ( 'NONE', *, *, #6661, .F. ) ;
#16048=CARTESIAN_POINT ( 'NONE',  ( 0.3732672031689003855, 27.05179143783847451, 2.138410171147020922 ) ) ;
#16051=VERTEX_POINT ( 'NONE', #2906 ) ;
#16056=CARTESIAN_POINT ( 'NONE',  ( -1.888459278277104156E-11, 26.49469377355791977, -2.394693773557865057 ) ) ;
#16058=CARTESIAN_POINT ( 'NONE',  ( 0.3219846793369715576, 27.58545158304634626, -2.185093432021212312 ) ) ;
#16061=DIRECTION ( 'NONE',  ( 0.000000000000000000, -1.000000000000000000, 0.000000000000000000 ) ) ;
#16062=EDGE_LOOP ( 'NONE', ( #4316, #1369, #17762, #13539 ) ) ;
#16065=CARTESIAN_POINT ( 'NONE',  ( 1.745401010056999880, 27.34913313894999831, 1.745401010056999880 ) ) ;
#16084=CARTESIAN_POINT ( 'NONE',  ( -0.3631102237552999989, 28.93590169452000183, 2.430407043875000284 ) ) ;
#16087=VERTEX_POINT ( 'NONE', #3027 ) ;
#16089=DIRECTION ( 'NONE',  ( 0.000000000000000000, 1.000000000000000000, 0.000000000000000000 ) ) ;
#16091=CARTESIAN_POINT ( 'NONE',  ( 0.1326132519488843198, 24.52237361985764252, -2.377626380141467433 ) ) ;
#16097=DIRECTION ( 'NONE',  ( 0.000000000000000000, 0.000000000000000000, 1.000000000000000000 ) ) ;
#16098=AXIS2_PLACEMENT_3D ( 'NONE', #10071, #17456, #15619 ) ;
#16099=CARTESIAN_POINT ( 'NONE',  ( 1.699999998870999951, 12.90000000000000036, 1.053565372968999991 ) ) ;
#16102=CARTESIAN_POINT ( 'NONE',  ( 0.6689641713224000474, 25.78843094911999856, 2.455688058221999981 ) ) ;
#16106=CARTESIAN_POINT ( 'NONE',  ( 0.6543697108981982868, 27.76666666666666572, -2.434931691670790155 ) ) ;
#16107=CARTESIAN_POINT ( 'NONE',  ( -4.750000000000000000, 21.89999999999999858, 0.000000000000000000 ) ) ;
#16110=CARTESIAN_POINT ( 'NONE',  ( 2.184465970885649089, 30.16753006952333038, 1.259047450927240241 ) ) ;
#16111=DIRECTION ( 'NONE',  ( 0.000000000000000000, 0.000000000000000000, 1.000000000000000000 ) ) ;
#16117=CARTESIAN_POINT ( 'NONE',  ( 1.958365003997999843, 25.72990814437000040, -0.6262921420760999558 ) ) ;
#16119=CARTESIAN_POINT ( 'NONE',  ( 0.000000000000000000, 23.00000000000000000, 0.000000000000000000 ) ) ;
#16120=CARTESIAN_POINT ( 'NONE',  ( 2.009621439914000440, 30.44153028435000152, 0.8133916002304999449 ) ) ;
#16127=DIRECTION ( 'NONE',  ( 1.000000000000000000, 0.000000000000000000, 0.000000000000000000 ) ) ;
#16128=CONICAL_SURFACE ( 'NONE', #15342, 4.309401076758999416, 1.119376321708719590 ) ;
#16130=CARTESIAN_POINT ( 'NONE',  ( 2.500000000000000000, 30.00000000000000000, 0.000000000000000000 ) ) ;
#16132=AXIS2_PLACEMENT_3D ( 'NONE', #315, #13043, #5781 ) ;
#16136=VERTEX_POINT ( 'NONE', #17806 ) ;
#16137=FACE_OUTER_BOUND ( 'NONE', #23858, .T. ) ;
#16141=EDGE_LOOP ( 'NONE', ( #2948, #3473, #12416, #15283 ) ) ;
#16145=DIRECTION ( 'NONE',  ( -1.000000000000000000, 0.000000000000000000, 0.000000000000000000 ) ) ;
#16147=CIRCLE ( 'NONE', #18471, 4.750000000000000000 ) ;
#16150=CARTESIAN_POINT ( 'NONE',  ( -0.9467213981002000622, 29.56141545196999942, 2.143184182326999920 ) ) ;
#16153=CARTESIAN_POINT ( 'NONE',  ( 1.506643486780510299, 29.90540180240715529, -1.547753345910543699 ) ) ;
#16154=ORIENTED_EDGE ( 'NONE', *, *, #4489, .T. ) ;
#16160=SHAPE_REPRESENTATION ( 'Valve Operating Stem', ( #4390 ), #23331 ) ;
#16161=LINE ( 'NONE', #8673, #1781 ) ;
#16164=CONICAL_SURFACE ( 'NONE', #22352, 2.849999993810000021, 0.7853981633972997312 ) ;
#16168=VERTEX_POINT ( 'NONE', #13254 ) ;
#16169=CARTESIAN_POINT ( 'NONE',  ( -0.2537098930414913855, 27.01480801923332820, 2.155742384934690392 ) ) ;
#16175=CARTESIAN_POINT ( 'NONE',  ( 0.000000000000000000, 9.100092063578999912, 0.000000000000000000 ) ) ;
#16182=CARTESIAN_POINT ( 'NONE',  ( -1.488838795626273637, 27.10843084945087256, 1.583244740691588159 ) ) ;
#16184=CARTESIAN_POINT ( 'NONE',  ( 4.000000000000000000, 26.20000000000000284, -2.309401076759000304 ) ) ;
#16186=CARTESIAN_POINT ( 'NONE',  ( 1.299491417509237579, 30.72164040778775274, -1.726027442315023697 ) ) ;
#16188=CARTESIAN_POINT ( 'NONE',  ( -0.6950034797113096019, 26.37418302490043587, -4.217541707417931995 ) ) ;
#16190=CARTESIAN_POINT ( 'NONE',  ( -1.675531247043999805, 27.15413313894999803, 1.812579491195999815 ) ) ;
#16193=CARTESIAN_POINT ( 'NONE',  ( -1.197800277839999872, 28.25864211381999880, -1.954613887214999846 ) ) ;
#16195=VECTOR ( 'NONE', #3828, 1000.000000000000000 ) ;
#16199=DIRECTION ( 'NONE',  ( 0.000000000000000000, 0.000000000000000000, 1.000000000000000000 ) ) ;
#16203=ORIENTED_EDGE ( 'NONE', *, *, #5417, .F. ) ;
#16210=CIRCLE ( 'NONE', #2271, 1.600000000000000089 ) ;
#16211=ORIENTED_EDGE ( 'NONE', *, *, #3199, .F. ) ;
#16213=CARTESIAN_POINT ( 'NONE',  ( -0.9741922325766999569, 29.81343306396000159, 2.543667732614000254 ) ) ;
#16215=DIRECTION ( 'NONE',  ( 0.8500000008401347174, 0.000000000000000000, 0.5267826862870217397 ) ) ;
#16218=EDGE_LOOP ( 'NONE', ( #4412, #18166, #7113, #68, #18494, #10436 ) ) ;
#16220=CARTESIAN_POINT ( 'NONE',  ( 0.000000000000000000, 15.09999999999999964, 0.000000000000000000 ) ) ;
#16221=LINE ( 'NONE', #7020, #11975 ) ;
#16224=CARTESIAN_POINT ( 'NONE',  ( 2.424643331163519964E-11, 24.52694564545263844, -2.373054354547839306 ) ) ;
#16225=EDGE_CURVE ( 'NONE', #12189, #5466, #6126, .T. ) ;
#16227=CARTESIAN_POINT ( 'NONE',  ( 2.063594504837999888E-14, 28.80370090847999975, 2.160000000000000142 ) ) ;
#16229=DIRECTION ( 'NONE',  ( -0.000000000000000000, 1.000000000000000000, 0.000000000000000000 ) ) ;
#16232=CARTESIAN_POINT ( 'NONE',  ( 1.727343568716567690, 12.96873773180061207, 1.061322550613886140 ) ) ;
#16234=ORIENTED_EDGE ( 'NONE', *, *, #14565, .T. ) ;
#16236=CARTESIAN_POINT ( 'NONE',  ( 1.775541456815999952, 24.57013026871000250, -2.083124542231000298 ) ) ;
#16240=LINE ( 'NONE', #7037, #13297 ) ;
#16241=CARTESIAN_POINT ( 'NONE',  ( -1.315747796919693791, 23.71666666666667211, -1.829618100335548725 ) ) ;
#16245=CARTESIAN_POINT ( 'NONE',  ( -1.412199477822031035, 26.21336570662361964, 1.592595083443383963 ) ) ;
#16249=DIRECTION ( 'NONE',  ( 1.000000000000000000, 0.000000000000000000, 0.000000000000000000 ) ) ;
#16257=CARTESIAN_POINT ( 'NONE',  ( -0.8020744510286262896, 26.50000000000000355, 2.262007200476410684 ) ) ;
#16258=ORIENTED_EDGE ( 'NONE', *, *, #12823, .T. ) ;
#16260=DIRECTION ( 'NONE',  ( 1.511005137241999593E-08, -0.9999999999999997780, 8.997177532459998026E-09 ) ) ;
#16270=ORIENTED_EDGE ( 'NONE', *, *, #20638, .T. ) ;
#16272=CARTESIAN_POINT ( 'NONE',  ( -2.000000000000000000, 26.50000000000000355, 3.464101615137999968 ) ) ;
#16275=CARTESIAN_POINT ( 'NONE',  ( -2.186232643004999865, 30.22719044073999939, -0.09498792041393000485 ) ) ;
#16276=CONICAL_SURFACE ( 'NONE', #5833, 4.309401076758999416, 1.119376321708719590 ) ;
#16278=CARTESIAN_POINT ( 'NONE',  ( 0.8953157965490899928, 29.94952453685389315, -1.965511115583160384 ) ) ;
#16283=CARTESIAN_POINT ( 'NONE',  ( -0.9598074410945768298, 23.62549911315723605, -1.896475888262205478 ) ) ;
#16284=ORIENTED_EDGE ( 'NONE', *, *, #10409, .F. ) ;
#16292=CARTESIAN_POINT ( 'NONE',  ( 1.330759560658445029, 26.31212306573571524, 1.751177748763361075 ) ) ;
#16303=CARTESIAN_POINT ( 'NONE',  ( -1.781275706426519445, 27.08192969757271484, 1.242185054261912391 ) ) ;
#16304=DIRECTION ( 'NONE',  ( -0.7071067811905932254, -0.7071067811824932603, -1.099460899159990341E-07 ) ) ;
#16306=ORIENTED_EDGE ( 'NONE', *, *, #22837, .F. ) ;
#16309=CARTESIAN_POINT ( 'NONE',  ( 1.831974274068000064, 25.68369850838000090, 0.9334375154566999511 ) ) ;
#16312=CARTESIAN_POINT ( 'NONE',  ( 2.089231778180999921, 25.80521896305999974, 0.4700916780637000580 ) ) ;
#16320=ORIENTED_EDGE ( 'NONE', *, *, #14119, .F. ) ;
#16321=EDGE_CURVE ( 'NONE', #23625, #17141, #23535, .T. ) ;
#16322=CARTESIAN_POINT ( 'NONE',  ( -1.259047450927199163, 24.13333333333333641, 2.184465970885673070 ) ) ;
#16327=CARTESIAN_POINT ( 'NONE',  ( -2.135391386772000022, 30.15892637698999934, 0.2566162452548999551 ) ) ;
#16328=B_SPLINE_CURVE_WITH_KNOTS ( 'NONE', 3,
 ( #9648, #4315, #17270, #670, #18005, #23197, #23435, #2865 ),
 .UNSPECIFIED., .F., .F.,
 ( 4, 2, 2, 4 ),
 ( 0.000000000000000000, 0.2499999999999998890, 0.4999999999999997780, 1.000000000000000000 ),
 .UNSPECIFIED. ) ;
#16331=CIRCLE ( 'NONE', #20986, 3.100000000000000089 ) ;
#16332=ORIENTED_EDGE ( 'NONE', *, *, #10757, .T. ) ;
#16334=DIRECTION ( 'NONE',  ( 0.000000000000000000, -1.000000000000000000, 0.000000000000000000 ) ) ;
#16336=DIRECTION ( 'NONE',  ( -0.000000000000000000, 1.000000000000000000, -0.000000000000000000 ) ) ;
#16340=ADVANCED_FACE ( 'NONE', ( #23713 ), #5370, .T. ) ;
#16342=VERTEX_POINT ( 'NONE', #2353 ) ;
#16343=CARTESIAN_POINT ( 'NONE',  ( 1.350509132759432740, 30.61094555582495502, 2.026494689485950573 ) ) ;
#16345=B_SPLINE_CURVE_WITH_KNOTS ( 'NONE', 3,
 ( #8571, #2091, #3796, #20739 ),
 .UNSPECIFIED., .F., .F.,
 ( 4, 4 ),
 ( 0.000000000000000000, 1.000000000000000000 ),
 .UNSPECIFIED. ) ;
#16347=ORIENTED_EDGE ( 'NONE', *, *, #4552, .F. ) ;
#16348=CARTESIAN_POINT ( 'NONE',  ( -2.152918217223999786, 24.53250749508999817, -0.1897174181730999776 ) ) ;
#16354=CARTESIAN_POINT ( 'NONE',  ( -2.443333333333321811, 23.94333333333336356, -0.4702601233135134673 ) ) ;
#16355=EDGE_CURVE ( 'NONE', #10321, #2748, #10527, .T. ) ;
#16358=CARTESIAN_POINT ( 'NONE',  ( -0.02719911563634819923, 26.24132134161193264, 2.156122861279925917 ) ) ;
#16360=VERTEX_POINT ( 'NONE', #15540 ) ;
#16362=CARTESIAN_POINT ( 'NONE',  ( 2.101206698852999821, 24.06483916994999817, 0.4292744954273000624 ) ) ;
#16364=CARTESIAN_POINT ( 'NONE',  ( -4.000000000000000000, 24.50000000000000000, 2.309401076759000304 ) ) ;
#16370=EDGE_CURVE ( 'NONE', #16646, #17341, #8466, .T. ) ;
#16374=ORIENTED_EDGE ( 'NONE', *, *, #21183, .F. ) ;
#16375=CARTESIAN_POINT ( 'NONE',  ( 2.062405688592416908, 30.08447145040267401, -1.608325556874773410 ) ) ;
#16379=EDGE_CURVE ( 'NONE', #11959, #9355, #9984, .T. ) ;
#16380=VERTEX_POINT ( 'NONE', #23047 ) ;
#16389=AXIS2_PLACEMENT_3D ( 'NONE', #19944, #15812, #1175 ) ;
#16390=B_SPLINE_CURVE_WITH_KNOTS ( 'NONE', 3,
 ( #707, #17308, #17808, #2785, #17556, #830, #8476, #22987, #12234, #10171, #952, #1204, #22869, #15600, #15716, #8233, #15483, #8595 ),
 .UNSPECIFIED., .F., .F.,
 ( 4, 2, 2, 2, 2, 2, 2, 2, 4 ),
 ( 0.000000000000000000, 0.1250000000000000000, 0.2500000000000000000, 0.3750000000000000000, 0.5000000000000000000, 0.6250000000000000000, 0.7500000000000000000, 0.8750000000000000000, 1.000000000000000000 ),
 .UNSPECIFIED. ) ;
#16393=CARTESIAN_POINT ( 'NONE',  ( 1.724429579411198787, 29.88617415415703604, -1.300538479143458215 ) ) ;
#16396=CARTESIAN_POINT ( 'NONE',  ( -1.958067310766663738, 26.26028141853885245, 0.9125917284305815613 ) ) ;
#16397=CONICAL_SURFACE ( 'NONE', #15613, 4.699999872533999756, 0.7853981633972997312 ) ;
#16398=ORIENTED_EDGE ( 'NONE', *, *, #23265, .F. ) ;
#16402=ORIENTED_EDGE ( 'NONE', *, *, #21535, .F. ) ;
#16404=CIRCLE ( 'NONE', #11003, 2.500000000000001776 ) ;
#16405=VERTEX_POINT ( 'NONE', #6469 ) ;
#16408=LINE ( 'NONE', #5516, #19881 ) ;
#16417=CARTESIAN_POINT ( 'NONE',  ( -1.762470634073454390, 26.28689514065213473, 1.324303524335109783 ) ) ;
#16423=CARTESIAN_POINT ( 'NONE',  ( 2.267779804951839839, 26.36777980495183726, 5.387954023152814032E-08 ) ) ;
#16426=CARTESIAN_POINT ( 'NONE',  ( 1.516486965307999979, 26.72937716036000211, -1.923654546119000219 ) ) ;
#16429=ORIENTED_EDGE ( 'NONE', *, *, #4818, .T. ) ;
#16432=CARTESIAN_POINT ( 'NONE',  ( -1.944928363488455325, 29.16054931928814398, -1.185957275569452296 ) ) ;
#16433=ORIENTED_EDGE ( 'NONE', *, *, #17675, .F. ) ;
#16441=CARTESIAN_POINT ( 'NONE',  ( 1.633551575390000288, 29.03387112891999777, -1.399019918242000005 ) ) ;
#16452=CARTESIAN_POINT ( 'NONE',  ( 1.948101474242260878, 29.06061311738025665, -0.9327975164393527141 ) ) ;
#16453=EDGE_CURVE ( 'NONE', #23527, #20342, #13984, .T. ) ;
#16458=CARTESIAN_POINT ( 'NONE',  ( 1.401975630126000016, 24.25382637699000199, -1.644844636836000129 ) ) ;
#16462=CONICAL_SURFACE ( 'NONE', #12991, 1.449999902385000095, 0.7853981633972997312 ) ;
#16463=DIRECTION ( 'NONE',  ( 0.000000000000000000, 1.000000000000000000, 0.000000000000000000 ) ) ;
#16464=DIRECTION ( 'NONE',  ( 0.000000000000000000, -1.000000000000000000, 0.000000000000000000 ) ) ;
#16465=ADVANCED_FACE ( 'NONE', ( #15421 ), #6907, .T. ) ;
#16469=FACE_OUTER_BOUND ( 'NONE', #10885, .T. ) ;
#16474=CARTESIAN_POINT ( 'NONE',  ( -2.139397391632000378, 25.28162034356000021, -0.1494154476599000025 ) ) ;
#16476=B_SPLINE_CURVE_WITH_KNOTS ( 'NONE', 3,
 ( #1673, #23476, #14281, #5088, #5202, #12585, #16322, #19970, #8592, #7119, #3391, #8954, #10774, #14509, #14158, #12702, #18274, #20096 ),
 .UNSPECIFIED., .F., .F.,
 ( 4, 2, 2, 2, 2, 2, 2, 2, 4 ),
 ( 0.000000000000000000, 0.1250000000000000000, 0.2500000000000000000, 0.3750000000000000000, 0.5000000000000000000, 0.6250000000000000000, 0.7500000000000000000, 0.8750000000000000000, 1.000000000000000000 ),
 .UNSPECIFIED. ) ;
#16479=CARTESIAN_POINT ( 'NONE',  ( -0.6993571119973001071, 28.64630814436999984, 1.933477428368000073 ) ) ;
#16481=CARTESIAN_POINT ( 'NONE',  ( 0.000000000000000000, 24.65000000000000213, 0.000000000000000000 ) ) ;
#16483=AXIS2_PLACEMENT_3D ( 'NONE', #7935, #15185, #5987 ) ;
#16484=CARTESIAN_POINT ( 'NONE',  ( 0.000000000000000000, 16.94999982584599962, -3.049999825846000157 ) ) ;
#16486=ORIENTED_EDGE ( 'NONE', *, *, #3368, .F. ) ;
#16489=ORIENTED_EDGE ( 'NONE', *, *, #5432, .T. ) ;
#16490=CARTESIAN_POINT ( 'NONE',  ( 0.000000000000000000, 7.049999902385000183, 0.000000000000000000 ) ) ;
#16496=CARTESIAN_POINT ( 'NONE',  ( 1.960438172910999866, 27.17462896666999939, -1.812210406530999851 ) ) ;
#16506=B_SPLINE_CURVE_WITH_KNOTS ( 'NONE', 3,
 ( #1431, #3494, #3377, #21538, #8580, #10874, #23335, #16188, #14264, #14611 ),
 .UNSPECIFIED., .F., .F.,
 ( 4, 1, 1, 2, 2, 4 ),
 ( 0.000000000000000000, 0.2499999999999986677, 0.3749999999999980016, 0.4374999999999982236, 0.4999999999999984457, 1.000000000000000000 ),
 .UNSPECIFIED. ) ;
#16507=DIRECTION ( 'NONE',  ( -1.000000000000000000, 0.000000000000000000, 0.000000000000000000 ) ) ;
#16510=CARTESIAN_POINT ( 'NONE',  ( 0.3478861622692999700, 29.63335247264999950, 2.317001308406999804 ) ) ;
#16511=AXIS2_PLACEMENT_3D ( 'NONE', #8183, #6716, #6605 ) ;
#16513=AXIS2_PLACEMENT_3D ( 'NONE', #9561, #1939, #18758 ) ;
#16514=CARTESIAN_POINT ( 'NONE',  ( 2.137821094052745341, 29.82197946150706258, -0.3076343826834448403 ) ) ;
#16515=EDGE_CURVE ( 'NONE', #12867, #4139, #9612, .T. ) ;
#16516=ORIENTED_EDGE ( 'NONE', *, *, #7422, .T. ) ;
#16517=CARTESIAN_POINT ( 'NONE',  ( -0.7870591911094999560, 24.47971612415000209, -2.034558558890000146 ) ) ;
#16518=ADVANCED_FACE ( 'NONE', ( #9014 ), #3217, .T. ) ;
#16520=CONICAL_SURFACE ( 'NONE', #13415, 2.849999993810000021, 0.7853981633972997312 ) ;
#16526=ORIENTED_EDGE ( 'NONE', *, *, #9413, .T. ) ;
#16532=ORIENTED_EDGE ( 'NONE', *, *, #2301, .T. ) ;
#16539=CARTESIAN_POINT ( 'NONE',  ( 1.348160915820032946, 27.51919870340391938, -1.702933945497973722 ) ) ;
#16541=CARTESIAN_POINT ( 'NONE',  ( 2.022753006592888259, 30.64948983276336136, -0.7574018599443589350 ) ) ;
#16542=ORIENTED_EDGE ( 'NONE', *, *, #8685, .T. ) ;
#16545=VECTOR ( 'NONE', #22714, 1000.000000000000114 ) ;
#16547=CARTESIAN_POINT ( 'NONE',  ( 1.679993844339999987, 27.52771896306000343, -1.552970335759000120 ) ) ;
#16548=B_SPLINE_CURVE_WITH_KNOTS ( 'NONE', 3,
 ( #4345, #10045, #21179, #18878 ),
 .UNSPECIFIED., .F., .F.,
 ( 4, 4 ),
 ( 0.000000000000000000, 1.000000000000000000 ),
 .UNSPECIFIED. ) ;
#16549=DIRECTION ( 'NONE',  ( 0.000000000000000000, 0.000000000000000000, 1.000000000000000000 ) ) ;
#16551=EDGE_LOOP ( 'NONE', ( #19641, #12402, #660, #23603 ) ) ;
#16553=ORIENTED_CLOSED_SHELL ( 'NONE', *, #7696, .F. );
#16555=CYLINDRICAL_SURFACE ( 'NONE', #19229, 2.500000000000000000 ) ;
#16566=B_SPLINE_CURVE_WITH_KNOTS ( 'NONE', 3,
 ( #22044, #5453, #20118, #3527, #20230, #1815, #15976, #23369, #18752, #3872, #7491, #104, #7739, #15222, #2048, #16579, #9438, #337 ),
 .UNSPECIFIED., .F., .F.,
 ( 4, 2, 2, 2, 2, 2, 2, 2, 4 ),
 ( 0.000000000000000000, 0.1249999999999999445, 0.2499999999999998890, 0.3749999999999998335, 0.4999999999999997780, 0.6249999999999997780, 0.7499999999999998890, 0.8750000000000000000, 1.000000000000000000 ),
 .UNSPECIFIED. ) ;
#16568=CARTESIAN_POINT ( 'NONE',  ( 0.000000000000000000, 26.50000000000000355, 0.000000000000000000 ) ) ;
#16571=AXIS2_PLACEMENT_3D ( 'NONE', #10759, #3495, #12571 ) ;
#16574=FACE_OUTER_BOUND ( 'NONE', #17965, .T. ) ;
#16576=CARTESIAN_POINT ( 'NONE',  ( -1.261798464217251281, 29.28330482960407721, -1.753041514665990785 ) ) ;
#16579=CARTESIAN_POINT ( 'NONE',  ( -1.953336881554591065, 23.67957374523190239, 1.002735915203931683 ) ) ;
#16580=CONICAL_SURFACE ( 'NONE', #3815, 4.309401076758999416, 1.119376321708719590 ) ;
#16585=CARTESIAN_POINT ( 'NONE',  ( 0.000000000000000000, 13.00000000000000000, 0.000000000000000000 ) ) ;
#16592=DIRECTION ( 'NONE',  ( 0.000000000000000000, 0.000000000000000000, -1.000000000000000000 ) ) ;
#16593=PLANE ( 'NONE',  #3643 ) ;
#16594=EDGE_LOOP ( 'NONE', ( #15326, #19610, #1926, #5443 ) ) ;
#16597=CARTESIAN_POINT ( 'NONE',  ( 1.932058739753999888, 24.83333254276000090, 0.9308572216049000314 ) ) ;
#16599=CIRCLE ( 'NONE', #10024, 4.649999999999999467 ) ;
#16602=CARTESIAN_POINT ( 'NONE',  ( -0.9763371410079000334, 29.33077125539000107, 2.149176381922999646 ) ) ;
#16605=CARTESIAN_POINT ( 'NONE',  ( -1.615659476414179396, 26.36314323815835792, 1.591840916758156199 ) ) ;
#16607=ORIENTED_EDGE ( 'NONE', *, *, #19335, .F. ) ;
#16609=VECTOR ( 'NONE', #18052, 1000.000000000000000 ) ;
#16610=AXIS2_PLACEMENT_3D ( 'NONE', #9312, #18287, #9194 ) ;
#16617=DIRECTION ( 'NONE',  ( 0.000000000000000000, 0.000000000000000000, -1.000000000000000000 ) ) ;
#16618=CARTESIAN_POINT ( 'NONE',  ( -2.096579189799000265, 27.56462896666999995, 1.652809762273000027 ) ) ;
#16630=CARTESIAN_POINT ( 'NONE',  ( -2.328322743135000206, 31.00015586545000090, -0.2610490293201000456 ) ) ;
#16634=CARTESIAN_POINT ( 'NONE',  ( 2.093433345533683099, 29.77039470201872717, 0.5628675214677475447 ) ) ;
#16636=CARTESIAN_POINT ( 'NONE',  ( 1.585875242673999930, 25.49199905389999898, 1.504396160838000096 ) ) ;
#16638=CARTESIAN_POINT ( 'NONE',  ( -0.8685634062544059786, 23.64940451091839790, -1.966097736889167225 ) ) ;
#16641=CARTESIAN_POINT ( 'NONE',  ( 0.000000000000000000, 16.89999999999999858, -3.000000000000013323 ) ) ;
#16642=FACE_OUTER_BOUND ( 'NONE', #12786, .T. ) ;
#16646=VERTEX_POINT ( 'NONE', #15119 ) ;
#16649=CARTESIAN_POINT ( 'NONE',  ( -2.434931691670787934, 29.63333333333333286, 0.6543697108982051702 ) ) ;
#16653=ADVANCED_FACE ( 'NONE', ( #466 ), #11528, .F. ) ;
#16659=CARTESIAN_POINT ( 'NONE',  ( 1.994114618456069632, 26.41019129450748082, -1.176349860261615143 ) ) ;
#16662=CARTESIAN_POINT ( 'NONE',  ( 2.141160088383624149, 30.62055634019574057, -0.2848521897935961666 ) ) ;
#16664=CARTESIAN_POINT ( 'NONE',  ( 0.7923955384326393236, 26.27095271610905769, 2.035725376479952331 ) ) ;
#16667=CARTESIAN_POINT ( 'NONE',  ( 2.266239109532000029, 26.65021896306000215, -0.3134588398365999451 ) ) ;
#16673=CARTESIAN_POINT ( 'NONE',  ( 0.7185112213146519489, 28.67261440401754058, 2.100171626021731797 ) ) ;
#16674=ORIENTED_EDGE ( 'NONE', *, *, #19165, .T. ) ;
#16680=CARTESIAN_POINT ( 'NONE',  ( -2.196349052328999907, 29.40402464138999861, -0.8124029318252000698 ) ) ;
#16682=CARTESIAN_POINT ( 'NONE',  ( 0.5243867192824805956, 24.49999999999999645, 2.383703889157006373 ) ) ;
#16683=ORIENTED_EDGE ( 'NONE', *, *, #12170, .F. ) ;
#16689=CARTESIAN_POINT ( 'NONE',  ( -2.100000000000000089, 18.00000000000000000, 0.000000000000000000 ) ) ;
#16692=CARTESIAN_POINT ( 'NONE',  ( 1.930882614817647891, 29.06295433460837430, -0.9682181790307279323 ) ) ;
#16697=CARTESIAN_POINT ( 'NONE',  ( -0.6958892446922999575, 24.01090960993000323, 2.247974813822000151 ) ) ;
#16708=CARTESIAN_POINT ( 'NONE',  ( 1.645212785078999929, 25.60182591557000009, 1.375746322452999992 ) ) ;
#16713=CARTESIAN_POINT ( 'NONE',  ( -2.548054378949999865, 29.87161659520999990, -0.1605585572842999909 ) ) ;
#16716=FACE_OUTER_BOUND ( 'NONE', #13948, .T. ) ;
#16720=CARTESIAN_POINT ( 'NONE',  ( 1.167231323634179585, 23.98248082379630475, -2.207338634965280377 ) ) ;
#16724=CARTESIAN_POINT ( 'NONE',  ( 1.125885562883627733, 24.63699083177793625, 1.968842548519072366 ) ) ;
#16727=CARTESIAN_POINT ( 'NONE',  ( 1.206163983883000057, 25.72006359724000291, -2.153772461420000006 ) ) ;
#16729=ORIENTED_EDGE ( 'NONE', *, *, #21707, .F. ) ;
#16732=CARTESIAN_POINT ( 'NONE',  ( 1.500000000000000000, 8.900000000000000355, 0.000000000000000000 ) ) ;
#16740=ADVANCED_FACE ( 'NONE', ( #11604, #683 ), #8090, .T. ) ;
#16741=CARTESIAN_POINT ( 'NONE',  ( 1.435961984585999884, 29.47955444677999992, 1.657103211982000168 ) ) ;
#16743=CARTESIAN_POINT ( 'NONE',  ( 1.551074172888720959, 29.70570296557802337, 1.503492241676404717 ) ) ;
#16745=CARTESIAN_POINT ( 'NONE',  ( 1.552832420049000017, 24.32177879045000424, -1.744744256400999838 ) ) ;
#16766=CARTESIAN_POINT ( 'NONE',  ( 2.402140947178999647E-14, 29.00000000000000000, 2.500000000000000000 ) ) ;
#16769=CARTESIAN_POINT ( 'NONE',  ( 0.000000000000000000, 24.40000007355299871, 0.000000000000000000 ) ) ;
#16770=CARTESIAN_POINT ( 'NONE',  ( 0.5899383557787000187, 29.08750240009999999, 2.621867217767999581 ) ) ;
#16771=AXIS2_PLACEMENT_3D ( 'NONE', #22817, #4424, #15431 ) ;
#16772=CARTESIAN_POINT ( 'NONE',  ( -0.6694547791842193618, 30.36376599517464570, 2.053524939800617233 ) ) ;
#16773=ORIENTED_EDGE ( 'NONE', *, *, #7439, .T. ) ;
#16777=CARTESIAN_POINT ( 'NONE',  ( -1.488814495283000028, 27.47864211382000121, -1.743177805438000050 ) ) ;
#16779=AXIS2_PLACEMENT_3D ( 'NONE', #1481, #5578, #12958 ) ;
#16781=CARTESIAN_POINT ( 'NONE',  ( -2.500000000000000000, 27.19999999999999929, 0.000000000000000000 ) ) ;
#16783=VERTEX_POINT ( 'NONE', #16916 ) ;
#16792=ADVANCED_FACE ( 'NONE', ( #5785 ), #18860, .T. ) ;
#16794=CARTESIAN_POINT ( 'NONE',  ( 2.112683224871000132, 28.96769140845000123, -0.4028931246161000512 ) ) ;
#16799=CARTESIAN_POINT ( 'NONE',  ( -1.536366799937273875, 28.91666666666665719, 1.999167105995461213 ) ) ;
#16806=CARTESIAN_POINT ( 'NONE',  ( 1.964204535412830577, 29.05835064317297523, -0.8983286665718945851 ) ) ;
#16810=EDGE_CURVE ( 'NONE', #19347, #11582, #319, .T. ) ;
#16813=ORIENTED_EDGE ( 'NONE', *, *, #9479, .T. ) ;
#16814=CARTESIAN_POINT ( 'NONE',  ( -0.2682084311547999755, 25.15954001082000246, -2.144554451708999832 ) ) ;
#16816=CARTESIAN_POINT ( 'NONE',  ( -1.780325977227999790, 27.77549822781000088, 1.403495832404999977 ) ) ;
#16817=CARTESIAN_POINT ( 'NONE',  ( 0.000000000000000000, 20.00000000000000000, 0.000000000000000000 ) ) ;
#16820=DIRECTION ( 'NONE',  ( 1.000000000000000000, 0.000000000000000000, 0.000000000000000000 ) ) ;
#16821=( NAMED_UNIT ( * ) SI_UNIT ( $, .STERADIAN. ) SOLID_ANGLE_UNIT ( ) );
#16823=AXIS2_PLACEMENT_3D ( 'NONE', #11399, #22172, #15012 ) ;
#16828=CARTESIAN_POINT ( 'NONE',  ( 0.2699447682128000015, 24.59981568338000102, 2.319434643344000069 ) ) ;
#16833=CARTESIAN_POINT ( 'NONE',  ( -1.973994283211000011, 29.25896236979000165, 1.294426475701000001 ) ) ;
#16836=CARTESIAN_POINT ( 'NONE',  ( -2.500000000000000000, 26.63419673618999894, 0.000000000000000000 ) ) ;
#16842=DIRECTION ( 'NONE',  ( 0.000000000000000000, -1.000000000000000000, 0.000000000000000000 ) ) ;
#16846=CARTESIAN_POINT ( 'NONE',  ( 1.245756108708024223, 24.65778661989681098, 1.870434635796481393 ) ) ;
#16850=CARTESIAN_POINT ( 'NONE',  ( 2.157402177123000087, 25.41962896667000038, 1.099251314038999894 ) ) ;
#16853=CARTESIAN_POINT ( 'NONE',  ( -1.536366799937290084, 27.31753006952332896, -1.999167105995447669 ) ) ;
#16854=CARTESIAN_POINT ( 'NONE',  ( 0.000000000000000000, 24.50000000000000000, -4.618802153517000519 ) ) ;
#16863=CARTESIAN_POINT ( 'NONE',  ( -1.818533399173999809, 29.50782023400000043, 1.217198483556999999 ) ) ;
#16865=CARTESIAN_POINT ( 'NONE',  ( 1.865992796466994230, 29.73627313755168089, 1.093859238132237843 ) ) ;
#16867=CARTESIAN_POINT ( 'NONE',  ( -1.361207393629999984, 23.69359890096000143, -1.897971811607999992 ) ) ;
#16869=CARTESIAN_POINT ( 'NONE',  ( -4.749999920006001020, 24.30000007999099765, -4.227385599170000255E-08 ) ) ;
#16872=CONICAL_SURFACE ( 'NONE', #619, 1.449999902385000095, 0.7853981633972997312 ) ;
#16873=DIRECTION ( 'NONE',  ( 0.000000000000000000, 0.000000000000000000, -1.000000000000000000 ) ) ;
#16876=ORIENTED_EDGE ( 'NONE', *, *, #23708, .T. ) ;
#16882=CARTESIAN_POINT ( 'NONE',  ( -3.099999776787000005, 15.00000022320933013, -5.570936493763999179E-07 ) ) ;
#16884=VECTOR ( 'NONE', #2405, 1000.000000000000000 ) ;
#16886=ADVANCED_FACE ( 'NONE', ( #13639, #20558 ), #3972, .T. ) ;
#16890=DIRECTION ( 'NONE',  ( -0.5000000000000169864, 0.000000000000000000, 0.8660254037844289376 ) ) ;
#16891=CONICAL_SURFACE ( 'NONE', #7996, 4.649999883068000273, 0.7853981633972997312 ) ;
#16892=PRESENTATION_STYLE_ASSIGNMENT (( #418 ) ) ;
#16893=DIRECTION ( 'NONE',  ( 0.000000000000000000, 1.000000000000000000, 0.000000000000000000 ) ) ;
#16894=CARTESIAN_POINT ( 'NONE',  ( -0.6792780159082327796, 30.36314944672238170, 2.050295082915816192 ) ) ;
#16897=LINE ( 'NONE', #7222, #1153 ) ;
#16900=CARTESIAN_POINT ( 'NONE',  ( 0.04500887484489999452, 26.99114211382000050, 2.291988582794999729 ) ) ;
#16908=CARTESIAN_POINT ( 'NONE',  ( 0.000000000000000000, 15.00000000000000000, 0.000000000000000000 ) ) ;
#16909=B_SPLINE_CURVE_WITH_KNOTS ( 'NONE', 3,
 ( #22206, #5394, #16396, #18345 ),
 .UNSPECIFIED., .F., .F.,
 ( 4, 4 ),
 ( 0.000000000000000000, 1.000000000000000000 ),
 .UNSPECIFIED. ) ;
#16912=DIRECTION ( 'NONE',  ( 1.000000000000000000, 0.000000000000000000, 0.000000000000000000 ) ) ;
#16914=EDGE_CURVE ( 'NONE', #3216, #14758, #330, .T. ) ;
#16915=CARTESIAN_POINT ( 'NONE',  ( 0.000000000000000000, 18.00000000000000000, 0.000000000000000000 ) ) ;
#16916=CARTESIAN_POINT ( 'NONE',  ( -4.649999999999999467, 20.00000000000000000, 0.000000000000000000 ) ) ;
#16929=EDGE_CURVE ( 'NONE', #479, #1813, #3863, .T. ) ;
#16933=CARTESIAN_POINT ( 'NONE',  ( 0.000000000000000000, 7.049999902385000183, 0.000000000000000000 ) ) ;
#16937=CARTESIAN_POINT ( 'NONE',  ( -2.500000000000000000, 28.00000000000000000, 0.000000000000000000 ) ) ;
#16938=DIRECTION ( 'NONE',  ( 0.000000000000000000, 1.000000000000000000, 0.000000000000000000 ) ) ;
#16941=AXIS2_PLACEMENT_3D ( 'NONE', #5566, #18989, #9201 ) ;
#16947=DIRECTION ( 'NONE',  ( 0.000000000000000000, 1.000000000000000000, 0.000000000000000000 ) ) ;
#16950=EDGE_CURVE ( 'NONE', #20095, #6198, #9256, .T. ) ;
#16953=CARTESIAN_POINT ( 'NONE',  ( 2.275265428382999833, 24.62246328160999909, 1.096212662431000018 ) ) ;
#16959=CARTESIAN_POINT ( 'NONE',  ( 1.797218016695999898, 28.57905665442000043, 1.813427700862999981 ) ) ;
#16963=CARTESIAN_POINT ( 'NONE',  ( -2.500000000000000000, 29.83419673618999823, 0.000000000000000000 ) ) ;
#16967=ORIENTED_EDGE ( 'NONE', *, *, #7310, .T. ) ;
#16975=DIRECTION ( 'NONE',  ( 0.000000000000000000, -1.000000000000000000, 0.000000000000000000 ) ) ;
#16976=CARTESIAN_POINT ( 'NONE',  ( -2.030073792688000367, 26.58962896666999853, -1.733846816783999989 ) ) ;
#16978=VERTEX_POINT ( 'NONE', #16056 ) ;
#16981=AXIS2_PLACEMENT_3D ( 'NONE', #12834, #18185, #11136 ) ;
#16982=DIRECTION ( 'NONE',  ( -1.000000000000000000, 0.000000000000000000, 0.000000000000000000 ) ) ;
#16991=CARTESIAN_POINT ( 'NONE',  ( 2.100031370072000136, 29.55149146746000000, 0.6307504428255000795 ) ) ;
#16992=AXIS2_PLACEMENT_3D ( 'NONE', #14051, #4858, #19386 ) ;
#16994=CARTESIAN_POINT ( 'NONE',  ( 1.013493880231960853, 29.66610983716606498, 1.907327710277805233 ) ) ;
#16995=ORIENTED_EDGE ( 'NONE', *, *, #7908, .T. ) ;
#16996=CARTESIAN_POINT ( 'NONE',  ( 2.179541537902999870, 25.03809824813999896, -0.09213785550823000436 ) ) ;
#17002=DIRECTION ( 'NONE',  ( 0.000000000000000000, 0.000000000000000000, 1.000000000000000000 ) ) ;
#17003=AXIS2_PLACEMENT_3D ( 'NONE', #6243, #20667, #13512 ) ;
#17018=CARTESIAN_POINT ( 'NONE',  ( -2.500000000000000000, 29.03419673619000108, 0.000000000000000000 ) ) ;
#17021=CARTESIAN_POINT ( 'NONE',  ( 2.157679587390584963, 30.59770904888307541, 0.1054980346066700797 ) ) ;
#17022=EDGE_LOOP ( 'NONE', ( #911, #6725, #20465, #12755 ) ) ;
#17028=CARTESIAN_POINT ( 'NONE',  ( 0.5061648749513000256, 28.64946440326000143, 2.249552142899000184 ) ) ;
#17032=EDGE_CURVE ( 'NONE', #21355, #20086, #7308, .T. ) ;
#17034=FACE_OUTER_BOUND ( 'NONE', #14618, .T. ) ;
#17040=DIRECTION ( 'NONE',  ( 0.7071067811865462405, -0.7071067811865462405, 6.203608920934410591E-08 ) ) ;
#17046=FACE_OUTER_BOUND ( 'NONE', #760, .T. ) ;
#17049=CARTESIAN_POINT ( 'NONE',  ( 1.960438172910999866, 27.64956776952000084, -1.812210406530999851 ) ) ;
#17052=CARTESIAN_POINT ( 'NONE',  ( 1.663296876077221098, 28.91427789370213475, 1.406703391654695601 ) ) ;
#17055=LINE ( 'NONE', #4102, #6889 ) ;
#17057=CARTESIAN_POINT ( 'NONE',  ( -0.2163914088228000021, 23.55712358172999998, -2.044654028020000069 ) ) ;
#17059=CARTESIAN_POINT ( 'NONE',  ( -0.3106091461881000382, 27.87299822781000103, 2.245636445400999825 ) ) ;
#17069=CARTESIAN_POINT ( 'NONE',  ( 0.2919651418062000348, 24.49438105280999878, 2.508639337735000030 ) ) ;
#17072=FACE_OUTER_BOUND ( 'NONE', #17114, .T. ) ;
#17074=CARTESIAN_POINT ( 'NONE',  ( -0.3955362644989000587, 28.45937517842000020, 2.431766998741000219 ) ) ;
#17078=DIRECTION ( 'NONE',  ( -1.000000000000000000, 0.000000000000000000, 0.000000000000000000 ) ) ;
#17081=CARTESIAN_POINT ( 'NONE',  ( 0.000000000000000000, 18.50000000000000000, 0.000000000000000000 ) ) ;
#17082=VERTEX_POINT ( 'NONE', #13019 ) ;
#17085=CARTESIAN_POINT ( 'NONE',  ( -1.463919501975000204, 24.98815194586000032, 2.312767826279999994 ) ) ;
#17088=CARTESIAN_POINT ( 'NONE',  ( 1.336097305351384046, 24.08750628805587368, 1.739191107916495227 ) ) ;
#17091=EDGE_LOOP ( 'NONE', ( #19516, #9345, #10662, #22045 ) ) ;
#17094=CARTESIAN_POINT ( 'NONE',  ( -2.447990496630999768, 25.70419433610000226, -1.500144717171000064 ) ) ;
#17095=ORIENTED_EDGE ( 'NONE', *, *, #751, .F. ) ;
#17096=ORIENTED_EDGE ( 'NONE', *, *, #275, .T. ) ;
#17101=CARTESIAN_POINT ( 'NONE',  ( 0.000000000000000000, 15.00000000000000000, 0.000000000000000000 ) ) ;
#17108=EDGE_CURVE ( 'NONE', #5087, #13716, #13146, .T. ) ;
#17109=CARTESIAN_POINT ( 'NONE',  ( 2.133856304126000136, 29.00426108927999991, 0.4850359739721999963 ) ) ;
#17110=ADVANCED_FACE ( 'NONE', ( #2009 ), #6146, .F. ) ;
#17113=CARTESIAN_POINT ( 'NONE',  ( 1.254264882015703408, 29.68262165342926551, 1.758418893165299091 ) ) ;
#17114=EDGE_LOOP ( 'NONE', ( #7856, #9690, #2311 ) ) ;
#17115=CARTESIAN_POINT ( 'NONE',  ( -0.6595438615518000036, 25.38572581233000491, 2.254392134147999993 ) ) ;
#17117=ORIENTED_EDGE ( 'NONE', *, *, #10609, .T. ) ;
#17118=CARTESIAN_POINT ( 'NONE',  ( -1.147416861493836482, 24.56833304100603854, -2.035450680677415303 ) ) ;
#17121=EDGE_CURVE ( 'NONE', #2821, #19945, #19484, .T. ) ;
#17137=DIRECTION ( 'NONE',  ( -0.000000000000000000, 1.000000000000000000, 0.000000000000000000 ) ) ;
#17140=CARTESIAN_POINT ( 'NONE',  ( 1.029509027115623088, 30.46714375698348221, 1.899064101531559912 ) ) ;
#17141=VERTEX_POINT ( 'NONE', #13259 ) ;
#17147=CARTESIAN_POINT ( 'NONE',  ( -1.599833206071999969, 27.51196440325999859, -1.873164014766999896 ) ) ;
#17152=CARTESIAN_POINT ( 'NONE',  ( -4.000000000000000000, 24.80000000000000426, -2.309401076759000304 ) ) ;
#17153=CARTESIAN_POINT ( 'NONE',  ( 0.6140746919655077907, 27.86542664715151574, 2.111358184564343432 ) ) ;
#17159=DIRECTION ( 'NONE',  ( -1.877655957117991099E-08, -0.9999999999999978906, 6.187284373139976848E-08 ) ) ;
#17162=CARTESIAN_POINT ( 'NONE',  ( -1.732016619652910761, 30.87844438891047005, -1.225611771103511494 ) ) ;
#17166=ORIENTED_EDGE ( 'NONE', *, *, #20638, .F. ) ;
#17168=DIRECTION ( 'NONE',  ( -1.127782589537999921E-10, -1.517608444995555245E-19, 1.000000000000000000 ) ) ;
#17169=CARTESIAN_POINT ( 'NONE',  ( 1.887779699469000150, 27.45456776952000411, 1.887779699469000150 ) ) ;
#17171=CARTESIAN_POINT ( 'NONE',  ( 2.154139288595608104, 29.01452026705025133, -0.1796810215235566943 ) ) ;
#17173=ORIENTED_EDGE ( 'NONE', *, *, #19488, .T. ) ;
#17174=CARTESIAN_POINT ( 'NONE',  ( -4.000000000000000000, 24.80000000000000426, -2.309401076759000304 ) ) ;
#17187=ORIENTED_EDGE ( 'NONE', *, *, #7194, .F. ) ;
#17188=CARTESIAN_POINT ( 'NONE',  ( 2.613167118632000019, 25.39225721452000073, -0.3773460266549999442 ) ) ;
#17194=CARTESIAN_POINT ( 'NONE',  ( 2.618739119015000227, 29.33532865103999754, 0.8251606127257998802 ) ) ;
#17198=DIRECTION ( 'NONE',  ( 0.000000000000000000, 1.000000000000000000, 0.000000000000000000 ) ) ;
#17199=DIRECTION ( 'NONE',  ( 0.000000000000000000, -1.000000000000000000, 0.000000000000000000 ) ) ;
#17202=FACE_OUTER_BOUND ( 'NONE', #7017, .T. ) ;
#17208=VECTOR ( 'NONE', #22409, 1000.000000000000000 ) ;
#17210=CARTESIAN_POINT ( 'NONE',  ( 2.402140947178999647E-14, 29.00000000000000000, 2.500000000000000000 ) ) ;
#17212=CARTESIAN_POINT ( 'NONE',  ( 2.320116128650000054, 25.31419433610000169, 1.182158213329999930 ) ) ;
#17217=DIRECTION ( 'NONE',  ( 1.000000000000000000, 0.000000000000000000, 0.000000000000000000 ) ) ;
#17218=EDGE_LOOP ( 'NONE', ( #12909, #2194, #7917 ) ) ;
#17223=CARTESIAN_POINT ( 'NONE',  ( 2.205132044672000191, 30.37612098430000174, 0.8301523867869999851 ) ) ;
#17226=AXIS2_PLACEMENT_3D ( 'NONE', #16568, #13053, #14861 ) ;
#17228=CARTESIAN_POINT ( 'NONE',  ( 0.4599695686195089950, 29.63102501646989850, 2.110344102147514445 ) ) ;
#17230=CARTESIAN_POINT ( 'NONE',  ( -2.199644512527999751, 25.17633251583999865, -0.8239167990765999816 ) ) ;
#17232=ORIENTED_EDGE ( 'NONE', *, *, #882, .T. ) ;
#17233=CARTESIAN_POINT ( 'NONE',  ( -1.235289751754999887, 30.50000000000000000, -2.173490103315000255 ) ) ;
#17234=CARTESIAN_POINT ( 'NONE',  ( -2.122520971047507921, 30.87747901625595759, 0.04286016723165855802 ) ) ;
#17241=CIRCLE ( 'NONE', #23043, 1.899912543625999373 ) ;
#17248=CARTESIAN_POINT ( 'NONE',  ( 4.000000000000000000, 26.39685207198629158, -1.322601766568779924 ) ) ;
#17249=DIRECTION ( 'NONE',  ( 0.000000000000000000, -1.000000000000000000, 0.000000000000000000 ) ) ;
#17256=ADVANCED_FACE ( 'NONE', ( #17072 ), #15809, .T. ) ;
#17258=DIRECTION ( 'NONE',  ( 3.842525697690999187E-09, -0.9999999999999998890, -1.654014142263999949E-08 ) ) ;
#17259=CARTESIAN_POINT ( 'NONE',  ( 1.999167105995449445, 28.71753006952332754, -1.536366799937288530 ) ) ;
#17261=CARTESIAN_POINT ( 'NONE',  ( 2.103635563519576035, 30.57149230880223811, 0.5442943234456341095 ) ) ;
#17262=ORIENTED_EDGE ( 'NONE', *, *, #5517, .T. ) ;
#17269=CARTESIAN_POINT ( 'NONE',  ( 0.1450207862197000208, 27.41446440326000200, -2.459101194521000178 ) ) ;
#17270=CARTESIAN_POINT ( 'NONE',  ( -3.653528746112522541, 24.70780860099737453, -2.509315635920815524 ) ) ;
#17271=ORIENTED_EDGE ( 'NONE', *, *, #11060, .F. ) ;
#17273=DIRECTION ( 'NONE',  ( 0.000000000000000000, -1.000000000000000000, 0.000000000000000000 ) ) ;
#17274=CIRCLE ( 'NONE', #10320, 2.899999999999999911 ) ;
#17275=CARTESIAN_POINT ( 'NONE',  ( -0.7113715763943910808, 28.27224425180803280, -2.049892269754120200 ) ) ;
#17276=CIRCLE ( 'NONE', #20004, 4.549999999999999822 ) ;
#17278=ORIENTED_EDGE ( 'NONE', *, *, #3445, .F. ) ;
#17290=DIRECTION ( 'NONE',  ( 0.000000000000000000, -1.000000000000000000, 0.000000000000000000 ) ) ;
#17291=CARTESIAN_POINT ( 'NONE',  ( 0.5289967318967999654, 28.42163313894999987, -2.411020654974999733 ) ) ;
#17292=CONICAL_SURFACE ( 'NONE', #2598, 4.699999872533999756, 0.7853981633972997312 ) ;
#17301=CARTESIAN_POINT ( 'NONE',  ( -1.600000000000000089, 8.900000000000000355, 1.856656273168999865E-09 ) ) ;
#17308=CARTESIAN_POINT ( 'NONE',  ( -2.499999999999999556, 27.21666666666666146, 0.3272492347489423525 ) ) ;
#17309=VERTEX_POINT ( 'NONE', #7992 ) ;
#17311=CARTESIAN_POINT ( 'NONE',  ( -2.231919210383000340, 23.57515785297000122, -0.1739934626373000059 ) ) ;
#17316=CARTESIAN_POINT ( 'NONE',  ( -1.217060697036999928, 28.83266645185000243, -2.461188343967999792 ) ) ;
#17320=DIRECTION ( 'NONE',  ( 0.000000000000000000, -1.000000000000000000, 0.000000000000000000 ) ) ;
#17325=B_SPLINE_SURFACE_WITH_KNOTS ( 'NONE', 3, 3, ( 
 ( #603, #21209, #8375, #8004, #4624, #19395, #18907, #15379, #2808, #10190, #22533, #5939, #13325, #20724, #4130, #2315, #9703, #17085, #484, #7886, #6789, #1471, #14308, #16236, #4747, #4993, #10312, #6915, #8739, #21701, #4868, #12381, #14060, #3294, #1349 ),
 ( #19996, #3416, #8616, #12493, #16102, #2928, #12132, #7033, #1101, #8501, #23626, #10558, #21453, #21811, #6667, #5226, #3054, #21581, #3176, #12257, #23504, #10441, #19878, #5111, #10676, #12609, #19520, #10799, #15864, #18192, #17704, #1593, #23254, #17830, #1225 ),
 ( #15741, #14184, #14418, #23128, #6553, #13938, #15978, #19766, #21332, #23372, #7378, #106, #3751, #1935, #7615, #11022, #20343, #8250, #12946, #18644, #11140, #14760, #18526, #2050, #14650, #1817, #9323, #7493, #16697, #9203, #11383, #22158, #14878, #22264, #11267 ),
 ( #20232, #3874, #5569, #18754, #5803, #5681, #13067, #1698, #20466, #9441, #16814, #22390, #219, #14992, #20576, #18405, #13185, #3988, #8975, #16348, #23736, #14532, #21926, #16458, #22046, #5338, #12726, #20121, #3529, #18296, #9087, #23849, #5455, #7741, #17057 ) ),
 .UNSPECIFIED., .F., .F., .F.,
 ( 4, 4 ),
 ( 4, 1, 1, 1, 1, 1, 1, 1, 1, 1, 1, 1, 1, 1, 1, 1, 1, 1, 1, 1, 1, 1, 1, 1, 1, 1, 1, 1, 1, 1, 1, 1, 4 ),
 ( -0.3056682515952000023, 1.305668251594999996 ),
 ( -0.01429133938984000068, 0.008932087118648001159, 0.03215551362712999739, 0.05537894013562000284, 0.07860236664410000240, 0.1018257931525999999, 0.1250492196610999973, 0.1482726461695999809, 0.1714960726779999889, 0.1947194991865000002, 0.2179429256950000116, 0.2411663522034999951, 0.2643897787120000342, 0.2876132052204999900, 0.3108366317290000014, 0.3340600582373999816, 0.3572834847458999930, 0.3805069112544000043, 0.4037303377629000156, 0.4269537642714000270, 0.4501771907798999828, 0.4734006172883000185, 0.4966240437968000299, 0.5198474703052999857, 0.5430708968138000525, 0.5662943233223000083, 0.5895177498307999642, 0.6127411763393000310, 0.6359646028477000668, 0.6591880293561999116, 0.6824114558646999784, 0.7056348823732000453, 0.7288583088817000011 ),
 .UNSPECIFIED. ) ;
#17328=CARTESIAN_POINT ( 'NONE',  ( -2.061627795661847617, 24.55982949481376920, -0.7474695682632446214 ) ) ;
#17329=CARTESIAN_POINT ( 'NONE',  ( -4.000000000000000000, 26.20000000000000284, 2.309401076759000304 ) ) ;
#17333=CARTESIAN_POINT ( 'NONE',  ( 2.108296854627000005, 27.06919433610000070, -1.948889566018999986 ) ) ;
#17338=AXIS2_PLACEMENT_3D ( 'NONE', #22687, #10107, #15786 ) ;
#17339=CARTESIAN_POINT ( 'NONE',  ( -2.399999988616999591, 24.50000001138332806, -6.337991255853999810E-08 ) ) ;
#17341=VERTEX_POINT ( 'NONE', #23241 ) ;
#17343=DIRECTION ( 'NONE',  ( 1.000000000000000000, 0.000000000000000000, 0.000000000000000000 ) ) ;
#17346=CONICAL_SURFACE ( 'NONE', #11215, 3.049999825846000157, 0.7853981633972997312 ) ;
#17350=CARTESIAN_POINT ( 'NONE',  ( 0.000000000000000000, 22.19999999999999574, -2.749999999999999556 ) ) ;
#17351=ADVANCED_FACE ( 'NONE', ( #8360 ), #8892, .T. ) ;
#17352=CARTESIAN_POINT ( 'NONE',  ( -0.9793716477997560510, 29.54380556444507633, 1.925535291027464346 ) ) ;
#17354=CARTESIAN_POINT ( 'NONE',  ( -0.8474553701696999619, 24.26896156435000051, -2.190683491321000265 ) ) ;
#17355=CIRCLE ( 'NONE', #9236, 2.100000000000000089 ) ;
#17357=AXIS2_PLACEMENT_3D ( 'NONE', #9894, #11365, #7594 ) ;
#17361=CARTESIAN_POINT ( 'NONE',  ( -2.134263429621519048, 30.85404986398537019, 0.2236583631314258136 ) ) ;
#17362=AXIS2_PLACEMENT_3D ( 'NONE', #15614, #11522, #22641 ) ;
#17364=EDGE_CURVE ( 'NONE', #8845, #17082, #16221, .T. ) ;
#17372=CARTESIAN_POINT ( 'NONE',  ( -2.090639349808711689, 24.68204389809848109, 0.7662985136386953888 ) ) ;
#17378=AXIS2_PLACEMENT_3D ( 'NONE', #17692, #963, #1215 ) ;
#17385=CARTESIAN_POINT ( 'NONE',  ( 0.3272492347489341924, 28.81753006952333251, -2.500000000000000888 ) ) ;
#17386=CARTESIAN_POINT ( 'NONE',  ( 0.000000000000000000, 19.00000000000000000, 0.000000000000000000 ) ) ;
#17387=ADVANCED_FACE ( 'NONE', ( #14170 ), #348, .T. ) ;
#17388=CARTESIAN_POINT ( 'NONE',  ( -1.378834737919759856, 30.31601879608736638, 1.669154270543806051 ) ) ;
#17390=EDGE_CURVE ( 'NONE', #11075, #23046, #13121, .T. ) ;
#17395=CIRCLE ( 'NONE', #6954, 2.949999999999999734 ) ;
#17398=CONICAL_SURFACE ( 'NONE', #3447, 2.249999993254999886, 0.7853981633972997312 ) ;
#17399=B_SPLINE_CURVE_WITH_KNOTS ( 'NONE', 3,
 ( #761, #22916, #17610, #21241 ),
 .UNSPECIFIED., .F., .F.,
 ( 4, 4 ),
 ( 0.000000000000000000, 1.000000000000000000 ),
 .UNSPECIFIED. ) ;
#17404=DIRECTION ( 'NONE',  ( -0.7071067811867999264, 0.7071067811862000729, 3.665336534966999651E-07 ) ) ;
#17405=CARTESIAN_POINT ( 'NONE',  ( -1.676242427568033211, 27.71749297273097312, 1.380892551129798251 ) ) ;
#17415=CARTESIAN_POINT ( 'NONE',  ( -3.999999999999999112, 26.29977277844471573, -1.897803675662255385 ) ) ;
#17416=CARTESIAN_POINT ( 'NONE',  ( 2.402140947178999647E-14, 29.00000000000000000, 2.500000000000000000 ) ) ;
#17418=B_SPLINE_CURVE_WITH_KNOTS ( 'NONE', 3,
 ( #15937, #3008, #21295, #23332, #21408, #1184, #18023, #1307, #23456, #16184 ),
 .UNSPECIFIED., .F., .F.,
 ( 4, 1, 1, 2, 2, 4 ),
 ( 0.000000000000000000, 0.2500000000000001665, 0.3750000000000001665, 0.4375000000000000555, 0.4999999999999999445, 1.000000000000000000 ),
 .UNSPECIFIED. ) ;
#17419=DIRECTION ( 'NONE',  ( 0.000000000000000000, 1.000000000000000000, 0.000000000000000000 ) ) ;
#17420=ORIENTED_EDGE ( 'NONE', *, *, #18394, .F. ) ;
#17422=CARTESIAN_POINT ( 'NONE',  ( 1.016344414748000080, 28.90913313895000059, 1.994688225595000253 ) ) ;
#17424=CARTESIAN_POINT ( 'NONE',  ( 2.059625858907598417, 28.96477123800895725, 0.6504964593587068133 ) ) ;
#17430=EDGE_CURVE ( 'NONE', #20723, #9936, #13511, .T. ) ;
#17437=ORIENTED_EDGE ( 'NONE', *, *, #12545, .T. ) ;
#17442=AXIS2_PLACEMENT_3D ( 'NONE', #20233, #20577, #3637 ) ;
#17446=DIRECTION ( 'NONE',  ( -1.000000000000000000, 0.000000000000000000, 0.000000000000000000 ) ) ;
#17450=DIRECTION ( 'NONE',  ( 0.000000000000000000, 1.000000000000000000, 0.000000000000000000 ) ) ;
#17451=CARTESIAN_POINT ( 'NONE',  ( 2.184465970885644648, 29.50086340285666964, -1.259047450927249345 ) ) ;
#17456=DIRECTION ( 'NONE',  ( 0.000000000000000000, 1.000000000000000000, 0.000000000000000000 ) ) ;
#17457=CARTESIAN_POINT ( 'NONE',  ( 1.536366799937304295, 28.51753006952333536, 1.999167105995438121 ) ) ;
#17462=CARTESIAN_POINT ( 'NONE',  ( -0.2814148094397999622, 26.38669433609999970, -2.857252503208999705 ) ) ;
#17468=ADVANCED_FACE ( 'NONE', ( #14295 ), #21320, .F. ) ;
#17469=ORIENTED_EDGE ( 'NONE', *, *, #17841, .F. ) ;
#17470=CARTESIAN_POINT ( 'NONE',  ( 0.000000000000000000, 13.00000000000000000, 0.000000000000000000 ) ) ;
#17474=CARTESIAN_POINT ( 'NONE',  ( -0.9520732478256999087, 29.36900269487000159, 2.155299678714000411 ) ) ;
#17477=AXIS2_PLACEMENT_3D ( 'NONE', #18477, #7442, #22216 ) ;
#17478=CARTESIAN_POINT ( 'NONE',  ( -1.202564115966959557, 29.52878198405490906, 1.797833957355160717 ) ) ;
#17480=CARTESIAN_POINT ( 'NONE',  ( -2.306707304653000001, 25.24613028134000103, 0.4431434081515999712 ) ) ;
#17482=B_SPLINE_CURVE_WITH_KNOTS ( 'NONE', 3,
 ( #16423, #14498, #11104, #18152, #18026, #20082, #8940, #9290, #16664, #70 ),
 .UNSPECIFIED., .F., .F.,
 ( 4, 2, 2, 2, 4 ),
 ( 4.238274817591080088E-05, 0.0007680267671880953821, 0.001493670786200280119, 0.002219314805212464423, 0.002944958824224649160 ),
 .UNSPECIFIED. ) ;
#17488=CARTESIAN_POINT ( 'NONE',  ( 0.000000000000000000, 21.87500000000000000, 0.000000000000000000 ) ) ;
#17491=CARTESIAN_POINT ( 'NONE',  ( -1.999167105995452998, 27.11666666666667425, -1.536366799937284089 ) ) ;
#17493=EDGE_CURVE ( 'NONE', #14758, #14191, #8727, .T. ) ;
#17494=EDGE_LOOP ( 'NONE', ( #14093, #1947, #17262 ) ) ;
#17508=ADVANCED_FACE ( 'NONE', ( #19865 ), #961, .T. ) ;
#17509=CARTESIAN_POINT ( 'NONE',  ( -1.706528196843968725, 30.28866702718950776, 1.336746582747178502 ) ) ;
#17513=CARTESIAN_POINT ( 'NONE',  ( -2.184465970885641983, 27.50086340285666608, 1.259047450927253564 ) ) ;
#17514=CARTESIAN_POINT ( 'NONE',  ( 1.526275108040723971, 24.72983374295983339, 1.538304002670136894 ) ) ;
#17515=CARTESIAN_POINT ( 'NONE',  ( 0.000000000000000000, 20.10000000000000142, -3.000000000000416112 ) ) ;
#17522=CARTESIAN_POINT ( 'NONE',  ( -0.6943634456196157156, 27.47093684869671293, -2.086060929983299950 ) ) ;
#17524=ORIENTED_EDGE ( 'NONE', *, *, #23005, .T. ) ;
#17531=CARTESIAN_POINT ( 'NONE',  ( -0.6838519464012248195, 24.63336607546796841, 4.223839491855484241 ) ) ;
#17535=EDGE_CURVE ( 'NONE', #9272, #10321, #17418, .T. ) ;
#17539=CARTESIAN_POINT ( 'NONE',  ( -2.866097959738999723, 27.26750240009999970, 0.1690226414555000001 ) ) ;
#17546=CARTESIAN_POINT ( 'NONE',  ( 0.000000000000000000, 17.00000000000000000, 0.000000000000000000 ) ) ;
#17553=LINE ( 'NONE', #8347, #5961 ) ;
#17556=CARTESIAN_POINT ( 'NONE',  ( -1.999167105995447224, 27.28333333333333499, 1.536366799937292305 ) ) ;
#17561=CARTESIAN_POINT ( 'NONE',  ( -0.2155490653164000014, 30.96541312239999755, -2.523581531315999715 ) ) ;
#17567=CARTESIAN_POINT ( 'NONE',  ( -2.740231804698999962, 29.76618196464000121, -0.1726680830762000185 ) ) ;
#17569=DIRECTION ( 'NONE',  ( -0.000000000000000000, 1.000000000000000000, 0.000000000000000000 ) ) ;
#17575=DIRECTION ( 'NONE',  ( 0.000000000000000000, -1.000000000000000000, 0.000000000000000000 ) ) ;
#17576=ORIENTED_EDGE ( 'NONE', *, *, #23915, .T. ) ;
#17578=CARTESIAN_POINT ( 'NONE',  ( 1.768240990936880142, 24.49990546444021078, -1.767061324597003713 ) ) ;
#17579=ORIENTED_EDGE ( 'NONE', *, *, #3143, .F. ) ;
#17581=CARTESIAN_POINT ( 'NONE',  ( 2.079313456931997539, 24.24494735708400839, -0.6989243223293186702 ) ) ;
#17587=ORIENTED_EDGE ( 'NONE', *, *, #9534, .F. ) ;
#17589=CONICAL_SURFACE ( 'NONE', #23380, 2.949999959913000236, 0.7853981633972997312 ) ;
#17590=CARTESIAN_POINT ( 'NONE',  ( 0.000000000000000000, 18.27087121525220681, 0.000000000000000000 ) ) ;
#17595=CARTESIAN_POINT ( 'NONE',  ( -2.246347731941017223, 24.65365226805931087, -5.222125272214524731E-08 ) ) ;
#17596=PLANE ( 'NONE',  #4884 ) ;
#17598=( GEOMETRIC_REPRESENTATION_CONTEXT ( 3 ) GLOBAL_UNCERTAINTY_ASSIGNED_CONTEXT ( ( #3395 ) ) GLOBAL_UNIT_ASSIGNED_CONTEXT ( ( #4305, #11695, #7817 ) ) REPRESENTATION_CONTEXT ( 'NONE', 'WORKASPACE' ) );
#17603=FACE_BOUND ( 'NONE', #9613, .T. ) ;
#17604=CARTESIAN_POINT ( 'NONE',  ( -2.160954628185623783, 29.42171253127930797, 0.3064887866906846892 ) ) ;
#17605=ORIENTED_EDGE ( 'NONE', *, *, #9381, .F. ) ;
#17606=CARTESIAN_POINT ( 'NONE',  ( 2.346791958811000001, 24.82734368833999739, -0.09920819339686001714 ) ) ;
#17608=B_SPLINE_CURVE_WITH_KNOTS ( 'NONE', 3,
 ( #11985, #12107, #13545, #22863 ),
 .UNSPECIFIED., .F., .F.,
 ( 4, 4 ),
 ( 0.8463849510497769568, 1.000000000000000000 ),
 .UNSPECIFIED. ) ;
#17609=ORIENTED_EDGE ( 'NONE', *, *, #19165, .F. ) ;
#17610=CARTESIAN_POINT ( 'NONE',  ( -3.574277709506242531E-06, 28.66502397170827621, 2.098898342233183723 ) ) ;
#17624=CARTESIAN_POINT ( 'NONE',  ( -3.304996520289660733, 26.37418302490023692, 2.710661522857508388 ) ) ;
#17631=CARTESIAN_POINT ( 'NONE',  ( -2.140916772114409117, 30.22093133680311183, 0.2897247076014631273 ) ) ;
#17632=ORIENTED_EDGE ( 'NONE', *, *, #22973, .T. ) ;
#17635=CARTESIAN_POINT ( 'NONE',  ( -1.259047450927242018, 27.56753006952333607, 2.184465970885648201 ) ) ;
#17637=CARTESIAN_POINT ( 'NONE',  ( -2.135131282218049265, 24.38894026383828972, -0.7200268973484618140 ) ) ;
#17642=CARTESIAN_POINT ( 'NONE',  ( -4.000000000000000000, 24.50000000000000000, 0.000000000000000000 ) ) ;
#17647=ORIENTED_EDGE ( 'NONE', *, *, #9923, .T. ) ;
#17654=CARTESIAN_POINT ( 'NONE',  ( 0.8375244288382391877, 28.35398498632677189, -2.004067736020587187 ) ) ;
#17662=CARTESIAN_POINT ( 'NONE',  ( 0.1921407682535675732, 24.77615385734275932, 2.130435955740220155 ) ) ;
#17665=CARTESIAN_POINT ( 'NONE',  ( 1.798742361870000028, 27.50937716035999969, -1.662740336262000129 ) ) ;
#17666=AXIS2_PLACEMENT_3D ( 'NONE', #13872, #2862, #19818 ) ;
#17667=CARTESIAN_POINT ( 'NONE',  ( 0.000000000000000000, 24.65000000000000213, 0.000000000000000000 ) ) ;
#17668=ORIENTED_EDGE ( 'NONE', *, *, #7146, .T. ) ;
#17673=CARTESIAN_POINT ( 'NONE',  ( 0.1325762199310360212, 30.23768260327807411, 2.274129417085968718 ) ) ;
#17675=EDGE_CURVE ( 'NONE', #15250, #3998, #13898, .T. ) ;
#17680=ORIENTED_EDGE ( 'NONE', *, *, #20310, .F. ) ;
#17682=CARTESIAN_POINT ( 'NONE',  ( 1.375673147160000109, 30.52907988946000017, 1.895117694842000100 ) ) ;
#17683=AXIS2_PLACEMENT_3D ( 'NONE', #10322, #3301, #21221 ) ;
#17687=CIRCLE ( 'NONE', #13795, 3.000000000000000000 ) ;
#17688=EDGE_CURVE ( 'NONE', #19360, #16087, #6164, .T. ) ;
#17691=CARTESIAN_POINT ( 'NONE',  ( 0.000000000000000000, 18.50000000000000000, 0.000000000000000000 ) ) ;
#17692=CARTESIAN_POINT ( 'NONE',  ( 0.000000000000000000, -1.550000000000000044, 0.000000000000000000 ) ) ;
#17694=AXIS2_PLACEMENT_3D ( 'NONE', #10825, #1250, #6816 ) ;
#17696=DIRECTION ( 'NONE',  ( 1.000000000000000000, 0.000000000000000000, 0.000000000000000000 ) ) ;
#17704=CARTESIAN_POINT ( 'NONE',  ( -2.505762909214999556, 23.97700368146000116, 0.4461716537489999745 ) ) ;
#17707=VECTOR ( 'NONE', #20435, 1000.000000000000000 ) ;
#17713=EDGE_CURVE ( 'NONE', #8845, #5602, #15828, .T. ) ;
#17715=CARTESIAN_POINT ( 'NONE',  ( 3.653528746108709147, 24.70780860099632292, 2.509315635922550580 ) ) ;
#17716=DIRECTION ( 'NONE',  ( 0.000000000000000000, 0.000000000000000000, -1.000000000000000000 ) ) ;
#17717=ORIENTED_EDGE ( 'NONE', *, *, #3051, .T. ) ;
#17723=LINE ( 'NONE', #20984, #12255 ) ;
#17727=CIRCLE ( 'NONE', #21969, 0.5500000000000001554 ) ;
#17728=CARTESIAN_POINT ( 'NONE',  ( -1.957297221654172192, 29.45966400265699292, 0.9176472163504577617 ) ) ;
#17729=ORIENTED_EDGE ( 'NONE', *, *, #22848, .F. ) ;
#17730=B_SPLINE_CURVE_WITH_KNOTS ( 'NONE', 3,
 ( #13573, #20967, #11767, #9942 ),
 .UNSPECIFIED., .F., .F.,
 ( 4, 4 ),
 ( 0.000000000000000000, 1.000000000000000000 ),
 .UNSPECIFIED. ) ;
#17731=CARTESIAN_POINT ( 'NONE',  ( -0.5723425338777000659, 23.45465430019000053, -2.197853533198000253 ) ) ;
#17733=EDGE_LOOP ( 'NONE', ( #22310, #2756, #3871 ) ) ;
#17734=AXIS2_PLACEMENT_3D ( 'NONE', #22877, #17446, #1090 ) ;
#17739=EDGE_CURVE ( 'NONE', #7057, #23948, #5416, .T. ) ;
#17741=DIRECTION ( 'NONE',  ( -0.7071067811865975328, 0.000000000000000000, 0.7071067811864976127 ) ) ;
#17743=CARTESIAN_POINT ( 'NONE',  ( -0.6836813991252411737, 24.62756664670458662, -4.224074002601207134 ) ) ;
#17747=CARTESIAN_POINT ( 'NONE',  ( 0.000000000000000000, 15.00000000000000000, 0.000000000000000000 ) ) ;
#17753=AXIS2_PLACEMENT_3D ( 'NONE', #4709, #12094, #8696 ) ;
#17756=CARTESIAN_POINT ( 'NONE',  ( -1.422584979458079157, 30.09537825555706547, -1.627545391958989507 ) ) ;
#17757=ORIENTED_EDGE ( 'NONE', *, *, #12143, .T. ) ;
#17758=CARTESIAN_POINT ( 'NONE',  ( 2.230746854092000131, 25.83406370960000231, -0.3522458802031000480 ) ) ;
#17762=ORIENTED_EDGE ( 'NONE', *, *, #5783, .F. ) ;
#17767=AXIS2_PLACEMENT_3D ( 'NONE', #22138, #14514, #1917 ) ;
#17772=CARTESIAN_POINT ( 'NONE',  ( 1.486729910992351078, 27.12575827504875647, 1.582850948029659088 ) ) ;
#17774=LINE ( 'NONE', #6501, #20644 ) ;
#17775=ORIENTED_EDGE ( 'NONE', *, *, #14592, .F. ) ;
#17777=VECTOR ( 'NONE', #17575, 1000.000000000000000 ) ;
#17786=CIRCLE ( 'NONE', #10049, 4.000000000000000000 ) ;
#17788=ORIENTED_EDGE ( 'NONE', *, *, #18144, .F. ) ;
#17791=CARTESIAN_POINT ( 'NONE',  ( -0.5724186824819998964, 25.97619850838000133, -2.193530619437999984 ) ) ;
#17792=VECTOR ( 'NONE', #4744, 1000.000000000000000 ) ;
#17797=CARTESIAN_POINT ( 'NONE',  ( 1.008585698963999855, 28.87437716036000168, 1.979460888490000015 ) ) ;
#17800=CARTESIAN_POINT ( 'NONE',  ( 1.399999999999999911, 7.000000000000000000, 0.000000000000000000 ) ) ;
#17802=DIRECTION ( 'NONE',  ( 0.000000000000000000, 1.000000000000000000, 0.000000000000000000 ) ) ;
#17805=CARTESIAN_POINT ( 'NONE',  ( -2.197444295422539717, 30.81144470851556960, -0.03941198171681850604 ) ) ;
#17806=CARTESIAN_POINT ( 'NONE',  ( -2.500000000000000000, 29.83419673618999823, 0.000000000000000000 ) ) ;
#17808=CARTESIAN_POINT ( 'NONE',  ( -2.434931691670787934, 27.23333333333334139, 0.6543697108982051702 ) ) ;
#17810=ORIENTED_EDGE ( 'NONE', *, *, #16225, .F. ) ;
#17811=CARTESIAN_POINT ( 'NONE',  ( -2.184465970885646424, 28.73333333333333428, -1.259047450927245126 ) ) ;
#17812=CARTESIAN_POINT ( 'NONE',  ( 0.8513612441708000578, 29.31092011053999968, -2.385437969772000066 ) ) ;
#17815=AXIS2_PLACEMENT_3D ( 'NONE', #7449, #13147, #16890 ) ;
#17816=ORIENTED_EDGE ( 'NONE', *, *, #21535, .T. ) ;
#17819=FACE_OUTER_BOUND ( 'NONE', #9376, .T. ) ;
#17820=PLANE ( 'NONE',  #2296 ) ;
#17824=ADVANCED_FACE ( 'NONE', ( #12567 ), #4374, .F. ) ;
#17825=CARTESIAN_POINT ( 'NONE',  ( -2.750000000000000000, 24.29999999999999716, 0.000000000000000000 ) ) ;
#17826=ORIENTED_EDGE ( 'NONE', *, *, #14448, .T. ) ;
#17827=DIRECTION ( 'NONE',  ( 0.000000000000000000, 0.000000000000000000, 1.000000000000000000 ) ) ;
#17830=CARTESIAN_POINT ( 'NONE',  ( -0.6940159635513000191, 23.79121626938999867, -2.361381702958999629 ) ) ;
#17831=DIRECTION ( 'NONE',  ( 1.000000000000000000, 0.000000000000000000, 0.000000000000000000 ) ) ;
#17835=EDGE_CURVE ( 'NONE', #20342, #5650, #10808, .T. ) ;
#17837=ORIENTED_EDGE ( 'NONE', *, *, #18558, .T. ) ;
#17839=CARTESIAN_POINT ( 'NONE',  ( -1.937289889703149859, 26.22758819317520818, 0.8800478335377882599 ) ) ;
#17841=EDGE_CURVE ( 'NONE', #5021, #6219, #5643, .T. ) ;
#17842=ORIENTED_EDGE ( 'NONE', *, *, #8643, .F. ) ;
#17847=CARTESIAN_POINT ( 'NONE',  ( 3.999996093285163035, 24.62756664670878948, 1.519951541579177778 ) ) ;
#17851=ORIENTED_EDGE ( 'NONE', *, *, #14592, .T. ) ;
#17853=CARTESIAN_POINT ( 'NONE',  ( -2.009380400686512580, 29.45175883193518374, 0.7931520617424835384 ) ) ;
#17854=EDGE_CURVE ( 'NONE', #7466, #14519, #16897, .T. ) ;
#17865=DIRECTION ( 'NONE',  ( 0.000000000000000000, 1.000000000000000000, 0.000000000000000000 ) ) ;
#17870=DIRECTION ( 'NONE',  ( 0.000000000000000000, 0.000000000000000000, -1.000000000000000000 ) ) ;
#17876=CARTESIAN_POINT ( 'NONE',  ( 1.182434930542718865, 26.44682129341587284, 3.936123028068912344 ) ) ;
#17877=CARTESIAN_POINT ( 'NONE',  ( -1.904442799929577879, 30.26744504660184631, 1.036340829782300688 ) ) ;
#17878=EDGE_CURVE ( 'NONE', #10966, #14748, #9273, .T. ) ;
#17888=ORIENTED_EDGE ( 'NONE', *, *, #4812, .F. ) ;
#17896=CARTESIAN_POINT ( 'NONE',  ( 2.500000000000003109, 26.77499936725412866, 0.4908862760595652519 ) ) ;
#17902=CARTESIAN_POINT ( 'NONE',  ( -2.132962310478440315, 27.02892739381266907, 0.4133339932766221803 ) ) ;
#17908=CARTESIAN_POINT ( 'NONE',  ( -2.263084017374999757, 26.95119850837999920, 0.1334610483750000021 ) ) ;
#17910=DIRECTION ( 'NONE',  ( 0.000000000000000000, 1.000000000000000000, 0.000000000000000000 ) ) ;
#17914=ORIENTED_EDGE ( 'NONE', *, *, #11499, .T. ) ;
#17920=CARTESIAN_POINT ( 'NONE',  ( -1.869327042239785852, 30.61308158997630002, -1.502106005567143354 ) ) ;
#17924=VERTEX_POINT ( 'NONE', #6843 ) ;
#17925=CARTESIAN_POINT ( 'NONE',  ( 0.000000000000000000, 17.00000000000000000, -4.649999999999999467 ) ) ;
#17926=CARTESIAN_POINT ( 'NONE',  ( -1.625358910797000123, 29.44327955148999720, -1.942508336889000153 ) ) ;
#17930=DIRECTION ( 'NONE',  ( 0.000000000000000000, 1.000000000000000000, 0.000000000000000000 ) ) ;
#17941=CARTESIAN_POINT ( 'NONE',  ( 2.000000000000198508, 24.49999999999999645, -3.464101615138341028 ) ) ;
#17942=ORIENTED_EDGE ( 'NONE', *, *, #9381, .T. ) ;
#17946=VECTOR ( 'NONE', #7805, 1000.000000000000114 ) ;
#17952=CARTESIAN_POINT ( 'NONE',  ( 0.000000000000000000, 17.89999999999999858, -3.000000000002987832 ) ) ;
#17954=CARTESIAN_POINT ( 'NONE',  ( -1.399999999999999911, 7.000000000000000000, 0.000000000000000000 ) ) ;
#17962=CARTESIAN_POINT ( 'NONE',  ( 2.045270984003000336, 28.93354368677000110, -0.7190670843306999904 ) ) ;
#17963=CARTESIAN_POINT ( 'NONE',  ( 1.699986222664000124, 9.100024384209000061, 1.053575639828000066 ) ) ;
#17965=EDGE_LOOP ( 'NONE', ( #15912, #15772, #3720, #18106 ) ) ;
#17971=CARTESIAN_POINT ( 'NONE',  ( 2.999999956181000016, 17.90000004382000043, -2.609181548331000199E-08 ) ) ;
#17972=VERTEX_POINT ( 'NONE', #271 ) ;
#17973=EDGE_CURVE ( 'NONE', #19300, #11498, #12129, .T. ) ;
#17974=CARTESIAN_POINT ( 'NONE',  ( -1.584557413972607076, 30.28301061182800780, -2.080722500251575457 ) ) ;
#17978=CARTESIAN_POINT ( 'NONE',  ( 1.745401010056999880, 27.08506359724000134, 1.745401010056999880 ) ) ;
#17980=ORIENTED_EDGE ( 'NONE', *, *, #20589, .F. ) ;
#17984=ORIENTED_EDGE ( 'NONE', *, *, #17713, .T. ) ;
#17991=CARTESIAN_POINT ( 'NONE',  ( 0.1765322295559999810, 30.44300150276000139, 2.181163051615000015 ) ) ;
#17994=CARTESIAN_POINT ( 'NONE',  ( 1.461484340634618073, 29.90904337753413955, -1.590560646070451778 ) ) ;
#17995=VERTEX_POINT ( 'NONE', #397 ) ;
#17998=CARTESIAN_POINT ( 'NONE',  ( -1.269727886480190193, 23.61570448070820305, -1.692922358328529553 ) ) ;
#17999=VECTOR ( 'NONE', #14899, 1000.000000000000000 ) ;
#18001=EDGE_CURVE ( 'NONE', #16978, #12276, #7677, .T. ) ;
#18002=CARTESIAN_POINT ( 'NONE',  ( -1.908614251018468710, 23.69762311453393977, 1.108721817513677266 ) ) ;
#18003=DIRECTION ( 'NONE',  ( 0.000000000000000000, 1.000000000000000000, 0.000000000000000000 ) ) ;
#18005=CARTESIAN_POINT ( 'NONE',  ( -3.150855693194152707, 24.60222989789001957, -2.799640769043123978 ) ) ;
#18012=CARTESIAN_POINT ( 'NONE',  ( 0.000000000000000000, 7.000000000000000000, 0.000000000000000000 ) ) ;
#18022=CARTESIAN_POINT ( 'NONE',  ( -0.2789569746687909357, 27.18793430507837527, 2.190778598715106718 ) ) ;
#18023=CARTESIAN_POINT ( 'NONE',  ( 2.944270284434495899, 26.42936170367566362, -2.918926912232258530 ) ) ;
#18025=ORIENTED_EDGE ( 'NONE', *, *, #3143, .T. ) ;
#18026=CARTESIAN_POINT ( 'NONE',  ( 1.920340719802868357, 26.32472163128880638, 1.149393952743590130 ) ) ;
#18027=CARTESIAN_POINT ( 'NONE',  ( -0.6576354733792000307, 28.70619850838000175, 2.169172474974999876 ) ) ;
#18031=CARTESIAN_POINT ( 'NONE',  ( 2.449054215377000077, 27.41187716035999955, 0.04809324771317000091 ) ) ;
#18033=VERTEX_POINT ( 'NONE', #13807 ) ;
#18034=DIRECTION ( 'NONE',  ( 0.000000000000000000, -1.000000000000000000, 0.000000000000000000 ) ) ;
#18038=VERTEX_POINT ( 'NONE', #22561 ) ;
#18040=CARTESIAN_POINT ( 'NONE',  ( 0.000000000000000000, 15.00000000000000000, 0.000000000000000000 ) ) ;
#18041=CIRCLE ( 'NONE', #2949, 4.000000000000000000 ) ;
#18045=CARTESIAN_POINT ( 'NONE',  ( 1.536366799937286087, 28.51666666666666927, -1.999167105995451665 ) ) ;
#18046=CARTESIAN_POINT ( 'NONE',  ( 2.575680369362000288, 29.21781557969000076, 0.8860769631535000412 ) ) ;
#18050=CONICAL_SURFACE ( 'NONE', #13770, 3.049999825846000157, 0.7853981633972997312 ) ;
#18052=DIRECTION ( 'NONE',  ( 0.000000000000000000, 0.4362437346113740011, -0.8998285414523820025 ) ) ;
#18056=CARTESIAN_POINT ( 'NONE',  ( 0.000000000000000000, 15.00000000000000000, -4.649999999999999467 ) ) ;
#18059=ORIENTED_EDGE ( 'NONE', *, *, #10475, .T. ) ;
#18061=AXIS2_PLACEMENT_3D ( 'NONE', #12347, #10407, #1437 ) ;
#18062=DIRECTION ( 'NONE',  ( 0.000000000000000000, 0.000000000000000000, -1.000000000000000000 ) ) ;
#18064=VERTEX_POINT ( 'NONE', #2679 ) ;
#18073=CARTESIAN_POINT ( 'NONE',  ( -1.875162437998086684, 26.21985616695894450, 0.9907346142373321118 ) ) ;
#18074=CONICAL_SURFACE ( 'NONE', #21934, 4.699999872533999756, 0.7853981633972997312 ) ;
#18076=ORIENTED_EDGE ( 'NONE', *, *, #8818, .F. ) ;
#18084=CARTESIAN_POINT ( 'NONE',  ( -1.901491585825000108, 30.15429474195000026, 1.041399949541000014 ) ) ;
#18090=CARTESIAN_POINT ( 'NONE',  ( -2.184465970885646424, 29.53333333333333144, -1.259047450927245126 ) ) ;
#18091=DIRECTION ( 'NONE',  ( 0.000000000000000000, 1.000000000000000000, 0.000000000000000000 ) ) ;
#18092=CONICAL_SURFACE ( 'NONE', #5323, 4.309401076758999416, 1.119376321708719590 ) ;
#18096=ADVANCED_FACE ( 'NONE', ( #10068 ), #15046, .F. ) ;
#18100=AXIS2_PLACEMENT_3D ( 'NONE', #22954, #13394, #6371 ) ;
#18101=CARTESIAN_POINT ( 'NONE',  ( 2.052373795670999979, 28.06006359723999921, -1.371352433351999744 ) ) ;
#18102=VERTEX_POINT ( 'NONE', #14057 ) ;
#18106=ORIENTED_EDGE ( 'NONE', *, *, #14312, .T. ) ;
#18107=DIRECTION ( 'NONE',  ( 0.000000000000000000, 1.000000000000000000, 0.000000000000000000 ) ) ;
#18115=CARTESIAN_POINT ( 'NONE',  ( 1.316912383867000047, 30.51493852343000412, 1.747677774086999980 ) ) ;
#18117=CARTESIAN_POINT ( 'NONE',  ( 1.721625935243284999, 29.88644617415637228, -1.304246024930588721 ) ) ;
#18118=ORIENTED_EDGE ( 'NONE', *, *, #15284, .F. ) ;
#18126=EDGE_CURVE ( 'NONE', #7614, #1045, #21329, .T. ) ;
#18129=ORIENTED_EDGE ( 'NONE', *, *, #1582, .F. ) ;
#18132=CARTESIAN_POINT ( 'NONE',  ( 2.177371421982348121, 27.24903633706587769, -0.3268671095024456852 ) ) ;
#18134=EDGE_CURVE ( 'NONE', #4988, #551, #3928, .T. ) ;
#18136=AXIS2_PLACEMENT_3D ( 'NONE', #12936, #20334, #7249 ) ;
#18137=ORIENTED_EDGE ( 'NONE', *, *, #19301, .T. ) ;
#18141=EDGE_CURVE ( 'NONE', #11746, #18064, #2119, .T. ) ;
#18144=EDGE_CURVE ( 'NONE', #4139, #21511, #13407, .T. ) ;
#18146=CARTESIAN_POINT ( 'NONE',  ( 1.684526538292457465, 28.11547461990329211, 1.425451057090266982 ) ) ;
#18152=CARTESIAN_POINT ( 'NONE',  ( 2.040326213578687486, 26.33271864848902055, 0.9387218070561216265 ) ) ;
#18153=CARTESIAN_POINT ( 'NONE',  ( 0.3985328791175999918, 26.36619850838000190, 2.231710853292999897 ) ) ;
#18154=AXIS2_PLACEMENT_3D ( 'NONE', #2544, #17450, #17696 ) ;
#18156=CARTESIAN_POINT ( 'NONE',  ( 0.9420013681046000009, 28.89271896306000187, 1.848781781241999989 ) ) ;
#18166=ORIENTED_EDGE ( 'NONE', *, *, #19913, .F. ) ;
#18173=CARTESIAN_POINT ( 'NONE',  ( 0.2320996736816000328, 30.35746553841000051, 2.138195049080999777 ) ) ;
#18178=VECTOR ( 'NONE', #22253, 1000.000000000000114 ) ;
#18179=DIRECTION ( 'NONE',  ( 0.000000000000000000, 1.000000000000000000, 0.000000000000000000 ) ) ;
#18181=LINE ( 'NONE', #7247, #18178 ) ;
#18184=DIRECTION ( 'NONE',  ( 0.000000000000000000, -1.000000000000000000, 0.000000000000000000 ) ) ;
#18185=DIRECTION ( 'NONE',  ( 0.000000000000000000, 1.000000000000000000, 0.000000000000000000 ) ) ;
#18189=CARTESIAN_POINT ( 'NONE',  ( -4.000000000000000000, 26.31534065533125144, 1.802053058880663805 ) ) ;
#18192=CARTESIAN_POINT ( 'NONE',  ( -1.907767351274999967, 24.04667396097999799, 1.684751507996000042 ) ) ;
#18193=DIRECTION ( 'NONE',  ( 0.000000000000000000, -1.000000000000000000, 0.000000000000000000 ) ) ;
#18196=DIRECTION ( 'NONE',  ( 0.000000000000000000, 0.000000000000000000, -1.000000000000000000 ) ) ;
#18200=AXIS2_PLACEMENT_3D ( 'NONE', #13402, #20803, #21037 ) ;
#18201=CARTESIAN_POINT ( 'NONE',  ( -1.963703823225463774, 26.25920717875808563, 0.8995588027868727243 ) ) ;
#18205=CARTESIAN_POINT ( 'NONE',  ( 1.244068065386999988, 24.76929142835999897, 1.746894613178000100 ) ) ;
#18207=LINE ( 'NONE', #10332, #11414 ) ;
#18211=DIRECTION ( 'NONE',  ( 0.000000000000000000, 0.000000000000000000, -1.000000000000000000 ) ) ;
#18219=EDGE_CURVE ( 'NONE', #21511, #10829, #7524, .T. ) ;
#18229=CARTESIAN_POINT ( 'NONE',  ( -1.706122057262999814, 30.94656064747999835, -1.370363639857999916 ) ) ;
#18231=CARTESIAN_POINT ( 'NONE',  ( 2.127842856066609389, 29.82575304422995899, -0.3714889427421172452 ) ) ;
#18232=ORIENTED_EDGE ( 'NONE', *, *, #12310, .T. ) ;
#18236=CARTESIAN_POINT ( 'NONE',  ( -2.102266727616999731, 23.66000000000000014, 0.4960590750638999569 ) ) ;
#18241=ADVANCED_FACE ( 'NONE', ( #8612 ), #17589, .T. ) ;
#18247=ORIENTED_EDGE ( 'NONE', *, *, #15909, .F. ) ;
#18254=CARTESIAN_POINT ( 'NONE',  ( 1.948395284584199638, 28.14197577173313292, 1.033326755142028430 ) ) ;
#18255=CARTESIAN_POINT ( 'NONE',  ( -1.500144717171000064, 28.73000240009999828, -2.447990496630999768 ) ) ;
#18257=ORIENTED_EDGE ( 'NONE', *, *, #3368, .T. ) ;
#18262=EDGE_CURVE ( 'NONE', #479, #14961, #23623, .T. ) ;
#18265=CARTESIAN_POINT ( 'NONE',  ( -0.6636689712800000196, 28.79521896306000173, 2.189073617939000016 ) ) ;
#18266=LINE ( 'NONE', #7349, #21659 ) ;
#18267=ORIENTED_EDGE ( 'NONE', *, *, #10127, .T. ) ;
#18268=ADVANCED_FACE ( 'NONE', ( #14179 ), #18732, .T. ) ;
#18271=AXIS2_PLACEMENT_3D ( 'NONE', #4354, #16947, #115 ) ;
#18272=CARTESIAN_POINT ( 'NONE',  ( 2.202166145775246164, 29.66321151848345394, -0.5828424432849000913 ) ) ;
#18273=ORIENTED_EDGE ( 'NONE', *, *, #3908, .T. ) ;
#18274=CARTESIAN_POINT ( 'NONE',  ( 2.500000000000001332, 24.38333333333333641, 0.3272492347489234787 ) ) ;
#18280=CARTESIAN_POINT ( 'NONE',  ( 1.754903278477999873, 30.62218442030999910, -1.243399122562000025 ) ) ;
#18283=AXIS2_PLACEMENT_3D ( 'NONE', #2087, #22432, #11062 ) ;
#18285=FACE_OUTER_BOUND ( 'NONE', #13377, .T. ) ;
#18287=DIRECTION ( 'NONE',  ( 0.000000000000000000, 1.000000000000000000, 0.000000000000000000 ) ) ;
#18291=CARTESIAN_POINT ( 'NONE',  ( 0.2552732384256292120, 29.18862125910514038, -2.144907518227253007 ) ) ;
#18294=CARTESIAN_POINT ( 'NONE',  ( 0.000000000000000000, 22.09999988306816832, 0.000000000000000000 ) ) ;
#18295=ORIENTED_EDGE ( 'NONE', *, *, #10087, .F. ) ;
#18296=CARTESIAN_POINT ( 'NONE',  ( -1.619994985406000065, 23.83580469984000061, 1.430619405864999916 ) ) ;
#18298=CARTESIAN_POINT ( 'NONE',  ( 2.184465970885649977, 28.33333333333333570, 1.259047450927240686 ) ) ;
#18303=ORIENTED_EDGE ( 'NONE', *, *, #20745, .F. ) ;
#18305=CARTESIAN_POINT ( 'NONE',  ( -0.8800650012412046808, 26.22123020134747762, 1.934182370176196208 ) ) ;
#18307=EDGE_LOOP ( 'NONE', ( #697, #4334, #218, #23684 ) ) ;
#18311=CARTESIAN_POINT ( 'NONE',  ( 0.01836207933452999735, 24.98406236978999928, -2.335018217200000024 ) ) ;
#18315=CARTESIAN_POINT ( 'NONE',  ( 1.263588213801000171, 30.36972139875000209, 1.761683537874000116 ) ) ;
#18319=EDGE_LOOP ( 'NONE', ( #6081, #22254, #17232, #22686, #1907 ) ) ;
#18323=ORIENTED_EDGE ( 'NONE', *, *, #9715, .F. ) ;
#18324=LINE ( 'NONE', #7286, #9915 ) ;
#18327=B_SPLINE_CURVE_WITH_KNOTS ( 'NONE', 3,
 ( #20182, #14715, #9040, #20297, #1769, #3943 ),
 .UNSPECIFIED., .F., .F.,
 ( 4, 2, 4 ),
 ( 0.000000000000000000, 0.1249467100871154007, 0.2498934201742307459 ),
 .UNSPECIFIED. ) ;
#18339=CARTESIAN_POINT ( 'NONE',  ( 0.5050338295773000308, 28.84204524523000046, 2.287831773294000115 ) ) ;
#18341=CARTESIAN_POINT ( 'NONE',  ( -0.2273216873190004872, 30.01705067798956250, -2.154795586676287567 ) ) ;
#18343=CARTESIAN_POINT ( 'NONE',  ( 2.234556666495999711, 24.25198102494999830, -0.6798364240153000893 ) ) ;
#18345=CARTESIAN_POINT ( 'NONE',  ( -1.955724675740084795, 26.26076676662178855, 0.9180910909140133080 ) ) ;
#18346=EDGE_LOOP ( 'NONE', ( #14507, #10019, #22168, #21936 ) ) ;
#18347=CARTESIAN_POINT ( 'NONE',  ( -0.3136752098478812756, 23.81257023422828922, 2.231325233347782877 ) ) ;
#18355=DIRECTION ( 'NONE',  ( 0.000000000000000000, -1.000000000000000000, 9.414779719719000361E-11 ) ) ;
#18363=CARTESIAN_POINT ( 'NONE',  ( -2.145417483866896013, 27.78421022192531709, -0.3448129055962916301 ) ) ;
#18365=CARTESIAN_POINT ( 'NONE',  ( 2.826365205286999860, 28.43750240009999786, 0.5047246425490000687 ) ) ;
#18366=EDGE_CURVE ( 'NONE', #20885, #23589, #6475, .T. ) ;
#18367=CARTESIAN_POINT ( 'NONE',  ( 1.888917822874810026, 30.66857564960811189, -1.051002523236465924 ) ) ;
#18368=ORIENTED_EDGE ( 'NONE', *, *, #14010, .T. ) ;
#18370=CARTESIAN_POINT ( 'NONE',  ( 1.539407619234959501, 24.77839267836325021, 1.461333290478949332 ) ) ;
#18372=CARTESIAN_POINT ( 'NONE',  ( 2.287373719275000106, 27.43021896306000329, 0.04491825056504000074 ) ) ;
#18373=CARTESIAN_POINT ( 'NONE',  ( -2.122871095894375948, 30.87585552377906595, 0.07971169187474370921 ) ) ;
#18374=CIRCLE ( 'NONE', #4459, 4.750000000000000000 ) ;
#18380=CARTESIAN_POINT ( 'NONE',  ( 1.412335231500430277, 28.94512266248814925, -1.787330250453557090 ) ) ;
#18382=FACE_OUTER_BOUND ( 'NONE', #20847, .T. ) ;
#18387=CARTESIAN_POINT ( 'NONE',  ( 1.999533992831999729, 29.69566833366999958, 0.7922197204133999415 ) ) ;
#18391=ORIENTED_EDGE ( 'NONE', *, *, #5373, .T. ) ;
#18392=CARTESIAN_POINT ( 'NONE',  ( -2.434931691670786602, 28.83333333333333215, 0.6543697108982093891 ) ) ;
#18394=EDGE_CURVE ( 'NONE', #12844, #19694, #11792, .T. ) ;
#18396=DIRECTION ( 'NONE',  ( -0.5000000000000169864, 0.000000000000000000, 0.8660254037844289376 ) ) ;
#18400=CARTESIAN_POINT ( 'NONE',  ( -0.4160351173932703150, 29.22861210950169308, -2.119817327165559817 ) ) ;
#18402=ORIENTED_EDGE ( 'NONE', *, *, #3722, .F. ) ;
#18404=ORIENTED_EDGE ( 'NONE', *, *, #6748, .F. ) ;
#18405=CARTESIAN_POINT ( 'NONE',  ( 1.092712698506000057, 24.81118861319000146, 1.864679196896000146 ) ) ;
#18406=CARTESIAN_POINT ( 'NONE',  ( -1.259047450927242462, 28.13333333333332931, 2.184465970885648201 ) ) ;
#18407=CIRCLE ( 'NONE', #21886, 4.750000000000000000 ) ;
#18411=CARTESIAN_POINT ( 'NONE',  ( -2.749999993363999806, 22.20000000663619844, 7.185653392336999782E-09 ) ) ;
#18412=CARTESIAN_POINT ( 'NONE',  ( 0.000000000000000000, 24.50000000000000000, 0.000000000000000000 ) ) ;
#18419=VERTEX_POINT ( 'NONE', #21132 ) ;
#18421=CARTESIAN_POINT ( 'NONE',  ( -1.109476331411000105, 25.04810348418999766, -2.054679907054999699 ) ) ;
#18426=CARTESIAN_POINT ( 'NONE',  ( -0.7614732458495000467, 28.54087351380000115, 2.105206779053000243 ) ) ;
#18431=ORIENTED_EDGE ( 'NONE', *, *, #23913, .T. ) ;
#18432=CARTESIAN_POINT ( 'NONE',  ( -1.326172741988208337, 24.10416131130349271, -2.158080337669399551 ) ) ;
#18436=CARTESIAN_POINT ( 'NONE',  ( 1.119414263319356229, 30.77472232402685037, -1.944946624573452576 ) ) ;
#18443=CARTESIAN_POINT ( 'NONE',  ( 0.4339301335947999827, 26.20756359724000006, 2.429928970624000151 ) ) ;
#18445=CIRCLE ( 'NONE', #4529, 4.625000000000000000 ) ;
#18455=CARTESIAN_POINT ( 'NONE',  ( 1.534365737191000001, 29.70528949332000224, 1.770661353676000083 ) ) ;
#18458=CARTESIAN_POINT ( 'NONE',  ( 1.516020976517132635, 29.90463563117074131, -1.538576683859487204 ) ) ;
#18459=VERTEX_POINT ( 'NONE', #13611 ) ;
#18460=CARTESIAN_POINT ( 'NONE',  ( 2.087681966606000028, 25.60832866306000355, -0.3296552320861999563 ) ) ;
#18463=CARTESIAN_POINT ( 'NONE',  ( -0.9013079783759136987, 23.63028988911640127, -1.930365035980913468 ) ) ;
#18464=ORIENTED_EDGE ( 'NONE', *, *, #10887, .T. ) ;
#18470=ORIENTED_EDGE ( 'NONE', *, *, #13997, .F. ) ;
#18471=AXIS2_PLACEMENT_3D ( 'NONE', #14883, #22397, #16820 ) ;
#18472=CARTESIAN_POINT ( 'NONE',  ( 0.000000000000000000, 22.19999999999999574, 0.000000000000000000 ) ) ;
#18477=CARTESIAN_POINT ( 'NONE',  ( 0.000000000000000000, 24.50000000000000000, 0.000000000000000000 ) ) ;
#18482=CARTESIAN_POINT ( 'NONE',  ( 1.165223649068083844, 26.45298450433979554, -2.066627348871238556 ) ) ;
#18486=ORIENTED_EDGE ( 'NONE', *, *, #11625, .T. ) ;
#18490=AXIS2_PLACEMENT_3D ( 'NONE', #12520, #18091, #3440 ) ;
#18492=CARTESIAN_POINT ( 'NONE',  ( -2.276798263289999902, 27.82021896306000031, -0.2242450566329000083 ) ) ;
#18494=ORIENTED_EDGE ( 'NONE', *, *, #5783, .T. ) ;
#18499=CARTESIAN_POINT ( 'NONE',  ( 0.1562663868984598969, 28.63946909753791914, 2.160009633825578756 ) ) ;
#18500=VERTEX_POINT ( 'NONE', #11812 ) ;
#18501=EDGE_CURVE ( 'NONE', #16087, #23589, #13312, .T. ) ;
#18506=CARTESIAN_POINT ( 'NONE',  ( 0.3272492347489454056, 29.25086340285666608, 2.499999999999998668 ) ) ;
#18507=CARTESIAN_POINT ( 'NONE',  ( 0.3299503294897000449, 29.56330889271999851, 2.125295521557999834 ) ) ;
#18509=DIRECTION ( 'NONE',  ( 0.000000000000000000, -1.000000000000000000, 0.000000000000000000 ) ) ;
#18517=DIRECTION ( 'NONE',  ( 0.000000000000000000, 1.000000000000000000, 0.000000000000000000 ) ) ;
#18520=CARTESIAN_POINT ( 'NONE',  ( 1.438533966298229494, 29.11160131773634774, -1.622102280252738060 ) ) ;
#18522=ORIENTED_EDGE ( 'NONE', *, *, #1261, .T. ) ;
#18526=CARTESIAN_POINT ( 'NONE',  ( 0.3718092809970000023, 24.42893128708999839, -2.323663357635999738 ) ) ;
#18532=VECTOR ( 'NONE', #4125, 1000.000000000000227 ) ;
#18536=FACE_OUTER_BOUND ( 'NONE', #23036, .T. ) ;
#18537=AXIS2_PLACEMENT_3D ( 'NONE', #846, #8249, #15616 ) ;
#18542=CARTESIAN_POINT ( 'NONE',  ( -2.212662158434000048, 24.34365122578000040, -0.7461725103679001103 ) ) ;
#18547=CARTESIAN_POINT ( 'NONE',  ( 1.488049260313999866, 30.15885213760000028, 2.074625148294999999 ) ) ;
#18548=EDGE_CURVE ( 'NONE', #2983, #1045, #548, .T. ) ;
#18555=CARTESIAN_POINT ( 'NONE',  ( 2.369722497171532272, 23.91240411898208151, -0.5226290486314587591 ) ) ;
#18557=B_SPLINE_CURVE_WITH_KNOTS ( 'NONE', 3,
 ( #4047, #1757, #400, #7318, #12885, #10096, #17118, #2345, #2836, #20880, #20993, #19173, #15529, #11677, #7918, #19050 ),
 .UNSPECIFIED., .F., .F.,
 ( 4, 2, 2, 2, 2, 2, 2, 4 ),
 ( 0.0007950867507350306432, 0.001248881430381147684, 0.001702676110027264832, 0.002156470789673382415, 0.002610265469319499564, 0.003517854828611732994, 0.003971649508257850576, 0.004425444187903967291 ),
 .UNSPECIFIED. ) ;
#18558=EDGE_CURVE ( 'NONE', #2559, #12315, #21499, .T. ) ;
#18559=ORIENTED_EDGE ( 'NONE', *, *, #23708, .F. ) ;
#18560=DIRECTION ( 'NONE',  ( 0.000000000000000000, 1.000000000000000000, 0.000000000000000000 ) ) ;
#18566=CARTESIAN_POINT ( 'NONE',  ( 2.669209039122999894, 27.07712896666999924, 0.05241653317053000111 ) ) ;
#18578=CARTESIAN_POINT ( 'NONE',  ( -2.187619468058000116, 29.43588321332000035, 0.05437783349231000568 ) ) ;
#18582=CARTESIAN_POINT ( 'NONE',  ( 1.222085875088660512, 29.68033221944324040, 1.780880044240042537 ) ) ;
#18584=CARTESIAN_POINT ( 'NONE',  ( -2.150969990163999590, 23.76339666646000026, -0.9104165138074999941 ) ) ;
#18587=ORIENTED_EDGE ( 'NONE', *, *, #1089, .T. ) ;
#18600=AXIS2_PLACEMENT_3D ( 'NONE', #9792, #12579, #12104 ) ;
#18606=CARTESIAN_POINT ( 'NONE',  ( -2.500000000000000000, 26.63419673618999894, 0.000000000000000000 ) ) ;
#18608=CARTESIAN_POINT ( 'NONE',  ( -0.6269526792712883934, 30.36641892158466050, 2.067003944720025466 ) ) ;
#18614=DIRECTION ( 'NONE',  ( 1.000000000000000000, 0.000000000000000000, 0.000000000000000000 ) ) ;
#18617=ORIENTED_EDGE ( 'NONE', *, *, #9231, .F. ) ;
#18621=ORIENTED_EDGE ( 'NONE', *, *, #8989, .F. ) ;
#18622=CARTESIAN_POINT ( 'NONE',  ( -1.775821082844895482, 26.49941889561072017, 1.759684967125137556 ) ) ;
#18625=CARTESIAN_POINT ( 'NONE',  ( -0.3272492347489284192, 29.21753006952332754, 2.500000000000001332 ) ) ;
#18626=CARTESIAN_POINT ( 'NONE',  ( 0.7229397994487999357, 29.10005084940000231, -2.025612581347999708 ) ) ;
#18633=DIRECTION ( 'NONE',  ( -0.7071067811865462405, -0.7071067811865462405, -6.203608861676411764E-08 ) ) ;
#18635=CARTESIAN_POINT ( 'NONE',  ( 0.000000000000000000, 22.10000000618969906, 0.000000000000000000 ) ) ;
#18636=DIRECTION ( 'NONE',  ( 0.000000000000000000, -1.000000000000000000, 0.000000000000000000 ) ) ;
#18637=B_SPLINE_CURVE_WITH_KNOTS ( 'NONE', 3,
 ( #4066, #11460, #15189, #19069, #15072, #14950, #22586, #419, #18836, #7818, #2484, #20542, #22467, #5764, #20777, #9873, #11580, #15434 ),
 .UNSPECIFIED., .F., .F.,
 ( 4, 2, 2, 2, 2, 2, 2, 2, 4 ),
 ( 0.000000000000000000, 0.1250000000000000555, 0.2500000000000000555, 0.3750000000000000555, 0.5000000000000000000, 0.6249999999999998890, 0.7499999999999998890, 0.8749999999999998890, 1.000000000000000000 ),
 .UNSPECIFIED. ) ;
#18639=CARTESIAN_POINT ( 'NONE',  ( -1.368941726107665957, 29.29130111891828037, -1.671115392335038363 ) ) ;
#18641=ORIENTED_EDGE ( 'NONE', *, *, #22278, .F. ) ;
#18643=ORIENTED_EDGE ( 'NONE', *, *, #9544, .T. ) ;
#18644=CARTESIAN_POINT ( 'NONE',  ( -2.344138058790000034, 24.63794212566000041, -0.2065679117753000116 ) ) ;
#18645=CARTESIAN_POINT ( 'NONE',  ( -1.536366799937282090, 28.11666666666666714, 1.999167105995454552 ) ) ;
#18646=DIRECTION ( 'NONE',  ( 0.000000000000000000, 0.000000000000000000, -1.000000000000000000 ) ) ;
#18657=CARTESIAN_POINT ( 'NONE',  ( 2.287833579909999582, 23.95940453936999859, 0.4674021866452000018 ) ) ;
#18661=CARTESIAN_POINT ( 'NONE',  ( 1.647802091131999935, 29.36895439600999680, 1.950156003153999951 ) ) ;
#18664=CARTESIAN_POINT ( 'NONE',  ( 0.000000000000000000, 24.80000000000000426, -4.618802153517000519 ) ) ;
#18677=CARTESIAN_POINT ( 'NONE',  ( -1.371352433351999744, 26.11006359723999992, 2.052373795670999979 ) ) ;
#18679=EDGE_LOOP ( 'NONE', ( #20858, #857, #19394 ) ) ;
#18681=CARTESIAN_POINT ( 'NONE',  ( -2.500000000000000000, 27.43419673618999965, 0.000000000000000000 ) ) ;
#18683=PLANE ( 'NONE',  #4791 ) ;
#18687=DIRECTION ( 'NONE',  ( 0.000000000000000000, -1.000000000000000000, 0.000000000000000000 ) ) ;
#18690=CARTESIAN_POINT ( 'NONE',  ( -2.353996515996000127, 30.01643588093000048, -0.1022769623496000008 ) ) ;
#18692=EDGE_CURVE ( 'NONE', #15019, #14560, #21481, .T. ) ;
#18693=CARTESIAN_POINT ( 'NONE',  ( -0.07238424743993485122, 29.59961443721505603, 2.158644815808733686 ) ) ;
#18694=CARTESIAN_POINT ( 'NONE',  ( 2.087036767532999715, 24.27032282765000204, -0.6349553063932998898 ) ) ;
#18699=CARTESIAN_POINT ( 'NONE',  ( -2.000000000000000000, 26.50000000000000355, 3.464101615137999968 ) ) ;
#18701=ADVANCED_FACE ( 'NONE', ( #8521 ), #21942, .T. ) ;
#18703=ORIENTED_EDGE ( 'NONE', *, *, #20897, .T. ) ;
#18706=AXIS2_PLACEMENT_3D ( 'NONE', #1540, #11089, #14713 ) ;
#18715=AXIS2_PLACEMENT_3D ( 'NONE', #7775, #15141, #22538 ) ;
#18716=ADVANCED_FACE ( 'NONE', ( #8994 ), #22599, .F. ) ;
#18717=CARTESIAN_POINT ( 'NONE',  ( 0.3837787240339659012, 30.42650728909961444, 2.125527850226935023 ) ) ;
#18718=ORIENTED_EDGE ( 'NONE', *, *, #21965, .T. ) ;
#18721=DIRECTION ( 'NONE',  ( 0.7071067811865474617, -0.7071067811865474617, -2.031299026805133754E-12 ) ) ;
#18724=CARTESIAN_POINT ( 'NONE',  ( -2.239169049547999890, 26.01614211382000263, 0.4912911496346999418 ) ) ;
#18732=CONICAL_SURFACE ( 'NONE', #7135, 4.309401076758999416, 1.119376321708719590 ) ;
#18741=DIRECTION ( 'NONE',  ( 0.000000000000000000, 0.000000000000000000, -1.000000000000000000 ) ) ;
#18744=ORIENTED_EDGE ( 'NONE', *, *, #7620, .F. ) ;
#18749=CARTESIAN_POINT ( 'NONE',  ( -0.3174390796334333187, 29.22271852741722853, -2.136439859271641595 ) ) ;
#18752=CARTESIAN_POINT ( 'NONE',  ( 0.5386878631261170502, 23.78722934400546762, 2.239973159359923915 ) ) ;
#18753=ORIENTED_EDGE ( 'NONE', *, *, #22670, .F. ) ;
#18754=CARTESIAN_POINT ( 'NONE',  ( 1.570067792648999871, 25.64723196749999801, 1.485270726656999996 ) ) ;
#18756=CARTESIAN_POINT ( 'NONE',  ( 2.245636445399999737, 26.50799822781000259, -0.3106091461882000138 ) ) ;
#18758=DIRECTION ( 'NONE',  ( 1.000000000000000000, 0.000000000000000000, 0.000000000000000000 ) ) ;
#18764=ORIENTED_EDGE ( 'NONE', *, *, #8818, .T. ) ;
#18766=CARTESIAN_POINT ( 'NONE',  ( -0.5993264675742000502, 24.11013436640999785, -2.453430812916000292 ) ) ;
#18770=CARTESIAN_POINT ( 'NONE',  ( -1.131706023269000161, 28.93810108242000112, -2.288580742153000003 ) ) ;
#18780=CARTESIAN_POINT ( 'NONE',  ( 2.100726171210397730, 23.93868288328740945, -1.266752783226519297 ) ) ;
#18783=DIRECTION ( 'NONE',  ( -8.659361257114346592E-17, 0.7071230553199298052, 0.7070905066786058457 ) ) ;
#18784=DIRECTION ( 'NONE',  ( 1.000000000000000000, 0.000000000000000000, 0.000000000000000000 ) ) ;
#18786=ORIENTED_EDGE ( 'NONE', *, *, #14420, .F. ) ;
#18789=CARTESIAN_POINT ( 'NONE',  ( 2.387212940976999764, 27.84919433610000183, -1.595084814687000030 ) ) ;
#18791=VERTEX_POINT ( 'NONE', #19894 ) ;
#18793=CARTESIAN_POINT ( 'NONE',  ( 2.500000000000000000, 27.03419673618999752, 0.000000000000000000 ) ) ;
#18794=PLANE ( 'NONE',  #11315 ) ;
#18797=ORIENTED_EDGE ( 'NONE', *, *, #11337, .T. ) ;
#18805=CARTESIAN_POINT ( 'NONE',  ( -0.9825804459669998936, 29.29200917197999843, -1.955293243215000087 ) ) ;
#18808=CARTESIAN_POINT ( 'NONE',  ( 1.414948191568242697, 29.69462877122279920, 1.631989406709256629 ) ) ;
#18810=AXIS2_PLACEMENT_3D ( 'NONE', #2991, #15808, #2623 ) ;
#18811=CARTESIAN_POINT ( 'NONE',  ( 1.908188185705999906, 24.96830048264000013, 1.057217360667000117 ) ) ;
#18820=B_SPLINE_CURVE_WITH_KNOTS ( 'NONE', 3,
 ( #735, #2812, #11889, #13451 ),
 .UNSPECIFIED., .F., .F.,
 ( 4, 4 ),
 ( 0.000000000000000000, 1.000000000000000000 ),
 .UNSPECIFIED. ) ;
#18821=DIRECTION ( 'NONE',  ( 0.5000000000000169864, 0.000000000000000000, 0.8660254037844288266 ) ) ;
#18822=CARTESIAN_POINT ( 'NONE',  ( 2.999999971291051892, 16.89999999999998437, -1.709463755659355061E-08 ) ) ;
#18827=DIRECTION ( 'NONE',  ( -1.000000000000000000, 0.000000000000000000, 0.000000000000000000 ) ) ;
#18833=CARTESIAN_POINT ( 'NONE',  ( 2.062331871376394954, 26.40495869946155594, -1.040606430369203750 ) ) ;
#18835=CARTESIAN_POINT ( 'NONE',  ( 0.9358744650684699407, 26.41068681084919589, -4.078474779182607257 ) ) ;
#18836=CARTESIAN_POINT ( 'NONE',  ( -0.3272492347489394104, 28.05086340285666324, -2.499999999999999112 ) ) ;
#18837=ADVANCED_FACE ( 'NONE', ( #7051 ), #10254, .F. ) ;
#18838=CARTESIAN_POINT ( 'NONE',  ( 0.8112170600937859133, 30.45292097617447524, 2.003657457152344890 ) ) ;
#18843=DIRECTION ( 'NONE',  ( 0.000000000000000000, 0.000000000000000000, -1.000000000000000000 ) ) ;
#18845=CARTESIAN_POINT ( 'NONE',  ( 0.000000000000000000, -1.550000000000000044, 0.000000000000000000 ) ) ;
#18846=VECTOR ( 'NONE', #9824, 1000.000000000000114 ) ;
#18850=FACE_OUTER_BOUND ( 'NONE', #19773, .T. ) ;
#18853=CARTESIAN_POINT ( 'NONE',  ( -1.009279597712957832, 28.56811160064914290, 1.920956085076729991 ) ) ;
#18855=EDGE_CURVE ( 'NONE', #1169, #2559, #18207, .T. ) ;
#18860=CYLINDRICAL_SURFACE ( 'NONE', #12363, 3.000000000000000000 ) ;
#18862=CARTESIAN_POINT ( 'NONE',  ( 1.065101660326078559, 24.49999999999999289, 2.250874270545449196 ) ) ;
#18866=EDGE_CURVE ( 'NONE', #23163, #8845, #22992, .T. ) ;
#18870=CARTESIAN_POINT ( 'NONE',  ( -2.665093312283999705, 27.16206776952000013, 0.1571687770952999719 ) ) ;
#18872=CARTESIAN_POINT ( 'NONE',  ( 2.500000000000000000, 30.23419673619000037, 0.000000000000000000 ) ) ;
#18875=VERTEX_POINT ( 'NONE', #5470 ) ;
#18877=ORIENTED_EDGE ( 'NONE', *, *, #14522, .F. ) ;
#18878=CARTESIAN_POINT ( 'NONE',  ( 0.4755391251864483082, 26.25858828695499270, 2.107219116345798948 ) ) ;
#18879=CARTESIAN_POINT ( 'NONE',  ( -1.259486242684000112, 26.21549822780999861, 1.884954223019000175 ) ) ;
#18881=DIRECTION ( 'NONE',  ( 0.000000000000000000, 1.000000000000000000, 0.000000000000000000 ) ) ;
#18888=CIRCLE ( 'NONE', #11551, 4.000000000000000000 ) ;
#18890=CARTESIAN_POINT ( 'NONE',  ( 2.521890885781000069, 24.68650439600999746, -0.1363133561440000030 ) ) ;
#18891=VECTOR ( 'NONE', #21300, 1000.000000000000114 ) ;
#18896=CARTESIAN_POINT ( 'NONE',  ( -2.527261889986999854, 30.66151433680000338, -0.3618990238287000394 ) ) ;
#18902=CARTESIAN_POINT ( 'NONE',  ( 0.000000000000000000, 24.49999999999999645, -4.549999999999999822 ) ) ;
#18907=CARTESIAN_POINT ( 'NONE',  ( -2.016898400252999934, 25.75452502063999916, 1.850425600441000018 ) ) ;
#18913=CARTESIAN_POINT ( 'NONE',  ( -1.500000000000000000, 7.100000000000000533, 0.000000000000000000 ) ) ;
#18914=CARTESIAN_POINT ( 'NONE',  ( -2.804372049896000085, 25.80169433610000240, 0.6153010951427000386 ) ) ;
#18915=ORIENTED_EDGE ( 'NONE', *, *, #12836, .T. ) ;
#18916=VERTEX_POINT ( 'NONE', #9104 ) ;
#18919=CONICAL_SURFACE ( 'NONE', #5762, 1.949955127985000258, 0.7853751480324476786 ) ;
#18922=ORIENTED_EDGE ( 'NONE', *, *, #23322, .T. ) ;
#18929=CARTESIAN_POINT ( 'NONE',  ( -0.7615468713905999554, 30.66386906700000026, -2.229746170830000374 ) ) ;
#18933=CARTESIAN_POINT ( 'NONE',  ( 0.9667294541704517519, 29.66303702619708105, 1.931402186862774428 ) ) ;
#18935=CARTESIAN_POINT ( 'NONE',  ( 0.3893505392225000694, 24.16584150941000075, -2.150934381757999780 ) ) ;
#18938=EDGE_CURVE ( 'NONE', #10250, #6636, #15124, .T. ) ;
#18940=LINE ( 'NONE', #11442, #22306 ) ;
#18942=EDGE_LOOP ( 'NONE', ( #16234, #17117, #23407 ) ) ;
#18944=DIRECTION ( 'NONE',  ( 0.000000000000000000, -1.000000000000000000, 0.000000000000000000 ) ) ;
#18945=ORIENTED_EDGE ( 'NONE', *, *, #2363, .T. ) ;
#18946=CARTESIAN_POINT ( 'NONE',  ( 4.000000000000000000, 26.50000000000000355, 0.000000000000000000 ) ) ;
#18955=CARTESIAN_POINT ( 'NONE',  ( 2.434931691670788823, 28.66753006952332683, -0.6543697108982007293 ) ) ;
#18957=CARTESIAN_POINT ( 'NONE',  ( 0.6841124492484266240, 30.44492334872505168, 2.049014591910544247 ) ) ;
#18964=CARTESIAN_POINT ( 'NONE',  ( -2.451511826319000331, 27.60946440325999873, -0.2414528406811000116 ) ) ;
#18965=DIRECTION ( 'NONE',  ( 1.000000000000000000, 0.000000000000000000, 0.000000000000000000 ) ) ;
#18969=CARTESIAN_POINT ( 'NONE',  ( -1.269001982510553850, 28.30922767041318622, -1.762276763077230912 ) ) ;
#18970=VERTEX_POINT ( 'NONE', #122 ) ;
#18975=DIRECTION ( 'NONE',  ( -0.000000000000000000, -1.000000000000000000, -0.000000000000000000 ) ) ;
#18980=DIRECTION ( 'NONE',  ( 0.000000000000000000, -1.000000000000000000, 0.000000000000000000 ) ) ;
#18983=CARTESIAN_POINT ( 'NONE',  ( -2.329463490920999913, 28.81956776951999899, 1.304555153736000062 ) ) ;
#18985=CARTESIAN_POINT ( 'NONE',  ( 2.114481634776250285, 29.03000053035885131, -0.4410627826741955748 ) ) ;
#18989=DIRECTION ( 'NONE',  ( 0.000000000000000000, 1.000000000000000000, 0.000000000000000000 ) ) ;
#18991=CARTESIAN_POINT ( 'NONE',  ( 0.000000000000000000, 15.00000000000000000, 0.000000000000000000 ) ) ;
#18993=CARTESIAN_POINT ( 'NONE',  ( -2.388357610153000188, 28.35256359723999964, -0.6232602838477999674 ) ) ;
#19000=DIRECTION ( 'NONE',  ( 0.000000000000000000, 0.000000000000000000, -1.000000000000000000 ) ) ;
#19002=CARTESIAN_POINT ( 'NONE',  ( -1.650266299029000017, 30.34287082775999878, -2.167006502583999961 ) ) ;
#19003=CARTESIAN_POINT ( 'NONE',  ( 1.465061595431000008, 24.55842216721000426, 2.057209151362000110 ) ) ;
#19006=CYLINDRICAL_SURFACE ( 'NONE', #4853, 2.000000000000000000 ) ;
#19017=LINE ( 'NONE', #3899, #9226 ) ;
#19020=CIRCLE ( 'NONE', #1247, 1.999999999999998668 ) ;
#19022=CARTESIAN_POINT ( 'NONE',  ( 1.713341213838733612, 24.28993051964441463, -1.368779845717938315 ) ) ;
#19026=CARTESIAN_POINT ( 'NONE',  ( 0.000000000000000000, 14.95000002005000006, -4.674999979945999584 ) ) ;
#19028=ORIENTED_EDGE ( 'NONE', *, *, #11737, .F. ) ;
#19034=ORIENTED_EDGE ( 'NONE', *, *, #8801, .T. ) ;
#19041=CARTESIAN_POINT ( 'NONE',  ( -1.837043917312000119, 30.73580608766999944, -1.475520569229000101 ) ) ;
#19043=AXIS2_PLACEMENT_3D ( 'NONE', #17590, #984, #15873 ) ;
#19045=CARTESIAN_POINT ( 'NONE',  ( 0.3079095288441306422, 29.62188598588733868, 2.138016069174891953 ) ) ;
#19047=CARTESIAN_POINT ( 'NONE',  ( 1.079791510068999871, 24.65442586790999968, 1.900569086254999984 ) ) ;
#19049=ORIENTED_EDGE ( 'NONE', *, *, #11754, .F. ) ;
#19050=CARTESIAN_POINT ( 'NONE',  ( -2.246347731941017223, 24.65365226805931087, -5.222125272214524731E-08 ) ) ;
#19052=CARTESIAN_POINT ( 'NONE',  ( -2.147180172777956919, 30.84444203262654938, 0.1925145778103813932 ) ) ;
#19055=ORIENTED_EDGE ( 'NONE', *, *, #14723, .T. ) ;
#19060=CARTESIAN_POINT ( 'NONE',  ( -2.008209816024387084, 24.68901357082605585, 0.9452844701119602622 ) ) ;
#19068=CARTESIAN_POINT ( 'NONE',  ( -1.678813317411953498, 26.50000000000001066, 3.649538832790644616 ) ) ;
#19069=CARTESIAN_POINT ( 'NONE',  ( -2.184465970885646424, 28.16753006952332683, -1.259047450927245126 ) ) ;
#19070=CARTESIAN_POINT ( 'NONE',  ( 2.158678543002582106, 30.61128633804222687, -0.1265477462312649959 ) ) ;
#19076=CARTESIAN_POINT ( 'NONE',  ( 2.500000000000000000, 27.83419673618999823, 0.000000000000000000 ) ) ;
#19078=CARTESIAN_POINT ( 'NONE',  ( 1.203722632180999952, 25.75696440325999959, -2.149413090608000232 ) ) ;
#19082=CARTESIAN_POINT ( 'NONE',  ( -2.500000000000000000, 27.43419673618999965, 0.000000000000000000 ) ) ;
#19083=DIRECTION ( 'NONE',  ( 0.000000000000000000, 0.000000000000000000, -1.000000000000000000 ) ) ;
#19085=ORIENTED_EDGE ( 'NONE', *, *, #3353, .T. ) ;
#19087=B_SPLINE_CURVE_WITH_KNOTS ( 'NONE', 3,
 ( #4565, #13751, #23068, #7953 ),
 .UNSPECIFIED., .F., .F.,
 ( 4, 4 ),
 ( 0.000000000000000000, 1.000000000000000000 ),
 .UNSPECIFIED. ) ;
#19089=CIRCLE ( 'NONE', #2088, 2.500000000000000000 ) ;
#19091=ADVANCED_FACE ( 'NONE', ( #15364 ), #19006, .T. ) ;
#19096=CARTESIAN_POINT ( 'NONE',  ( 0.000000000000000000, 21.94999982584599962, 0.000000000000000000 ) ) ;
#19098=CARTESIAN_POINT ( 'NONE',  ( 4.000024251878889991, 24.52555747447230416, -0.7498250608958109131 ) ) ;
#19102=CARTESIAN_POINT ( 'NONE',  ( -2.388357610153000188, 28.61663313895000016, -0.6232602838477999674 ) ) ;
#19104=CARTESIAN_POINT ( 'NONE',  ( 2.124360424174371431, 29.02695534453464532, -0.3899590626965727114 ) ) ;
#19107=ORIENTED_EDGE ( 'NONE', *, *, #18548, .T. ) ;
#19109=ORIENTED_EDGE ( 'NONE', *, *, #9534, .T. ) ;
#19113=DIRECTION ( 'NONE',  ( 0.000000000000000000, 1.000000000000000000, 0.000000000000000000 ) ) ;
#19121=CARTESIAN_POINT ( 'NONE',  ( 2.306244679868000080, 25.51903888322000213, -0.7375453083353000761 ) ) ;
#19124=ORIENTED_EDGE ( 'NONE', *, *, #17713, .F. ) ;
#19127=CARTESIAN_POINT ( 'NONE',  ( -2.408156795220000479, 29.83799085022999975, 1.318887963389000051 ) ) ;
#19131=VECTOR ( 'NONE', #20489, 1000.000000000000000 ) ;
#19134=DIRECTION ( 'NONE',  ( 0.000000000000000000, 1.000000000000000000, 0.000000000000000000 ) ) ;
#19138=CARTESIAN_POINT ( 'NONE',  ( -4.750000000000000000, 22.19999999999999574, 0.000000000000000000 ) ) ;
#19140=CARTESIAN_POINT ( 'NONE',  ( 2.147292731478545935, 24.17747261322704233, 0.4479935266175709141 ) ) ;
#19144=PLANE ( 'NONE',  #12906 ) ;
#19146=DIRECTION ( 'NONE',  ( 0.000000000000000000, -1.000000000000000000, 0.000000000000000000 ) ) ;
#19151=FACE_BOUND ( 'NONE', #6951, .T. ) ;
#19152=EDGE_CURVE ( 'NONE', #2047, #6636, #19547, .T. ) ;
#19155=EDGE_CURVE ( 'NONE', #19300, #15250, #21479, .T. ) ;
#19156=CARTESIAN_POINT ( 'NONE',  ( 1.700000000000000622, 12.91217734593225863, -1.053565373075000977 ) ) ;
#19162=CONICAL_SURFACE ( 'NONE', #12974, 4.674999979945999584, 0.7853981633972997312 ) ;
#19164=CARTESIAN_POINT ( 'NONE',  ( -2.122079233582688573, 29.37598636205398961, -0.4706325729297383687 ) ) ;
#19165=EDGE_CURVE ( 'NONE', #21798, #1224, #18374, .T. ) ;
#19168=CARTESIAN_POINT ( 'NONE',  ( -0.1537472993604999949, 23.39806608891999673, -2.073430105596999695 ) ) ;
#19169=EDGE_CURVE ( 'NONE', #17309, #2115, #12197, .T. ) ;
#19173=CARTESIAN_POINT ( 'NONE',  ( -2.151153546426574525, 24.62672406677130255, -0.7503138593518134947 ) ) ;
#19175=CARTESIAN_POINT ( 'NONE',  ( -2.125241982083288850, 30.86478522159566751, 0.2061377204366061922 ) ) ;
#19179=VECTOR ( 'NONE', #18517, 1000.000000000000000 ) ;
#19181=CARTESIAN_POINT ( 'NONE',  ( 0.000000000000000000, 24.80000000000000426, -4.618802153517000519 ) ) ;
#19183=ORIENTED_EDGE ( 'NONE', *, *, #3498, .T. ) ;
#19195=CARTESIAN_POINT ( 'NONE',  ( -2.106357140788216675, 30.17536992306000343, -0.4799468061218781223 ) ) ;
#19202=CIRCLE ( 'NONE', #23455, 4.649999999999999467 ) ;
#19205=DIRECTION ( 'NONE',  ( -1.000000000000000000, 0.000000000000000000, 0.000000000000000000 ) ) ;
#19210=CARTESIAN_POINT ( 'NONE',  ( -0.4182960933211564702, 28.60509501925429277, 2.130789602436458541 ) ) ;
#19211=AXIS2_PLACEMENT_3D ( 'NONE', #16908, #11358, #82 ) ;
#19222=CARTESIAN_POINT ( 'NONE',  ( -4.000000000000000000, 26.50000000000001066, -0.1857058784358549819 ) ) ;
#19223=CARTESIAN_POINT ( 'NONE',  ( 0.000000000000000000, 24.29999999999999716, -4.749999999999970690 ) ) ;
#19225=CARTESIAN_POINT ( 'NONE',  ( -1.236362846991004183, 26.50000008335574719, -2.171602059085420589 ) ) ;
#19228=CARTESIAN_POINT ( 'NONE',  ( -2.447990496630999768, 26.39000240010000198, -1.500144717171000064 ) ) ;
#19229=AXIS2_PLACEMENT_3D ( 'NONE', #14621, #5431, #12580 ) ;
#19231=CARTESIAN_POINT ( 'NONE',  ( 2.144482848013529619, 29.02030102469518980, -0.2779858083291430471 ) ) ;
#19240=LINE ( 'NONE', #19370, #14596 ) ;
#19245=CIRCLE ( 'NONE', #7650, 2.100000000000000089 ) ;
#19248=ORIENTED_EDGE ( 'NONE', *, *, #9835, .T. ) ;
#19250=CARTESIAN_POINT ( 'NONE',  ( -1.480915476144999854, 31.13702747345000077, -2.141804436516000276 ) ) ;
#19252=CARTESIAN_POINT ( 'NONE',  ( -2.261090823039999975, 23.59650489110000038, 0.2002084280613000145 ) ) ;
#19257=CARTESIAN_POINT ( 'NONE',  ( 1.867682715928999926, 29.47894642224000350, -2.012571957185000038 ) ) ;
#19262=CARTESIAN_POINT ( 'NONE',  ( -2.184465970885646424, 29.76753006952333180, -1.259047450927245126 ) ) ;
#19263=ORIENTED_EDGE ( 'NONE', *, *, #22523, .F. ) ;
#19265=CARTESIAN_POINT ( 'NONE',  ( 0.9658031675207989775, 24.49999999999999645, -2.222895075323709779 ) ) ;
#19266=ORIENTED_EDGE ( 'NONE', *, *, #9098, .T. ) ;
#19269=CARTESIAN_POINT ( 'NONE',  ( 0.000000000000000000, 14.90000000000000036, -4.724999999995984190 ) ) ;
#19270=CARTESIAN_POINT ( 'NONE',  ( 2.434931691670792819, 28.60086340285666751, 0.6543697108981857413 ) ) ;
#19283=ORIENTED_EDGE ( 'NONE', *, *, #7026, .F. ) ;
#19285=DIRECTION ( 'NONE',  ( -1.000000000000000000, 0.000000000000000000, 0.000000000000000000 ) ) ;
#19286=CARTESIAN_POINT ( 'NONE',  ( 0.000000000000000000, 30.84509624898000268, 0.000000000000000000 ) ) ;
#19290=DIRECTION ( 'NONE',  ( 0.000000000000000000, 0.000000000000000000, -1.000000000000000000 ) ) ;
#19292=DIRECTION ( 'NONE',  ( 1.000000000000000000, 0.000000000000000000, 0.000000000000000000 ) ) ;
#19293=ADVANCED_FACE ( 'NONE', ( #10545 ), #19507, .T. ) ;
#19294=AXIS2_PLACEMENT_3D ( 'NONE', #9782, #20566, #22613 ) ;
#19295=CARTESIAN_POINT ( 'NONE',  ( -2.044419059392999838, 29.44573095519140438, 0.6966517550941788706 ) ) ;
#19296=ORIENTED_EDGE ( 'NONE', *, *, #1121, .F. ) ;
#19297=CARTESIAN_POINT ( 'NONE',  ( -1.802597709787000069, 23.71057944035000276, 1.505962647774000018 ) ) ;
#19300=VERTEX_POINT ( 'NONE', #23614 ) ;
#19301=EDGE_CURVE ( 'NONE', #16017, #10983, #20023, .T. ) ;
#19304=CLOSED_SHELL ( 'NONE', ( #2109, #1430, #4082, #17508, #19623, #571 ) ) ;
#19311=CARTESIAN_POINT ( 'NONE',  ( 0.000000000000000000, 24.65000000000000213, 0.000000000000000000 ) ) ;
#19312=CIRCLE ( 'NONE', #14656, 2.750000000000000000 ) ;
#19317=CYLINDRICAL_SURFACE ( 'NONE', #9253, 4.750000000000000000 ) ;
#19319=AXIS2_PLACEMENT_3D ( 'NONE', #8604, #12481, #19508 ) ;
#19325=FACE_OUTER_BOUND ( 'NONE', #15860, .T. ) ;
#19326=CIRCLE ( 'NONE', #2635, 1.399999999999999911 ) ;
#19327=CYLINDRICAL_SURFACE ( 'NONE', #6764, 2.500000000000000000 ) ;
#19329=CARTESIAN_POINT ( 'NONE',  ( -1.951811984317841642, 30.14747925604160983, -0.9252638563299733221 ) ) ;
#19330=ORIENTED_EDGE ( 'NONE', *, *, #7908, .F. ) ;
#19335=EDGE_CURVE ( 'NONE', #11502, #19694, #12366, .T. ) ;
#19338=EDGE_CURVE ( 'NONE', #9790, #12389, #23011, .T. ) ;
#19344=CARTESIAN_POINT ( 'NONE',  ( -1.726962967392345671, 27.54490368590698779, -1.364955284461023322 ) ) ;
#19347=VERTEX_POINT ( 'NONE', #10785 ) ;
#19356=CARTESIAN_POINT ( 'NONE',  ( -2.189594054297049119, 28.61899650445837295, 0.2575912915343336329 ) ) ;
#19357=CARTESIAN_POINT ( 'NONE',  ( -1.259047450927242018, 26.76753006952333180, 2.184465970885648201 ) ) ;
#19358=CARTESIAN_POINT ( 'NONE',  ( 0.000000000000000000, 31.00000000000000000, 0.000000000000000000 ) ) ;
#19360=VERTEX_POINT ( 'NONE', #14520 ) ;
#19362=CARTESIAN_POINT ( 'NONE',  ( -2.153772461420000006, 28.71413313895000030, 1.206163983883000057 ) ) ;
#19368=ORIENTED_EDGE ( 'NONE', *, *, #936, .T. ) ;
#19370=CARTESIAN_POINT ( 'NONE',  ( 0.000000000000000000, 30.84509624898000268, -2.154903751016000069 ) ) ;
#19373=CARTESIAN_POINT ( 'NONE',  ( 2.184465970885644648, 27.10086340285666751, -1.259047450927249345 ) ) ;
#19379=CARTESIAN_POINT ( 'NONE',  ( 2.068822368684000157, 29.35017502063999828, -1.771798175640999951 ) ) ;
#19380=CARTESIAN_POINT ( 'NONE',  ( 1.883643770067999990, 23.87661750703000152, -1.956741025826999936 ) ) ;
#19382=ORIENTED_EDGE ( 'NONE', *, *, #8976, .T. ) ;
#19385=CARTESIAN_POINT ( 'NONE',  ( 1.772081371289000007, 29.26351976544000166, 2.097239190856999613 ) ) ;
#19386=DIRECTION ( 'NONE',  ( -1.000000000000000000, 0.000000000000000000, 0.000000000000000000 ) ) ;
#19394=ORIENTED_EDGE ( 'NONE', *, *, #22393, .T. ) ;
#19395=CARTESIAN_POINT ( 'NONE',  ( -0.7596549267136000205, 25.82419530016000309, 2.629617744858999906 ) ) ;
#19401=VERTEX_POINT ( 'NONE', #9310 ) ;
#19402=VERTEX_POINT ( 'NONE', #20561 ) ;
#19403=CARTESIAN_POINT ( 'NONE',  ( 1.999167105995457216, 30.15086340285667177, 1.536366799937278760 ) ) ;
#19405=CARTESIAN_POINT ( 'NONE',  ( 0.000000000000000000, 15.05000017415440006, 0.000000000000000000 ) ) ;
#19408=CARTESIAN_POINT ( 'NONE',  ( 1.699999998837999904, 12.90000000000000036, -1.053565373074999867 ) ) ;
#19414=CARTESIAN_POINT ( 'NONE',  ( -2.355489761170999952, 29.22512865352000233, 0.05855059890257999916 ) ) ;
#19418=CIRCLE ( 'NONE', #21743, 2.899999999999999911 ) ;
#19419=CARTESIAN_POINT ( 'NONE',  ( -2.067964573227998315, 29.44117847301367874, 0.6230106560362024259 ) ) ;
#19421=CARTESIAN_POINT ( 'NONE',  ( 2.183938845894000114, 24.79402139891000090, -0.09232374713782000308 ) ) ;
#19426=ADVANCED_FACE ( 'NONE', ( #18285 ), #22233, .T. ) ;
#19428=CIRCLE ( 'NONE', #18271, 3.100000000000000089 ) ;
#19437=CARTESIAN_POINT ( 'NONE',  ( 4.000000000000000000, 26.20000000000000284, -2.309401076759000304 ) ) ;
#19439=DIRECTION ( 'NONE',  ( -0.000000000000000000, -1.000000000000000000, -0.000000000000000000 ) ) ;
#19440=CONICAL_SURFACE ( 'NONE', #21779, 4.674999969225999585, 0.7853981633972997312 ) ;
#19444=ADVANCED_FACE ( 'NONE', ( #2152, #5789 ), #20448, .T. ) ;
#19445=PLANE ( 'NONE',  #22290 ) ;
#19447=CARTESIAN_POINT ( 'NONE',  ( -0.4393762720424915225, 26.31534065533142552, 4.365128144578328317 ) ) ;
#19448=CARTESIAN_POINT ( 'NONE',  ( 1.839173991642404138, 26.50000000000000355, 3.556954554355651776 ) ) ;
#19450=CARTESIAN_POINT ( 'NONE',  ( -1.801854931646215796, 30.12917346635381222, -1.194674909710682575 ) ) ;
#19454=CARTESIAN_POINT ( 'NONE',  ( -1.222626843528073604, 23.61650379099185670, -1.727787963671160165 ) ) ;
#19455=CARTESIAN_POINT ( 'NONE',  ( -2.217776889426126274, 24.45298137823828810, 0.3983591268742258107 ) ) ;
#19457=EDGE_CURVE ( 'NONE', #6384, #23625, #14146, .T. ) ;
#19462=DIRECTION ( 'NONE',  ( 1.000000000000000000, 0.000000000000000000, 0.000000000000000000 ) ) ;
#19470=EDGE_CURVE ( 'NONE', #5466, #12394, #23030, .T. ) ;
#19480=FACE_OUTER_BOUND ( 'NONE', #7153, .T. ) ;
#19481=CARTESIAN_POINT ( 'NONE',  ( -1.603077936557000038, 27.73913313894999888, -1.876963106047000007 ) ) ;
#19482=AXIS2_PLACEMENT_3D ( 'NONE', #6069, #4273, #17217 ) ;
#19484=B_SPLINE_CURVE_WITH_KNOTS ( 'NONE', 3,
 ( #16766, #294, #20774, #14945 ),
 .UNSPECIFIED., .F., .F.,
 ( 4, 4 ),
 ( 0.000000000000000000, 1.000000000000000000 ),
 .UNSPECIFIED. ) ;
#19486=CARTESIAN_POINT ( 'NONE',  ( 2.411379030285999647, 28.19187716036000069, 0.4306175354954999701 ) ) ;
#19488=EDGE_CURVE ( 'NONE', #23321, #2821, #10508, .T. ) ;
#19491=DIRECTION ( 'NONE',  ( 1.000000000000000000, 0.000000000000000000, 0.000000000000000000 ) ) ;
#19502=CARTESIAN_POINT ( 'NONE',  ( 2.330854569989000424, 30.66143933041000125, -0.2259880098311999874 ) ) ;
#19505=B_SPLINE_CURVE_WITH_KNOTS ( 'NONE', 3,
 ( #17233, #636, #20637, #8036, #2108, #162, #4048, #7552, #5623, #20407 ),
 .UNSPECIFIED., .F., .F.,
 ( 4, 2, 2, 2, 4 ),
 ( 0.000000000000000000, 0.2500000000000000000, 0.5000000000000000000, 0.7500000000000000000, 1.000000000000000000 ),
 .UNSPECIFIED. ) ;
#19506=ORIENTED_EDGE ( 'NONE', *, *, #10987, .T. ) ;
#19507=CYLINDRICAL_SURFACE ( 'NONE', #12575, 4.750000000000000000 ) ;
#19508=DIRECTION ( 'NONE',  ( 0.000000000000000000, 0.000000000000000000, -1.000000000000000000 ) ) ;
#19510=CARTESIAN_POINT ( 'NONE',  ( 0.000000000000000000, 26.50000000000000355, 0.000000000000000000 ) ) ;
#19512=DIRECTION ( 'NONE',  ( 1.000000000000000000, 0.000000000000000000, 0.000000000000000000 ) ) ;
#19515=DIRECTION ( 'NONE',  ( 0.000000000000000000, 1.000000000000000000, 0.000000000000000000 ) ) ;
#19516=ORIENTED_EDGE ( 'NONE', *, *, #20897, .F. ) ;
#19519=ORIENTED_EDGE ( 'NONE', *, *, #18855, .F. ) ;
#19520=CARTESIAN_POINT ( 'NONE',  ( 1.815435739943000115, 24.25568479955999734, 1.783857804741999953 ) ) ;
#19521=CARTESIAN_POINT ( 'NONE',  ( -1.376955291490763233, 24.71727056350960794, 1.708239419793794456 ) ) ;
#19523=AXIS2_PLACEMENT_3D ( 'NONE', #11712, #431, #7832 ) ;
#19527=ORIENTED_EDGE ( 'NONE', *, *, #16950, .T. ) ;
#19530=CARTESIAN_POINT ( 'NONE',  ( 3.824747490998164245, 24.75094615491877548, 2.410583160007404580 ) ) ;
#19535=CARTESIAN_POINT ( 'NONE',  ( 2.000000000000000000, 18.27087121525220681, 1.096451616434099242E-10 ) ) ;
#19544=CARTESIAN_POINT ( 'NONE',  ( -2.071691020321107857, 29.44040781721670186, 0.6104882387633735474 ) ) ;
#19545=ORIENTED_EDGE ( 'NONE', *, *, #6527, .T. ) ;
#19547=CIRCLE ( 'NONE', #9096, 4.750000000000000000 ) ;
#19549=ORIENTED_EDGE ( 'NONE', *, *, #12449, .T. ) ;
#19554=EDGE_CURVE ( 'NONE', #8792, #19900, #9663, .T. ) ;
#19557=CARTESIAN_POINT ( 'NONE',  ( 0.000000000000000000, 24.50000000000000000, 0.000000000000000000 ) ) ;
#19558=CARTESIAN_POINT ( 'NONE',  ( -2.500000000000000444, 27.18333333333333357, -0.3272492347489320275 ) ) ;
#19561=DIRECTION ( 'NONE',  ( 0.000000000000000000, 1.000000000000000000, 0.000000000000000000 ) ) ;
#19571=CARTESIAN_POINT ( 'NONE',  ( -1.722646045537596704, 30.12122296660216847, -1.303888318235613353 ) ) ;
#19576=LINE ( 'NONE', #14115, #7208 ) ;
#19579=VECTOR ( 'NONE', #37, 1000.000000000000114 ) ;
#19586=CARTESIAN_POINT ( 'NONE',  ( -4.000000000000073719, 24.70197603011089527, -1.905018119001588683 ) ) ;
#19587=CARTESIAN_POINT ( 'NONE',  ( 0.5551539414043799026, 26.26248452079970619, 2.089084675604010233 ) ) ;
#19590=CARTESIAN_POINT ( 'NONE',  ( -1.767805011140364924, 26.50018596745192312, 1.767686163102024643 ) ) ;
#19599=AXIS2_PLACEMENT_3D ( 'NONE', #23484, #15721, #12476 ) ;
#19604=CARTESIAN_POINT ( 'NONE',  ( 1.403495832404999977, 26.65869850838000232, -1.780325977227999790 ) ) ;
#19608=CARTESIAN_POINT ( 'NONE',  ( 1.732076717456000114, 27.31437716035999941, 1.732076717456000114 ) ) ;
#19610=ORIENTED_EDGE ( 'NONE', *, *, #18134, .F. ) ;
#19617=DIRECTION ( 'NONE',  ( -5.702245064659998234E-10, 0.9999999999999997780, 2.283934677740999354E-08 ) ) ;
#19618=CARTESIAN_POINT ( 'NONE',  ( -2.213186668863544426, 30.78310712015282036, -0.2500141473247705082 ) ) ;
#19623=ADVANCED_FACE ( 'NONE', ( #4092 ), #9502, .F. ) ;
#19625=CARTESIAN_POINT ( 'NONE',  ( 1.795439626675999989, 29.15163585920999978, 2.048365916996000458 ) ) ;
#19628=EDGE_LOOP ( 'NONE', ( #22802, #8963, #17668, #21109, #1345, #3384 ) ) ;
#19629=CIRCLE ( 'NONE', #22302, 2.399999999999999911 ) ;
#19632=CARTESIAN_POINT ( 'NONE',  ( 4.000000000000000000, 24.80000000000000426, -2.309401076759000304 ) ) ;
#19636=CARTESIAN_POINT ( 'NONE',  ( 0.000000000000000000, 18.50000000000000000, 0.000000000000000000 ) ) ;
#19639=CARTESIAN_POINT ( 'NONE',  ( -0.9538268690393967297, 30.53169873023693626, 2.326930193732148044 ) ) ;
#19641=ORIENTED_EDGE ( 'NONE', *, *, #17364, .F. ) ;
#19646=CIRCLE ( 'NONE', #266, 4.549999999999999822 ) ;
#19649=ORIENTED_EDGE ( 'NONE', *, *, #6404, .F. ) ;
#19650=CARTESIAN_POINT ( 'NONE',  ( 2.500000000000000000, 30.23419673619000037, 0.000000000000000000 ) ) ;
#19651=CARTESIAN_POINT ( 'NONE',  ( 0.2258413948657297943, 26.24995681965566519, 2.153052638588166978 ) ) ;
#19660=CARTESIAN_POINT ( 'NONE',  ( 1.181632374602280988, 24.55137445130629104, 3.936586548167761990 ) ) ;
#19665=B_SPLINE_CURVE_WITH_KNOTS ( 'NONE', 3,
 ( #534, #5877, #15305, #22819, #4182, #18835, #9635, #9872, #7700, #22585 ),
 .UNSPECIFIED., .F., .F.,
 ( 4, 1, 1, 2, 2, 4 ),
 ( 0.000000000000000000, 0.2499999999999969469, 0.3749999999999960032, 0.4374999999999962252, 0.4999999999999963363, 1.000000000000000000 ),
 .UNSPECIFIED. ) ;
#19667=CARTESIAN_POINT ( 'NONE',  ( -2.071136996602504610, 29.44052298352770691, 0.6123601400604211653 ) ) ;
#19672=AXIS2_PLACEMENT_3D ( 'NONE', #10547, #12482, #14830 ) ;
#19678=ORIENTED_EDGE ( 'NONE', *, *, #4145, .F. ) ;
#19683=FACE_OUTER_BOUND ( 'NONE', #1317, .T. ) ;
#19688=AXIS2_PLACEMENT_3D ( 'NONE', #4363, #22525, #7878 ) ;
#19693=CARTESIAN_POINT ( 'NONE',  ( -1.270048396745602881, 30.32394092141509745, 1.751222398791842050 ) ) ;
#19694=VERTEX_POINT ( 'NONE', #19223 ) ;
#19695=CARTESIAN_POINT ( 'NONE',  ( -1.727993674177999983, 25.50834080394000125, 1.571450918520000073 ) ) ;
#19706=AXIS2_PLACEMENT_3D ( 'NONE', #1094, #15735, #12005 ) ;
#19710=VECTOR ( 'NONE', #17040, 1000.000000000000000 ) ;
#19716=CIRCLE ( 'NONE', #8492, 3.050000000000000266 ) ;
#19725=EDGE_CURVE ( 'NONE', #18459, #8533, #8999, .T. ) ;
#19730=CARTESIAN_POINT ( 'NONE',  ( -0.6232602838478999985, 26.08163313895000002, -2.388357610153000188 ) ) ;
#19731=AXIS2_PLACEMENT_3D ( 'NONE', #19358, #10394, #10149 ) ;
#19732=VECTOR ( 'NONE', #18633, 1000.000000000000000 ) ;
#19736=EDGE_LOOP ( 'NONE', ( #17587, #16042 ) ) ;
#19748=CARTESIAN_POINT ( 'NONE',  ( -1.377056188230000089, 31.03159284288000208, -1.991595807317999789 ) ) ;
#19749=CARTESIAN_POINT ( 'NONE',  ( -0.3780989064092999952, 23.55641193502999897, 2.689602506303999885 ) ) ;
#19751=AXIS2_PLACEMENT_3D ( 'NONE', #21531, #4947, #22964 ) ;
#19753=CARTESIAN_POINT ( 'NONE',  ( 0.000000000000000000, 24.40000007355299871, -4.649999926447000220 ) ) ;
#19757=FACE_OUTER_BOUND ( 'NONE', #274, .T. ) ;
#19763=CARTESIAN_POINT ( 'NONE',  ( 0.4901246258882320794, 30.57924682558974538, 2.417188095590464325 ) ) ;
#19764=CARTESIAN_POINT ( 'NONE',  ( 0.000000000000000000, 24.80000000000000426, -4.618802153517000519 ) ) ;
#19766=CARTESIAN_POINT ( 'NONE',  ( -2.308536264861000387, 25.47398547997000051, 0.4564140279980999915 ) ) ;
#19773=EDGE_LOOP ( 'NONE', ( #7139, #4158, #8745 ) ) ;
#19774=DIRECTION ( 'NONE',  ( 0.000000000000000000, 0.000000000000000000, -1.000000000000000000 ) ) ;
#19775=AXIS2_PLACEMENT_3D ( 'NONE', #6790, #10800, #14061 ) ;
#19776=CARTESIAN_POINT ( 'NONE',  ( -0.7632405811354259217, 26.22308743037562095, 1.985132959746883641 ) ) ;
#19778=VERTEX_POINT ( 'NONE', #6545 ) ;
#19783=EDGE_CURVE ( 'NONE', #3685, #20723, #578, .T. ) ;
#19784=CARTESIAN_POINT ( 'NONE',  ( -2.034154838984999714, 30.92025618834000156, 0.4889338487552999934 ) ) ;
#19790=EDGE_LOOP ( 'NONE', ( #16526, #8579, #11214, #9807 ) ) ;
#19803=CARTESIAN_POINT ( 'NONE',  ( 3.316314694148171149, 24.62756664670258644, -2.704122461039530023 ) ) ;
#19807=CARTESIAN_POINT ( 'NONE',  ( -2.817565069457256932, 26.44682129341587995, 2.992080202207100470 ) ) ;
#19810=CARTESIAN_POINT ( 'NONE',  ( -0.7072731918244000715, 30.87462362680000183, -2.070837331812999782 ) ) ;
#19813=CARTESIAN_POINT ( 'NONE',  ( 0.8452009350949196698, 29.95273695107458067, -1.987689021054610317 ) ) ;
#19818=DIRECTION ( 'NONE',  ( -1.000000000000000000, 0.000000000000000000, 0.000000000000000000 ) ) ;
#19836=CARTESIAN_POINT ( 'NONE',  ( 1.986040474371530085, 27.34694121629901886, 0.9569010413172605034 ) ) ;
#19838=FACE_OUTER_BOUND ( 'NONE', #6621, .T. ) ;
#19842=CARTESIAN_POINT ( 'NONE',  ( 2.445091418594000032, 26.66663313895000087, -0.3381971108622000011 ) ) ;
#19843=AXIS2_PLACEMENT_3D ( 'NONE', #6677, #21821, #20129 ) ;
#19844=CARTESIAN_POINT ( 'NONE',  ( -1.923654546119000219, 27.89937716036000381, 1.516486965307999979 ) ) ;
#19846=ORIENTED_EDGE ( 'NONE', *, *, #9515, .F. ) ;
#19851=ORIENTED_EDGE ( 'NONE', *, *, #3091, .T. ) ;
#19852=ADVANCED_FACE ( 'NONE', ( #15370 ), #13439, .T. ) ;
#19858=EDGE_LOOP ( 'NONE', ( #5337, #11685, #11553, #17942 ) ) ;
#19860=CARTESIAN_POINT ( 'NONE',  ( -1.418793962560999988, 30.13200156660999696, -1.863054310995999829 ) ) ;
#19864=CARTESIAN_POINT ( 'NONE',  ( 0.000000000000000000, 22.00000000000000000, 0.000000000000000000 ) ) ;
#19865=FACE_OUTER_BOUND ( 'NONE', #3454, .T. ) ;
#19867=ADVANCED_FACE ( 'NONE', ( #4739 ), #19162, .T. ) ;
#19870=CARTESIAN_POINT ( 'NONE',  ( -2.000000000000000000, 24.50000000000000000, 3.464101615137999968 ) ) ;
#19871=DIRECTION ( 'NONE',  ( -1.000000000000000000, 0.000000000000000000, 0.000000000000000000 ) ) ;
#19872=CARTESIAN_POINT ( 'NONE',  ( 0.000000000000000000, -1.550000000000000044, 0.000000000000000000 ) ) ;
#19878=CARTESIAN_POINT ( 'NONE',  ( 0.4021391122705000321, 24.53436591766000063, -2.513213003584999772 ) ) ;
#19881=VECTOR ( 'NONE', #18355, 1000.000000000000000 ) ;
#19883=CARTESIAN_POINT ( 'NONE',  ( 2.500000000000000000, 27.61666666666666714, -0.3272492347489370235 ) ) ;
#19885=CARTESIAN_POINT ( 'NONE',  ( -0.9242717917835999719, 23.66000000000000014, -1.952260652400999996 ) ) ;
#19887=CARTESIAN_POINT ( 'NONE',  ( 0.6543697108982093891, 30.06753006952333607, 2.434931691670787490 ) ) ;
#19894=CARTESIAN_POINT ( 'NONE',  ( -3.000000000000000000, 16.89999999999999858, 0.000000000000000000 ) ) ;
#19896=CARTESIAN_POINT ( 'NONE',  ( -2.070379988957000261, 30.04886011138000157, 1.133895954157000174 ) ) ;
#19900=VERTEX_POINT ( 'NONE', #13679 ) ;
#19903=AXIS2_PLACEMENT_3D ( 'NONE', #18472, #1883, #3478 ) ;
#19904=DIRECTION ( 'NONE',  ( 0.000000000000000000, -1.000000000000000000, 0.000000000000000000 ) ) ;
#19905=FACE_OUTER_BOUND ( 'NONE', #691, .T. ) ;
#19910=DIRECTION ( 'NONE',  ( -1.000000000000000000, 0.000000000000000000, 0.000000000000000000 ) ) ;
#19913=EDGE_CURVE ( 'NONE', #6330, #20095, #8742, .T. ) ;
#19915=ORIENTED_EDGE ( 'NONE', *, *, #17973, .F. ) ;
#19925=CARTESIAN_POINT ( 'NONE',  ( 0.1890102160836000245, 30.42465970005999765, 2.335336163465000059 ) ) ;
#19927=AXIS2_PLACEMENT_3D ( 'NONE', #1747, #14576, #1394 ) ;
#19929=CARTESIAN_POINT ( 'NONE',  ( 1.691637037686638312, 29.88931209851202908, -1.343040514645775341 ) ) ;
#19942=CARTESIAN_POINT ( 'NONE',  ( 1.499758741878467250, 26.53402357736653627, -1.612855151721995117 ) ) ;
#19944=CARTESIAN_POINT ( 'NONE',  ( 0.000000000000000000, 26.50000000000000355, 0.000000000000000000 ) ) ;
#19945=VERTEX_POINT ( 'NONE', #16227 ) ;
#19950=DIRECTION ( 'NONE',  ( 0.000000000000000000, 1.000000000000000000, 0.000000000000000000 ) ) ;
#19954=CARTESIAN_POINT ( 'NONE',  ( 1.787816191774978414, 26.68441241925206597, -1.290061143064831883 ) ) ;
#19955=CARTESIAN_POINT ( 'NONE',  ( -1.864615697012000028, 27.95000240010000070, -2.183184479328999839 ) ) ;
#19956=CARTESIAN_POINT ( 'NONE',  ( 1.712608848029143926, 30.68724016082039796, -1.316683541910883104 ) ) ;
#19960=CARTESIAN_POINT ( 'NONE',  ( 0.4858445502738999999, 28.31619850838000119, -2.214344957515000267 ) ) ;
#19962=CARTESIAN_POINT ( 'NONE',  ( -1.662740336262000129, 27.11937716036000268, 1.798742361870000028 ) ) ;
#19970=CARTESIAN_POINT ( 'NONE',  ( -0.6543697108981503252, 24.16666666666667140, 2.434931691670802145 ) ) ;
#19971=CARTESIAN_POINT ( 'NONE',  ( 0.000000000000000000, 26.50000000000000355, 0.000000000000000000 ) ) ;
#19978=CARTESIAN_POINT ( 'NONE',  ( 0.7871505218098000523, 29.20548547997000099, -2.205525275559999887 ) ) ;
#19981=ORIENTED_EDGE ( 'NONE', *, *, #19155, .T. ) ;
#19983=DIRECTION ( 'NONE',  ( 1.000000000000000000, 0.000000000000000000, 0.000000000000000000 ) ) ;
#19985=CARTESIAN_POINT ( 'NONE',  ( 2.949999988794999695, 24.49999998879500041, 5.832342955284000153E-08 ) ) ;
#19986=CARTESIAN_POINT ( 'NONE',  ( -4.649999999999999467, 17.00000000000000000, 0.000000000000000000 ) ) ;
#19987=CARTESIAN_POINT ( 'NONE',  ( -3.649794085728322202, 24.70197603011190424, 2.511592555635381974 ) ) ;
#19989=EDGE_CURVE ( 'NONE', #3305, #5391, #1341, .T. ) ;
#19991=VERTEX_POINT ( 'NONE', #18056 ) ;
#19992=CARTESIAN_POINT ( 'NONE',  ( -1.409459525220179810, 30.51584936511932611, 2.103659993609944490 ) ) ;
#19995=EDGE_LOOP ( 'NONE', ( #3747, #1697, #18402, #5665 ) ) ;
#19996=CARTESIAN_POINT ( 'NONE',  ( 2.285327255250000356, 25.99744178769000058, -0.8000105884810000401 ) ) ;
#19997=CARTESIAN_POINT ( 'NONE',  ( 0.000000000000000000, -1.550000000000000044, 0.000000000000000000 ) ) ;
#20000=FACE_OUTER_BOUND ( 'NONE', #8803, .T. ) ;
#20004=AXIS2_PLACEMENT_3D ( 'NONE', #8711, #6640, #12466 ) ;
#20005=CARTESIAN_POINT ( 'NONE',  ( 1.699986957659999964, 9.000014576061998284, -0.8485216275457999613 ) ) ;
#20009=CARTESIAN_POINT ( 'NONE',  ( -1.018972323971000016, 25.15353811475999990, -1.887072216533999924 ) ) ;
#20013=CARTESIAN_POINT ( 'NONE',  ( -2.042556580646999631, 30.83875785297000149, 0.9163512981227001086 ) ) ;
#20020=CARTESIAN_POINT ( 'NONE',  ( -1.536366799937290084, 29.48333333333333428, -1.999167105995448113 ) ) ;
#20023=B_SPLINE_CURVE_WITH_KNOTS ( 'NONE', 3,
 ( #4855, #8603, #21565, #8726, #6777, #14169 ),
 .UNSPECIFIED., .F., .F.,
 ( 4, 2, 4 ),
 ( 0.002491295001356702652, 0.003048372566543609916, 0.003605450131730517181 ),
 .UNSPECIFIED. ) ;
#20024=ORIENTED_EDGE ( 'NONE', *, *, #9047, .F. ) ;
#20031=EDGE_CURVE ( 'NONE', #1813, #11130, #6402, .T. ) ;
#20032=EDGE_LOOP ( 'NONE', ( #2739, #16516, #19028, #16306 ) ) ;
#20045=CARTESIAN_POINT ( 'NONE',  ( 2.284685590549000000, 28.98591928658000327, 0.5193202084365000637 ) ) ;
#20047=ADVANCED_FACE ( 'NONE', ( #4860 ), #4076, .F. ) ;
#20048=CARTESIAN_POINT ( 'NONE',  ( 2.036831998448072500, 29.84739247495543779, -0.7268712922005031718 ) ) ;
#20057=VERTEX_POINT ( 'NONE', #16689 ) ;
#20058=ADVANCED_FACE ( 'NONE', ( #16574 ), #11257, .T. ) ;
#20059=DIRECTION ( 'NONE',  ( 0.000000000000000000, 0.000000000000000000, -1.000000000000000000 ) ) ;
#20063=LINE ( 'NONE', #21992, #6326 ) ;
#20065=ORIENTED_EDGE ( 'NONE', *, *, #936, .F. ) ;
#20074=CARTESIAN_POINT ( 'NONE',  ( -2.169831354736061702, 27.79746079784813162, -0.1190495946757019197 ) ) ;
#20075=VECTOR ( 'NONE', #8037, 1000.000000000000000 ) ;
#20078=CARTESIAN_POINT ( 'NONE',  ( 1.139984784021916608, 30.73313778691811748, -1.836321495231491463 ) ) ;
#20082=CARTESIAN_POINT ( 'NONE',  ( 1.611535839303107176, 26.30674319040050335, 1.527120279818484194 ) ) ;
#20084=CARTESIAN_POINT ( 'NONE',  ( -0.3140912549738999471, 27.77114211382000164, 2.270811333173000435 ) ) ;
#20086=VERTEX_POINT ( 'NONE', #3867 ) ;
#20093=AXIS2_PLACEMENT_3D ( 'NONE', #21754, #18003, #5167 ) ;
#20095=VERTEX_POINT ( 'NONE', #22039 ) ;
#20096=CARTESIAN_POINT ( 'NONE',  ( 2.500000000000000000, 24.40000000000000213, 0.000000000000000000 ) ) ;
#20103=CARTESIAN_POINT ( 'NONE',  ( -0.3357239997244999552, 28.83046706394999958, 2.247102726245999715 ) ) ;
#20104=CARTESIAN_POINT ( 'NONE',  ( 0.000000000000000000, 13.10000000000000142, 0.000000000000000000 ) ) ;
#20107=ORIENTED_EDGE ( 'NONE', *, *, #4806, .F. ) ;
#20115=CARTESIAN_POINT ( 'NONE',  ( -0.2348186520982191716, 29.21777802950449043, -2.147017149994515872 ) ) ;
#20118=CARTESIAN_POINT ( 'NONE',  ( 2.321942789092308779, 23.87531119754747522, 0.5770122056809254829 ) ) ;
#20120=CIRCLE ( 'NONE', #13912, 2.000000000000000000 ) ;
#20121=CARTESIAN_POINT ( 'NONE',  ( 0.5283825141746999465, 23.97514525888999870, 2.095676833831000341 ) ) ;
#20122=CARTESIAN_POINT ( 'NONE',  ( 1.536366799937295413, 28.28333333333333499, 1.999167105995444338 ) ) ;
#20129=DIRECTION ( 'NONE',  ( -1.000000000000000000, 0.000000000000000000, 0.000000000000000000 ) ) ;
#20130=FACE_OUTER_BOUND ( 'NONE', #17733, .T. ) ;
#20133=CARTESIAN_POINT ( 'NONE',  ( -0.3063878209169000333, 25.36830905619000021, 2.314903654952999990 ) ) ;
#20139=LINE ( 'NONE', #3547, #10011 ) ;
#20141=B_SPLINE_CURVE_WITH_KNOTS ( 'NONE', 3,
 ( #7727, #22488, #15335, #20446, #13170, #13283, #22372, #13049, #17162, #2035, #557, #7842, #2507, #7477, #11606, #5897 ),
 .UNSPECIFIED., .F., .F.,
 ( 4, 2, 2, 2, 2, 2, 2, 4 ),
 ( 0.000000000000000000, 0.2500000000000000000, 0.3750000000000000000, 0.4375000000000000000, 0.4687500000000000000, 0.5000000000000000000, 0.7500000000000000000, 1.000000000000000000 ),
 .UNSPECIFIED. ) ;
#20142=EDGE_LOOP ( 'NONE', ( #1752, #7829, #9763, #17788 ) ) ;
#20147=CARTESIAN_POINT ( 'NONE',  ( 1.980818591402529361, 30.73245735271817836, -1.143255368690362150 ) ) ;
#20151=CARTESIAN_POINT ( 'NONE',  ( 2.429928970624000151, 27.96256359723999907, 0.4339301335947000626 ) ) ;
#20162=CARTESIAN_POINT ( 'NONE',  ( 0.5113872014135000255, 30.80268660612999909, -2.127704381286000146 ) ) ;
#20166=CARTESIAN_POINT ( 'NONE',  ( 2.110692983767971764, 29.83106853030913186, -0.4604840047560345151 ) ) ;
#20168=CARTESIAN_POINT ( 'NONE',  ( -2.169404915079000240, 24.61931165514999975, -0.2292880595415000000 ) ) ;
#20174=ORIENTED_EDGE ( 'NONE', *, *, #2998, .T. ) ;
#20177=CARTESIAN_POINT ( 'NONE',  ( 2.504532394112000003E-14, 28.43419673618999965, 2.500000000000000000 ) ) ;
#20182=CARTESIAN_POINT ( 'NONE',  ( 2.500000000000000000, 24.40000000000000213, 0.000000000000000000 ) ) ;
#20187=CARTESIAN_POINT ( 'NONE',  ( -1.712953330202006796, 27.71795734230703445, -1.393201056469692611 ) ) ;
#20190=CARTESIAN_POINT ( 'NONE',  ( 1.602509900017840216, 30.69733188989498274, -1.449043562559991338 ) ) ;
#20191=ORIENTED_EDGE ( 'NONE', *, *, #6382, .T. ) ;
#20197=CARTESIAN_POINT ( 'NONE',  ( 0.4700916780637000580, 28.86021896306000301, 2.089231778180999921 ) ) ;
#20204=CARTESIAN_POINT ( 'NONE',  ( 2.220102258368206183, 28.80150489129345814, 0.5102462943910046622 ) ) ;
#20206=EDGE_CURVE ( 'NONE', #13196, #3402, #23840, .T. ) ;
#20209=DIRECTION ( 'NONE',  ( 0.000000000000000000, -1.000000000000000000, 0.000000000000000000 ) ) ;
#20214=CARTESIAN_POINT ( 'NONE',  ( 1.778641839820999992, 29.13930575949000001, -1.523279337374999987 ) ) ;
#20218=EDGE_LOOP ( 'NONE', ( #2101, #7807, #12267 ) ) ;
#20221=EDGE_CURVE ( 'NONE', #8499, #10321, #10763, .T. ) ;
#20223=EDGE_CURVE ( 'NONE', #6590, #17924, #17241, .T. ) ;
#20226=DIRECTION ( 'NONE',  ( 0.000000000000000000, -1.000000000000000000, 0.000000000000000000 ) ) ;
#20227=CARTESIAN_POINT ( 'NONE',  ( 0.3048288769163433609, 29.18568722789423475, -2.138368886124048629 ) ) ;
#20230=CARTESIAN_POINT ( 'NONE',  ( 1.940453181907765057, 23.84595057970013343, 1.348463719542498440 ) ) ;
#20232=CARTESIAN_POINT ( 'NONE',  ( 1.940602815664000058, 25.78657252654999965, -0.6793350042104999709 ) ) ;
#20233=CARTESIAN_POINT ( 'NONE',  ( 0.000000000000000000, 24.65000000000000213, 0.000000000000000000 ) ) ;
#20234=CYLINDRICAL_SURFACE ( 'NONE', #3401, 2.000000000000000000 ) ;
#20235=VECTOR ( 'NONE', #15756, 1000.000000000000000 ) ;
#20237=DIRECTION ( 'NONE',  ( 0.000000000000000000, 1.000000000000000000, 0.000000000000000000 ) ) ;
#20240=ORIENTED_EDGE ( 'NONE', *, *, #20221, .T. ) ;
#20246=CARTESIAN_POINT ( 'NONE',  ( 2.132304841933000183, 25.62447351380000171, -0.6819187252057000714 ) ) ;
#20250=CARTESIAN_POINT ( 'NONE',  ( 1.526121187041999949, 28.78992591556999869, 1.539885762186999907 ) ) ;
#20262=DIRECTION ( 'NONE',  ( 0.000000000000000000, 1.000000000000000000, 0.000000000000000000 ) ) ;
#20266=CARTESIAN_POINT ( 'NONE',  ( 0.6153010951426000075, 27.94669433610000198, -2.804372049896000085 ) ) ;
#20271=CARTESIAN_POINT ( 'NONE',  ( 4.649999849441000421, 22.00000015055399771, -6.648422772555000414E-08 ) ) ;
#20277=FACE_OUTER_BOUND ( 'NONE', #13238, .T. ) ;
#20280=CARTESIAN_POINT ( 'NONE',  ( 1.352523426442719501, 29.91753472705243766, -1.683999728453754674 ) ) ;
#20282=CARTESIAN_POINT ( 'NONE',  ( 1.961934450082000181, 25.63159458490000020, -0.6881597550252999129 ) ) ;
#20289=EDGE_LOOP ( 'NONE', ( #9143, #19382, #23698, #4754 ) ) ;
#20291=ORIENTED_EDGE ( 'NONE', *, *, #14578, .F. ) ;
#20295=ADVANCED_FACE ( 'NONE', ( #15802 ), #20721, .F. ) ;
#20297=CARTESIAN_POINT ( 'NONE',  ( 2.184730091557438136, 24.46663824537979082, -1.258552818647198146 ) ) ;
#20298=AXIS2_PLACEMENT_3D ( 'NONE', #16119, #3311, #15879 ) ;
#20306=CARTESIAN_POINT ( 'NONE',  ( 1.967353437452023623, 30.65813742271244635, -0.8921482303055430219 ) ) ;
#20308=CYLINDRICAL_SURFACE ( 'NONE', #20828, 2.750000000000000000 ) ;
#20310=EDGE_CURVE ( 'NONE', #5650, #367, #22571, .T. ) ;
#20312=CARTESIAN_POINT ( 'NONE',  ( -0.3134588398365999451, 28.01521896306000059, 2.266239109532000029 ) ) ;
#20313=CARTESIAN_POINT ( 'NONE',  ( 0.000000000000000000, 8.900000000000000355, 0.000000000000000000 ) ) ;
#20314=ORIENTED_EDGE ( 'NONE', *, *, #19989, .F. ) ;
#20317=CARTESIAN_POINT ( 'NONE',  ( -1.009755838453245902, 29.08874043368814810, -2.041968248507524564 ) ) ;
#20319=EDGE_CURVE ( 'NONE', #9272, #2748, #18041, .T. ) ;
#20320=CARTESIAN_POINT ( 'NONE',  ( 4.000000000000000000, 26.20000000000000284, 2.309401076759000304 ) ) ;
#20324=CARTESIAN_POINT ( 'NONE',  ( 0.9055761032497999796, 30.68836414079000008, -1.950832896806000027 ) ) ;
#20329=EDGE_CURVE ( 'NONE', #9720, #1224, #16161, .T. ) ;
#20330=DIRECTION ( 'NONE',  ( 0.000000000000000000, -1.000000000000000000, 0.000000000000000000 ) ) ;
#20334=DIRECTION ( 'NONE',  ( 0.000000000000000000, 1.000000000000000000, 0.000000000000000000 ) ) ;
#20337=CARTESIAN_POINT ( 'NONE',  ( -0.7609346232008592503, 29.24959062363414475, -2.021388052729749418 ) ) ;
#20342=VERTEX_POINT ( 'NONE', #6972 ) ;
#20343=CARTESIAN_POINT ( 'NONE',  ( -0.04029237313626999467, 24.84695296423999977, 2.352876976275999787 ) ) ;
#20346=CIRCLE ( 'NONE', #21102, 3.000000000000000000 ) ;
#20355=DIRECTION ( 'NONE',  ( -1.000000000000000000, 0.000000000000000000, 0.000000000000000000 ) ) ;
#20356=CARTESIAN_POINT ( 'NONE',  ( 0.000000000000000000, -1.550000000000000044, 0.000000000000000000 ) ) ;
#20359=CARTESIAN_POINT ( 'NONE',  ( -0.8815400351514000032, 24.53577456897999909, 2.162298408882000089 ) ) ;
#20363=CARTESIAN_POINT ( 'NONE',  ( -1.942407726809000090, 30.58970545120000040, -1.656974607114999998 ) ) ;
#20366=AXIS2_PLACEMENT_3D ( 'NONE', #21609, #23532, #5026 ) ;
#20367=CIRCLE ( 'NONE', #16483, 3.000000000000000000 ) ;
#20368=LINE ( 'NONE', #13319, #18532 ) ;
#20369=ADVANCED_FACE ( 'NONE', ( #16039 ), #16462, .T. ) ;
#20379=CIRCLE ( 'NONE', #9925, 4.000000000000000000 ) ;
#20382=CARTESIAN_POINT ( 'NONE',  ( 0.4693273880718999980, 26.10212896667000138, 2.628147087956000050 ) ) ;
#20384=ORIENTED_EDGE ( 'NONE', *, *, #21326, .T. ) ;
#20396=CARTESIAN_POINT ( 'NONE',  ( -0.7084080111906999599, 28.54437317801999896, 1.954714486706000010 ) ) ;
#20399=CARTESIAN_POINT ( 'NONE',  ( 0.9753730088590640834, 29.66360326960658611, 1.927051000882559428 ) ) ;
#20400=EDGE_LOOP ( 'NONE', ( #9356, #5750, #6029 ) ) ;
#20401=CARTESIAN_POINT ( 'NONE',  ( -1.194990091485000017, 24.75890718615000097, 1.825072431729000133 ) ) ;
#20403=CARTESIAN_POINT ( 'NONE',  ( -0.8858200100745838856, 23.63223437853404363, -1.939564297548260985 ) ) ;
#20407=CARTESIAN_POINT ( 'NONE',  ( 2.500000000000000000, 30.23419673619000037, 0.000000000000000000 ) ) ;
#20411=VECTOR ( 'NONE', #19617, 1000.000000000000000 ) ;
#20412=CARTESIAN_POINT ( 'NONE',  ( -1.259047450927231804, 28.36753006952333322, 2.184465970885654862 ) ) ;
#20418=ADVANCED_FACE ( 'NONE', ( #10500 ), #3354, .T. ) ;
#20425=CARTESIAN_POINT ( 'NONE',  ( -0.6074916215089999350, 30.83999999999999986, -2.072813047478000215 ) ) ;
#20426=ORIENTED_EDGE ( 'NONE', *, *, #23581, .F. ) ;
#20431=CARTESIAN_POINT ( 'NONE',  ( -0.2400955718764000157, 26.82687716036000225, -2.437731244915000151 ) ) ;
#20435=DIRECTION ( 'NONE',  ( 0.000000000000000000, -1.000000000000000000, -9.414809210018000201E-11 ) ) ;
#20436=CARTESIAN_POINT ( 'NONE',  ( 2.053005267516999902E-14, 28.63049582772000079, 2.160000000000000142 ) ) ;
#20437=ORIENTED_EDGE ( 'NONE', *, *, #14930, .T. ) ;
#20443=CARTESIAN_POINT ( 'NONE',  ( 1.259047450927257339, 29.30086340285666680, 2.184465970885639763 ) ) ;
#20444=CARTESIAN_POINT ( 'NONE',  ( -1.303057794327999952, 30.02656693603999827, -1.711078215202000097 ) ) ;
#20446=CARTESIAN_POINT ( 'NONE',  ( -1.398492736905084355, 30.86841771689475777, -1.613912722856696735 ) ) ;
#20447=ORIENTED_EDGE ( 'NONE', *, *, #12744, .F. ) ;
#20448=PLANE ( 'NONE',  #12956 ) ;
#20452=ORIENTED_EDGE ( 'NONE', *, *, #22278, .T. ) ;
#20454=CONICAL_SURFACE ( 'NONE', #10014, 4.674999979945999584, 0.7853981633972997312 ) ;
#20458=CARTESIAN_POINT ( 'NONE',  ( -1.235933521449031236, 29.28142108852966885, -1.771341811557728629 ) ) ;
#20462=CLOSED_SHELL ( 'NONE', ( #22269, #11860, #3511, #22140, #6902, #15270, #7634, #20047, #16023, #21101, #21232, #14955, #17351, #19091, #3063, #17110, #18716, #11293, #10272, #15890, #21553, #12352, #11120 ) ) ;
#20465=ORIENTED_EDGE ( 'NONE', *, *, #11482, .T. ) ;
#20466=CARTESIAN_POINT ( 'NONE',  ( -2.028744019202999738, 25.29888056986999700, -0.7451492096742999838 ) ) ;
#20468=CARTESIAN_POINT ( 'NONE',  ( 0.9334375154566999511, 28.75049822780999875, 1.831974274068000064 ) ) ;
#20470=DIRECTION ( 'NONE',  ( -1.000000000000000000, 0.000000000000000000, 0.000000000000000000 ) ) ;
#20473=CIRCLE ( 'NONE', #18154, 4.750000000000000000 ) ;
#20475=FACE_OUTER_BOUND ( 'NONE', #8971, .T. ) ;
#20476=VECTOR ( 'NONE', #4217, 1000.000000000000227 ) ;
#20481=CARTESIAN_POINT ( 'NONE',  ( 1.619437063074000038, 24.08748676817999979, -1.682281432622000139 ) ) ;
#20486=CARTESIAN_POINT ( 'NONE',  ( -2.355876953200999768, 29.97705122577999859, -0.1484490314924999943 ) ) ;
#20489=DIRECTION ( 'NONE',  ( 0.000000000000000000, 1.000000000000000000, 0.000000000000000000 ) ) ;
#20494=CARTESIAN_POINT ( 'NONE',  ( -0.7554624816769099915, 24.39581436972834538, 2.418296485626394876 ) ) ;
#20498=DIRECTION ( 'NONE',  ( -1.000000000000000000, 0.000000000000000000, 0.000000000000000000 ) ) ;
#20503=CARTESIAN_POINT ( 'NONE',  ( 2.254114612530000006, 25.55756359724000149, 0.5071914623444000458 ) ) ;
#20505=ORIENTED_EDGE ( 'NONE', *, *, #21491, .T. ) ;
#20509=EDGE_CURVE ( 'NONE', #7192, #1429, #8760, .T. ) ;
#20510=VERTEX_POINT ( 'NONE', #16641 ) ;
#20517=CARTESIAN_POINT ( 'NONE',  ( -1.096889435125999901, 30.16030992228000329, 2.085328208951000128 ) ) ;
#20519=CARTESIAN_POINT ( 'NONE',  ( 0.2333643206754606458, 29.61748404124761791, 2.147376024278286444 ) ) ;
#20520=EDGE_CURVE ( 'NONE', #17141, #6384, #223, .T. ) ;
#20522=CARTESIAN_POINT ( 'NONE',  ( 2.043066369328000231, 24.94995867995000083, 1.131945607266999998 ) ) ;
#20525=DIRECTION ( 'NONE',  ( -0.000000000000000000, -1.000000000000000000, -0.000000000000000000 ) ) ;
#20533=ORIENTED_EDGE ( 'NONE', *, *, #9515, .T. ) ;
#20539=CARTESIAN_POINT ( 'NONE',  ( 0.000000000000000000, 23.00000000000000000, 0.000000000000000000 ) ) ;
#20540=PLANE ( 'NONE',  #4265 ) ;
#20541=SURFACE_STYLE_FILL_AREA ( #13501 ) ;
#20542=CARTESIAN_POINT ( 'NONE',  ( 1.259047450927247569, 27.96753006952333465, -2.184465970885645536 ) ) ;
#20543=CARTESIAN_POINT ( 'NONE',  ( 0.8998430216380005620, 30.45864892563614745, 1.963489132376946333 ) ) ;
#20544=ORIENTED_EDGE ( 'NONE', *, *, #14987, .F. ) ;
#20546=B_SPLINE_CURVE_WITH_KNOTS ( 'NONE', 3,
 ( #5249, #12633, #1001, #8402, #18432, #22180, #7518, #11169, #9229, #4011, #18, #1960, #14902, #20494, #11290, #22293, #9465, #7647 ),
 .UNSPECIFIED., .F., .F.,
 ( 4, 2, 2, 2, 2, 2, 2, 2, 4 ),
 ( 0.000000000000000000, 0.09854977542085557873, 0.1970995508417111575, 0.2956493262625667362, 0.3941991016834223149, 0.4927488771042778937, 0.5912986525251334724, 0.6898484279459891066, 0.7883982033668446299 ),
 .UNSPECIFIED. ) ;
#20548=CARTESIAN_POINT ( 'NONE',  ( 0.000000000000000000, 16.94999982584599962, 0.000000000000000000 ) ) ;
#20549=CARTESIAN_POINT ( 'NONE',  ( -0.5788358281067000899, 25.82114211381999880, -2.218121370661999769 ) ) ;
#20558=FACE_OUTER_BOUND ( 'NONE', #1293, .T. ) ;
#20561=CARTESIAN_POINT ( 'NONE',  ( 0.000000000000000000, 26.50000000000000355, 4.000000000000614619 ) ) ;
#20564=FACE_OUTER_BOUND ( 'NONE', #4928, .T. ) ;
#20566=DIRECTION ( 'NONE',  ( 0.000000000000000000, -1.000000000000000000, 0.000000000000000000 ) ) ;
#20569=CARTESIAN_POINT ( 'NONE',  ( -1.246714904460894946, 29.28220451215178599, -1.763772490062673892 ) ) ;
#20572=CARTESIAN_POINT ( 'NONE',  ( 0.000000000000000000, 15.00000000000000000, -4.625000000000000000 ) ) ;
#20576=CARTESIAN_POINT ( 'NONE',  ( 1.903337834367000214, 24.88085889271999562, 1.023891906906999827 ) ) ;
#20577=DIRECTION ( 'NONE',  ( 0.000000000000000000, 1.000000000000000000, 0.000000000000000000 ) ) ;
#20581=DIRECTION ( 'NONE',  ( -1.000000000000000000, 0.000000000000000000, 0.000000000000000000 ) ) ;
#20585=CIRCLE ( 'NONE', #22512, 2.729128784747790970 ) ;
#20589=EDGE_CURVE ( 'NONE', #18102, #23527, #18557, .T. ) ;
#20590=CARTESIAN_POINT ( 'NONE',  ( 2.532323260332000281, 30.01197222537999920, 1.003311987937999916 ) ) ;
#20591=CARTESIAN_POINT ( 'NONE',  ( -1.199980338850999972, 24.94266885362000252, -2.222287597575000273 ) ) ;
#20595=CARTESIAN_POINT ( 'NONE',  ( 1.523522810973999997, 29.47438902658999993, 1.803072815451999933 ) ) ;
#20600=VERTEX_POINT ( 'NONE', #8406 ) ;
#20601=VECTOR ( 'NONE', #9829, 1000.000000000000000 ) ;
#20603=B_SPLINE_CURVE_WITH_KNOTS ( 'NONE', 3,
 ( #16099, #14181, #10910, #14416, #4990, #21923, #21579, #10674, #16232, #21809, #10796, #1591 ),
 .UNSPECIFIED., .F., .F.,
 ( 4, 2, 2, 2, 2, 4 ),
 ( 0.000000000000000000, 0.2499999999999396039, 0.3749999999999250599, 0.4374999999999310552, 0.4999999999999370504, 1.000000000000000000 ),
 .UNSPECIFIED. ) ;
#20604=ORIENTED_EDGE ( 'NONE', *, *, #12962, .F. ) ;
#20607=CARTESIAN_POINT ( 'NONE',  ( 0.000000000000000000, 18.50000000000000000, 0.000000000000000000 ) ) ;
#20608=DIRECTION ( 'NONE',  ( 0.000000000000000000, 1.000000000000000000, 0.000000000000000000 ) ) ;
#20612=CARTESIAN_POINT ( 'NONE',  ( -1.394936847711000016, 28.14962896667000081, -2.276308483783000103 ) ) ;
#20613=ORIENTED_EDGE ( 'NONE', *, *, #2998, .F. ) ;
#20614=ORIENTED_EDGE ( 'NONE', *, *, #12449, .F. ) ;
#20616=CARTESIAN_POINT ( 'NONE',  ( -2.184465970885646424, 27.36753006952333322, -1.259047450927245126 ) ) ;
#20619=ORIENTED_EDGE ( 'NONE', *, *, #14448, .F. ) ;
#20626=CARTESIAN_POINT ( 'NONE',  ( 1.466483324883999906, 29.69536550879999837, -1.630154757756000050 ) ) ;
#20629=CARTESIAN_POINT ( 'NONE',  ( 0.9925186210581510293, 29.66472845694044125, 1.918284758963818559 ) ) ;
#20631=CARTESIAN_POINT ( 'NONE',  ( -1.674130751070000089, 23.92133400015999811, 1.398636182056999910 ) ) ;
#20633=DIRECTION ( 'NONE',  ( 0.000000000000000000, -1.000000000000000000, 0.000000000000000000 ) ) ;
#20634=ORIENTED_EDGE ( 'NONE', *, *, #16453, .F. ) ;
#20637=CARTESIAN_POINT ( 'NONE',  ( -0.4221993467342085582, 30.45569945603167739, -2.502179599253123055 ) ) ;
#20638=EDGE_CURVE ( 'NONE', #19945, #2909, #17399, .T. ) ;
#20644=VECTOR ( 'NONE', #12557, 1000.000000000000227 ) ;
#20646=EDGE_CURVE ( 'NONE', #16380, #22057, #878, .T. ) ;
#20648=DIRECTION ( 'NONE',  ( 0.7071067811823850136, 0.7071067811898851252, 1.080116765722976056E-06 ) ) ;
#20653=CARTESIAN_POINT ( 'NONE',  ( 0.6100901480019267353, 26.47309547025852439, -2.313337588001243006 ) ) ;
#20654=CARTESIAN_POINT ( 'NONE',  ( -2.434931691670790155, 29.00086340285666608, -0.6543697108981963995 ) ) ;
#20657=CARTESIAN_POINT ( 'NONE',  ( 1.295298327500748581, 30.48557000331402733, 1.732529484320999069 ) ) ;
#20665=CARTESIAN_POINT ( 'NONE',  ( 1.808910716397999829, 27.31696440326000186, -1.672139866504000150 ) ) ;
#20667=DIRECTION ( 'NONE',  ( 0.000000000000000000, -1.000000000000000000, 0.000000000000000000 ) ) ;
#20671=AXIS2_PLACEMENT_3D ( 'NONE', #10112, #2599, #9991 ) ;
#20672=DIRECTION ( 'NONE',  ( -1.000000000000000000, 0.000000000000000000, 0.000000000000000000 ) ) ;
#20673=ORIENTED_EDGE ( 'NONE', *, *, #15278, .T. ) ;
#20675=DIRECTION ( 'NONE',  ( -1.000000000000000000, 0.000000000000000000, 0.000000000000000000 ) ) ;
#20676=B_SPLINE_CURVE_WITH_KNOTS ( 'NONE', 3,
 ( #6314, #19530, #17715, #13701, #21093, #4505, #11897, #12024 ),
 .UNSPECIFIED., .F., .F.,
 ( 4, 2, 2, 4 ),
 ( 0.000000000000000000, 0.2500000000000000000, 0.5000000000000000000, 1.000000000000000000 ),
 .UNSPECIFIED. ) ;
#20677=CIRCLE ( 'NONE', #10246, 4.724999999999999645 ) ;
#20688=CARTESIAN_POINT ( 'NONE',  ( 2.669209039122999894, 27.55206776952000070, 0.05241653317053000111 ) ) ;
#20691=CARTESIAN_POINT ( 'NONE',  ( 2.155476837356603781, 28.99572802833808538, 0.1381959937958471552 ) ) ;
#20693=ORIENTED_EDGE ( 'NONE', *, *, #5938, .T. ) ;
#20698=CARTESIAN_POINT ( 'NONE',  ( -0.5724186824819998964, 25.92299822780999818, -2.193530619437999984 ) ) ;
#20699=DIRECTION ( 'NONE',  ( 0.000000000000000000, -1.000000000000000000, 0.000000000000000000 ) ) ;
#20706=VERTEX_POINT ( 'NONE', #22677 ) ;
#20708=CARTESIAN_POINT ( 'NONE',  ( -2.413984953566000069, 23.46972322239999897, -0.1881867403046000031 ) ) ;
#20713=CARTESIAN_POINT ( 'NONE',  ( 1.661669601868999813, 28.68449128500000000, 1.676656731525000055 ) ) ;
#20716=DIRECTION ( 'NONE',  ( -0.7071067811905932254, 0.7071067811824932603, -1.099460837533990473E-07 ) ) ;
#20720=CARTESIAN_POINT ( 'NONE',  ( -2.000000000000000000, 24.50000000000000000, -3.464101615137999968 ) ) ;
#20721=TOROIDAL_SURFACE ( 'NONE', #22270, 2.100000000000000089, 0.1000000000000000056 ) ;
#20723=VERTEX_POINT ( 'NONE', #1617 ) ;
#20724=CARTESIAN_POINT ( 'NONE',  ( 2.733205704442000172, 25.26683306396000006, -0.1467716043025000250 ) ) ;
#20727=CARTESIAN_POINT ( 'NONE',  ( 0.7453833240861579279, 24.57675687152185873, 2.221003709730194675 ) ) ;
#20731=CARTESIAN_POINT ( 'NONE',  ( -2.104626470933999904, 25.91506359723999964, -1.289728978252000058 ) ) ;
#20732=VERTEX_POINT ( 'NONE', #3325 ) ;
#20739=CARTESIAN_POINT ( 'NONE',  ( 1.699986747157999911, 9.000014340785000400, 0.8485215224771999187 ) ) ;
#20740=AXIS2_PLACEMENT_3D ( 'NONE', #20607, #14680, #22072 ) ;
#20743=VECTOR ( 'NONE', #5010, 1000.000000000000114 ) ;
#20745=EDGE_CURVE ( 'NONE', #11746, #1877, #2336, .T. ) ;
#20746=CARTESIAN_POINT ( 'NONE',  ( -1.869146948832999922, 30.84635783959000221, 0.9105165119439999621 ) ) ;
#20748=CARTESIAN_POINT ( 'NONE',  ( 0.1279519981187458300, 29.61131102235037815, 2.157129590390447493 ) ) ;
#20750=AXIS2_PLACEMENT_3D ( 'NONE', #20548, #5996, #18843 ) ;
#20754=LINE ( 'NONE', #4289, #5778 ) ;
#20763=ORIENTED_EDGE ( 'NONE', *, *, #12170, .T. ) ;
#20769=B_SPLINE_CURVE_WITH_KNOTS ( 'NONE', 3,
 ( #2901, #7861, #21056, #21181 ),
 .UNSPECIFIED., .F., .F.,
 ( 4, 4 ),
 ( 0.2436176585163755404, 0.2478303497282951795 ),
 .UNSPECIFIED. ) ;
#20770=VECTOR ( 'NONE', #3756, 1000.000000000000000 ) ;
#20772=ADVANCED_FACE ( 'NONE', ( #14446 ), #8767, .T. ) ;
#20774=CARTESIAN_POINT ( 'NONE',  ( -9.031350480845023345E-06, 28.86929942113680170, 2.273237782549102803 ) ) ;
#20775=CARTESIAN_POINT ( 'NONE',  ( 2.500000000000000000, 18.50000000000000000, 0.000000000000000000 ) ) ;
#20777=CARTESIAN_POINT ( 'NONE',  ( 2.184465970885644648, 27.90086340285666822, -1.259047450927249345 ) ) ;
#20778=CARTESIAN_POINT ( 'NONE',  ( 1.105833872631340364, 30.47227404555147956, 1.856455373682658117 ) ) ;
#20785=CARTESIAN_POINT ( 'NONE',  ( -2.383523424258999768, 28.38946440325999987, -0.6219987658658000518 ) ) ;
#20793=DIRECTION ( 'NONE',  ( 0.000000000000000000, -1.000000000000000000, 0.000000000000000000 ) ) ;
#20799=DIRECTION ( 'NONE',  ( 0.000000000000000000, 0.000000000000000000, -1.000000000000000000 ) ) ;
#20803=DIRECTION ( 'NONE',  ( 0.000000000000000000, 1.000000000000000000, 0.000000000000000000 ) ) ;
#20810=CARTESIAN_POINT ( 'NONE',  ( -1.948889566018999986, 27.36500240009999985, 2.108296854627000005 ) ) ;
#20815=ADVANCED_FACE ( 'NONE', ( #7521 ), #4108, .T. ) ;
#20816=EDGE_CURVE ( 'NONE', #6675, #14207, #1793, .T. ) ;
#20817=CARTESIAN_POINT ( 'NONE',  ( 1.699986222664000124, 9.100024384209000061, 1.053575639828000066 ) ) ;
#20819=B_SPLINE_CURVE_WITH_KNOTS ( 'NONE', 3,
 ( #20177, #22213, #10860, #20412, #3938, #1647, #1765, #23797, #14597, #23917 ),
 .UNSPECIFIED., .F., .F.,
 ( 4, 2, 2, 2, 4 ),
 ( 0.000000000000000000, 0.2500000000000001110, 0.5000000000000001110, 0.7500000000000001110, 1.000000000000000000 ),
 .UNSPECIFIED. ) ;
#20820=CARTESIAN_POINT ( 'NONE',  ( -3.000000000000000000, 21.89999999999999858, 0.000000000000000000 ) ) ;
#20822=CIRCLE ( 'NONE', #8455, 2.000000000000000000 ) ;
#20828=AXIS2_PLACEMENT_3D ( 'NONE', #1779, #1661, #10875 ) ;
#20830=CARTESIAN_POINT ( 'NONE',  ( 1.146872940636000093, 31.00466803249999970, -2.470645430041999990 ) ) ;
#20831=CARTESIAN_POINT ( 'NONE',  ( -0.9534504523828000178, 24.43033993841000040, 2.338684930832999775 ) ) ;
#20834=AXIS2_PLACEMENT_3D ( 'NONE', #12294, #18107, #8780 ) ;
#20838=CARTESIAN_POINT ( 'NONE',  ( 0.7149603813832000609, 30.34065304942999575, -2.650948342028000226 ) ) ;
#20840=CARTESIAN_POINT ( 'NONE',  ( -1.779764907139927077, 26.49975665830813298, 1.755621799651315262 ) ) ;
#20842=AXIS2_PLACEMENT_3D ( 'NONE', #10276, #4715, #14028 ) ;
#20847=EDGE_LOOP ( 'NONE', ( #13727, #1079, #4508, #9755, #17095, #20447 ) ) ;
#20848=AXIS2_PLACEMENT_3D ( 'NONE', #15612, #10434, #9934 ) ;
#20849=FACE_OUTER_BOUND ( 'NONE', #6871, .T. ) ;
#20850=DIRECTION ( 'NONE',  ( 1.000000000000000000, 0.000000000000000000, 0.000000000000000000 ) ) ;
#20851=CARTESIAN_POINT ( 'NONE',  ( -1.999537075602261016, 23.75013256832107444, -0.9022053864054707661 ) ) ;
#20852=CARTESIAN_POINT ( 'NONE',  ( 1.556904262685800289, 24.71889605908289056, 1.535089544408534179 ) ) ;
#20853=AXIS2_PLACEMENT_3D ( 'NONE', #20539, #2123, #4303 ) ;
#20857=CARTESIAN_POINT ( 'NONE',  ( 2.621867217767999581, 25.34669433610000056, 0.5899383557787000187 ) ) ;
#20858=ORIENTED_EDGE ( 'NONE', *, *, #17493, .F. ) ;
#20859=ORIENTED_EDGE ( 'NONE', *, *, #9231, .T. ) ;
#20862=DIRECTION ( 'NONE',  ( 1.000000000000000000, 0.000000000000000000, 0.000000000000000000 ) ) ;
#20871=CARTESIAN_POINT ( 'NONE',  ( -2.008526492215999770, 30.87968012902000225, 0.9784123912684001834 ) ) ;
#20875=CARTESIAN_POINT ( 'NONE',  ( 0.2157408166878850564, 29.61644974637328431, 2.149169616069145583 ) ) ;
#20877=CARTESIAN_POINT ( 'NONE',  ( -0.5326254371206000648, 23.42133201074999960, -2.045335842707999952 ) ) ;
#20880=CARTESIAN_POINT ( 'NONE',  ( -1.823227943893884984, 24.59979839667439805, -1.434329759635685209 ) ) ;
#20882=CARTESIAN_POINT ( 'NONE',  ( 1.236794719700695211, 24.50000548481460427, 2.172625763342098004 ) ) ;
#20883=EDGE_CURVE ( 'NONE', #17924, #23795, #18324, .T. ) ;
#20885=VERTEX_POINT ( 'NONE', #5595 ) ;
#20888=ORIENTED_EDGE ( 'NONE', *, *, #23767, .F. ) ;
#20889=DIRECTION ( 'NONE',  ( 1.000000000000000000, 0.000000000000000000, 0.000000000000000000 ) ) ;
#20890=B_SPLINE_CURVE_WITH_KNOTS ( 'NONE', 3,
 ( #16937, #1699, #5804, #9204, #15109, #18645, #18406, #5545, #7379, #11268, #5914, #2051, #20122, #9442, #18298, #220, #7617, #573 ),
 .UNSPECIFIED., .F., .F.,
 ( 4, 2, 2, 2, 2, 2, 2, 2, 4 ),
 ( 0.000000000000000000, 0.1250000000000000000, 0.2500000000000000000, 0.3750000000000000000, 0.5000000000000000000, 0.6250000000000000000, 0.7500000000000000000, 0.8750000000000000000, 1.000000000000000000 ),
 .UNSPECIFIED. ) ;
#20897=EDGE_CURVE ( 'NONE', #9922, #19778, #15024, .T. ) ;
#20903=CARTESIAN_POINT ( 'NONE',  ( 0.9906019889434464210, 30.46455799699790745, 1.919774432312305823 ) ) ;
#20909=CARTESIAN_POINT ( 'NONE',  ( 1.683383295848999817, 27.28364211382000093, -1.556103512505999875 ) ) ;
#20914=LINE ( 'NONE', #10013, #22331 ) ;
#20916=VECTOR ( 'NONE', #13419, 1000.000000000000114 ) ;
#20927=CARTESIAN_POINT ( 'NONE',  ( -2.500000000000001332, 26.61184640831621806, -0.4388476615849645768 ) ) ;
#20928=ORIENTED_EDGE ( 'NONE', *, *, #14256, .F. ) ;
#20929=CARTESIAN_POINT ( 'NONE',  ( 3.000000000000000000, 22.00000000000000000, 0.000000000000000000 ) ) ;
#20930=CARTESIAN_POINT ( 'NONE',  ( 1.652809762273000027, 26.86956776951999970, -2.096579189799000265 ) ) ;
#20938=ADVANCED_FACE ( 'NONE', ( #7405 ), #16872, .T. ) ;
#20940=FACE_OUTER_BOUND ( 'NONE', #8718, .T. ) ;
#20950=CARTESIAN_POINT ( 'NONE',  ( 1.699553337878000114, 29.94579250490999911, 2.128570997566999967 ) ) ;
#20952=CARTESIAN_POINT ( 'NONE',  ( 2.429900969743000072, 25.49769184508999942, -0.3508820655058000337 ) ) ;
#20956=FACE_OUTER_BOUND ( 'NONE', #14204, .T. ) ;
#20964=VERTEX_POINT ( 'NONE', #19138 ) ;
#20967=CARTESIAN_POINT ( 'NONE',  ( -2.133777946215778432, 23.65390751601632857, 0.3359879145818772117 ) ) ;
#20976=CARTESIAN_POINT ( 'NONE',  ( 2.000000000000000000, 18.10000000000000142, 0.000000000000000000 ) ) ;
#20980=CARTESIAN_POINT ( 'NONE',  ( 1.712415232174588686, 12.94871783748642535, -1.057129568949859877 ) ) ;
#20981=CARTESIAN_POINT ( 'NONE',  ( 0.000000000000000000, 20.04999987253368943, -2.704938617610999654E-14 ) ) ;
#20984=CARTESIAN_POINT ( 'NONE',  ( -4.649999849441000421, 17.00000015055400127, 6.648422636708999828E-08 ) ) ;
#20986=AXIS2_PLACEMENT_3D ( 'NONE', #13946, #21341, #20862 ) ;
#20988=CARTESIAN_POINT ( 'NONE',  ( -1.790837194179027314, 29.47926921055185545, 1.208204829431328342 ) ) ;
#20989=EDGE_LOOP ( 'NONE', ( #4257, #22661, #13455, #18786 ) ) ;
#20990=CARTESIAN_POINT ( 'NONE',  ( -1.273908836082999985, 23.46786385441999911, -1.776248845517000019 ) ) ;
#20992=ORIENTED_EDGE ( 'NONE', *, *, #9098, .F. ) ;
#20993=CARTESIAN_POINT ( 'NONE',  ( -1.989420752042081908, 24.61064990806593045, -1.172145431141076388 ) ) ;
#20998=VERTEX_POINT ( 'NONE', #19269 ) ;
#21002=FACE_OUTER_BOUND ( 'NONE', #20032, .T. ) ;
#21007=CARTESIAN_POINT ( 'NONE',  ( 3.999999999999999112, 26.42936170367562809, 1.090349405812182315 ) ) ;
#21013=CARTESIAN_POINT ( 'NONE',  ( -0.3272492347489394104, 28.85086340285666751, -2.499999999999999112 ) ) ;
#21014=CARTESIAN_POINT ( 'NONE',  ( 1.800000000000000044, 13.00000000000000000, -1.081665382638999917 ) ) ;
#21016=CARTESIAN_POINT ( 'NONE',  ( -0.5448911592932419445, 30.37147015205572487, 2.090315897457275085 ) ) ;
#21021=CARTESIAN_POINT ( 'NONE',  ( 1.014287269782000012, 28.68196440326000030, 1.990650851275000299 ) ) ;
#21026=CARTESIAN_POINT ( 'NONE',  ( 4.649999849441000421, 14.99999984944626696, -6.648422669304000250E-08 ) ) ;
#21027=CARTESIAN_POINT ( 'NONE',  ( 2.153767644672030634, 28.01336032157206546, 0.2789828094273491543 ) ) ;
#21032=AXIS2_PLACEMENT_3D ( 'NONE', #23741, #16464, #23632 ) ;
#21037=DIRECTION ( 'NONE',  ( 0.000000000000000000, 0.000000000000000000, -1.000000000000000000 ) ) ;
#21040=ADVANCED_FACE ( 'NONE', ( #20849 ), #21142, .T. ) ;
#21041=CARTESIAN_POINT ( 'NONE',  ( 4.000000000000000000, 24.50000000000000000, 0.000000000000000000 ) ) ;
#21042=ORIENTED_EDGE ( 'NONE', *, *, #5432, .F. ) ;
#21043=VECTOR ( 'NONE', #13702, 1000.000000000000114 ) ;
#21044=AXIS2_PLACEMENT_3D ( 'NONE', #4319, #20793, #19083 ) ;
#21046=CARTESIAN_POINT ( 'NONE',  ( 0.5071914623445000769, 28.87663313894999817, 2.254114612530000006 ) ) ;
#21048=CARTESIAN_POINT ( 'NONE',  ( 1.853950820529611576, 28.93531059620830703, 1.108663733423250086 ) ) ;
#21051=ORIENTED_EDGE ( 'NONE', *, *, #19457, .T. ) ;
#21053=CARTESIAN_POINT ( 'NONE',  ( 0.000000000000000000, 17.00000000000000000, 0.000000000000000000 ) ) ;
#21056=CARTESIAN_POINT ( 'NONE',  ( -1.787520374624578690, 26.49857044772972969, 1.747825089855130187 ) ) ;
#21060=EDGE_CURVE ( 'NONE', #19402, #14961, #9821, .T. ) ;
#21065=CARTESIAN_POINT ( 'NONE',  ( 2.665366810462999947, 25.34956313825000151, 0.5220868594133000196 ) ) ;
#21067=VECTOR ( 'NONE', #8863, 1000.000000000000000 ) ;
#21071=ADVANCED_FACE ( 'NONE', ( #8254 ), #7980, .F. ) ;
#21083=DIRECTION ( 'NONE',  ( 0.000000000000000000, -0.4362437346113740011, 0.8998285414523820025 ) ) ;
#21093=CARTESIAN_POINT ( 'NONE',  ( 3.150855693196132457, 24.60222989789001957, 2.799640769041085164 ) ) ;
#21097=CARTESIAN_POINT ( 'NONE',  ( 1.719817536959529436, 12.95985172756701154, -1.059208683210195234 ) ) ;
#21101=ADVANCED_FACE ( 'NONE', ( #2431 ), #17325, .F. ) ;
#21102=AXIS2_PLACEMENT_3D ( 'NONE', #2334, #504, #17343 ) ;
#21103=CARTESIAN_POINT ( 'NONE',  ( -0.7612329563831000678, 28.57769546745999634, 2.100474675742999953 ) ) ;
#21105=ADVANCED_FACE ( 'NONE', ( #11621 ), #7977, .T. ) ;
#21108=CARTESIAN_POINT ( 'NONE',  ( -0.5855206035033558853, 29.56888966826695508, 2.079019416249454633 ) ) ;
#21109=ORIENTED_EDGE ( 'NONE', *, *, #8228, .F. ) ;
#21110=CARTESIAN_POINT ( 'NONE',  ( 1.634731643160000081, 23.91997273684999925, 1.686691236754999990 ) ) ;
#21118=B_SPLINE_CURVE_WITH_KNOTS ( 'NONE', 3,
 ( #4844, #12230, #3152, #17920, #7008, #21676, #1445, #19618, #17805, #8841 ),
 .UNSPECIFIED., .F., .F.,
 ( 4, 2, 2, 2, 4 ),
 ( 0.000000000000000000, 0.2499999999999998890, 0.4999999999999997780, 0.7499999999999998890, 1.000000000000000000 ),
 .UNSPECIFIED. ) ;
#21126=CARTESIAN_POINT ( 'NONE',  ( 0.000000000000000000, 19.00000000000000000, 0.000000000000000000 ) ) ;
#21132=CARTESIAN_POINT ( 'NONE',  ( 1.768240990936880142, 24.49990546444021078, -1.767061324597003713 ) ) ;
#21137=CARTESIAN_POINT ( 'NONE',  ( -2.159773237450644423, 30.20518305836949224, 0.02532526672096173034 ) ) ;
#21142=CONICAL_SURFACE ( 'NONE', #6033, 4.699999872533999756, 0.7853981633972997312 ) ;
#21143=CARTESIAN_POINT ( 'NONE',  ( 0.3272492347489454056, 27.65086340285666822, 2.499999999999998668 ) ) ;
#21144=VECTOR ( 'NONE', #7565, 1000.000000000000114 ) ;
#21148=ORIENTED_EDGE ( 'NONE', *, *, #3051, .F. ) ;
#21150=CARTESIAN_POINT ( 'NONE',  ( 0.000000000000000000, 22.19999999999999574, 0.000000000000000000 ) ) ;
#21152=CARTESIAN_POINT ( 'NONE',  ( -2.157506145421208554, 27.64352613552069116, 0.2337557657564511560 ) ) ;
#21154=AXIS2_PLACEMENT_3D ( 'NONE', #11507, #18881, #15479 ) ;
#21157=CARTESIAN_POINT ( 'NONE',  ( 0.000000000000000000, 15.09999999999999964, 0.000000000000000000 ) ) ;
#21164=CARTESIAN_POINT ( 'NONE',  ( -0.4496761300970291142, 28.77800341527711936, 2.126187163699609251 ) ) ;
#21166=CARTESIAN_POINT ( 'NONE',  ( 0.6543697108982093891, 26.86753006952333678, 2.434931691670787490 ) ) ;
#21171=CARTESIAN_POINT ( 'NONE',  ( 2.644546391786999795, 26.77206776951999956, -0.3657850755363000195 ) ) ;
#21173=CARTESIAN_POINT ( 'NONE',  ( 2.052791027186419814, 28.96347044016121686, 0.6716916050526000603 ) ) ;
#21179=CARTESIAN_POINT ( 'NONE',  ( 0.4925334044481964879, 26.25981921813487219, 2.102983069868059385 ) ) ;
#21181=CARTESIAN_POINT ( 'NONE',  ( -1.779764907139927077, 26.49975665830813298, 1.755621799651315262 ) ) ;
#21183=EDGE_CURVE ( 'NONE', #22057, #13042, #5657, .T. ) ;
#21184=CARTESIAN_POINT ( 'NONE',  ( 1.259047450927247569, 27.16753006952333038, -2.184465970885645536 ) ) ;
#21192=CARTESIAN_POINT ( 'NONE',  ( 0.9860083823784999701, 30.79379877136000232, -2.124103741218000163 ) ) ;
#21206=AXIS2_PLACEMENT_3D ( 'NONE', #600, #6054, #22644 ) ;
#21209=CARTESIAN_POINT ( 'NONE',  ( 2.614613892538000250, 26.07965299175999974, -0.4120747533924999928 ) ) ;
#21210=CARTESIAN_POINT ( 'NONE',  ( -1.681586879633373721, 24.51484633230852950, -1.409227352623252827 ) ) ;
#21221=DIRECTION ( 'NONE',  ( 0.000000000000000000, 0.000000000000000000, -1.000000000000000000 ) ) ;
#21222=DIRECTION ( 'NONE',  ( 0.7071067811865465735, 0.7071067811865465735, 5.135208691342337292E-08 ) ) ;
#21223=DIRECTION ( 'NONE',  ( 0.000000000000000000, 1.000000000000000000, 0.000000000000000000 ) ) ;
#21226=CARTESIAN_POINT ( 'NONE',  ( 1.800000000000000044, 13.00000000000000000, -1.081665382638999917 ) ) ;
#21229=CIRCLE ( 'NONE', #20842, 2.000000000000000000 ) ;
#21231=CARTESIAN_POINT ( 'NONE',  ( 0.2336534512014000198, 29.00931759149999678, -2.344603603009000281 ) ) ;
#21232=ADVANCED_FACE ( 'NONE', ( #23343 ), #10647, .T. ) ;
#21236=CARTESIAN_POINT ( 'NONE',  ( -1.090704560478623186, 29.53635738603347249, 1.864235603192405222 ) ) ;
#21238=CARTESIAN_POINT ( 'NONE',  ( -2.146635823351999761, 25.21280799190000010, 0.4123919462612000153 ) ) ;
#21241=CARTESIAN_POINT ( 'NONE',  ( 2.053005267516999902E-14, 28.63049582772000079, 2.160000000000000142 ) ) ;
#21246=DIRECTION ( 'NONE',  ( 0.000000000000000000, 1.000000000000000000, 0.000000000000000000 ) ) ;
#21253=CARTESIAN_POINT ( 'NONE',  ( 0.000000000000000000, 22.00131761696259503, 0.000000000000000000 ) ) ;
#21255=ORIENTED_EDGE ( 'NONE', *, *, #2867, .T. ) ;
#21256=CARTESIAN_POINT ( 'NONE',  ( -1.042632460611140788, 24.73976796275902146, 1.891962004173780576 ) ) ;
#21260=AXIS2_PLACEMENT_3D ( 'NONE', #13925, #4980, #2916 ) ;
#21263=DIRECTION ( 'NONE',  ( 0.000000000000000000, -1.000000000000000000, 0.000000000000000000 ) ) ;
#21266=EDGE_CURVE ( 'NONE', #18791, #20510, #21922, .T. ) ;
#21267=CARTESIAN_POINT ( 'NONE',  ( -0.9744765624120645953, 26.41693820796410819, 4.056187847889995979 ) ) ;
#21268=B_SPLINE_CURVE_WITH_KNOTS ( 'NONE', 3,
 ( #19076, #2132, #9521, #7708, #15557, #6724, #13743, #10371, #21143, #23427, #2744, #17635, #1034, #4802, #17513, #4557, #907, #6361 ),
 .UNSPECIFIED., .F., .F.,
 ( 4, 2, 2, 2, 2, 2, 2, 2, 4 ),
 ( 0.000000000000000000, 0.1250000000000000000, 0.2500000000000000000, 0.3750000000000000000, 0.5000000000000000000, 0.6250000000000000000, 0.7500000000000000000, 0.8750000000000000000, 1.000000000000000000 ),
 .UNSPECIFIED. ) ;
#21269=DIRECTION ( 'NONE',  ( 0.000000000000000000, 1.000000000000000000, 0.000000000000000000 ) ) ;
#21271=CARTESIAN_POINT ( 'NONE',  ( -1.180412381323944881, 30.07751909137916613, -1.808792577990875783 ) ) ;
#21275=CARTESIAN_POINT ( 'NONE',  ( -2.136729350344353850, 23.63672935034427880, -0.2192973291338879971 ) ) ;
#21280=VERTEX_POINT ( 'NONE', #17800 ) ;
#21284=CARTESIAN_POINT ( 'NONE',  ( 0.3677801680678270402, 26.60799041457681113, -2.168894944354226695 ) ) ;
#21294=CARTESIAN_POINT ( 'NONE',  ( -2.197883833863924163, 28.59249535265084674, -0.2145651371980360489 ) ) ;
#21295=CARTESIAN_POINT ( 'NONE',  ( 2.404489386789158356, 26.49040384242090695, -3.230569558791225315 ) ) ;
#21296=DIRECTION ( 'NONE',  ( -1.000000000000000000, 0.000000000000000000, 0.000000000000000000 ) ) ;
#21299=CARTESIAN_POINT ( 'NONE',  ( -0.2222064166829000043, 26.75619850838000247, -2.256099604565999783 ) ) ;
#21300=DIRECTION ( 'NONE',  ( -0.7071067811823850136, -0.7071067811898851252, -1.080116769369976149E-06 ) ) ;
#21305=DIRECTION ( 'NONE',  ( -1.000000000000000000, 0.000000000000000000, 0.000000000000000000 ) ) ;
#21309=FACE_OUTER_BOUND ( 'NONE', #7913, .T. ) ;
#21314=CARTESIAN_POINT ( 'NONE',  ( -0.3272492347489393549, 28.61666666666667069, -2.499999999999999556 ) ) ;
#21315=CARTESIAN_POINT ( 'NONE',  ( -2.375513208737999982, 29.50945927196000085, -0.8786735848391999948 ) ) ;
#21320=CYLINDRICAL_SURFACE ( 'NONE', #2686, 0.09999999999999939493 ) ;
#21321=CARTESIAN_POINT ( 'NONE',  ( 0.5025988904459999240, 29.55075530783999938, -2.699273784843000179 ) ) ;
#21326=EDGE_CURVE ( 'NONE', #14748, #9720, #7589, .T. ) ;
#21327=CARTESIAN_POINT ( 'NONE',  ( 0.000000000000000000, 7.000000000000000000, 0.000000000000000000 ) ) ;
#21329=LINE ( 'NONE', #23250, #23571 ) ;
#21332=CARTESIAN_POINT ( 'NONE',  ( -2.208934844301000400, 25.40431520043999924, -0.8113325475626999017 ) ) ;
#21333=CARTESIAN_POINT ( 'NONE',  ( 2.170273952127825812, 24.22245577580034848, -0.3150010920229354139 ) ) ;
#21336=DIRECTION ( 'NONE',  ( 0.000000000000000000, 0.000000000000000000, -1.000000000000000000 ) ) ;
#21337=CARTESIAN_POINT ( 'NONE',  ( 0.1690226414553999690, 27.16669433610000084, -2.866097959738999723 ) ) ;
#21341=DIRECTION ( 'NONE',  ( 0.000000000000000000, -1.000000000000000000, 0.000000000000000000 ) ) ;
#21342=CARTESIAN_POINT ( 'NONE',  ( 0.000000000000000000, 16.89999999999999858, -4.749999999999985789 ) ) ;
#21345=CARTESIAN_POINT ( 'NONE',  ( 1.709407021842912489, 12.94283542261882047, -1.056280950884417091 ) ) ;
#21349=CARTESIAN_POINT ( 'NONE',  ( -2.020778351004999696, 29.15319163284999959, -1.211699210884999989 ) ) ;
#21354=CARTESIAN_POINT ( 'NONE',  ( -1.423014976520625474, 29.51237747527418520, 1.625193323046951743 ) ) ;
#21355=VERTEX_POINT ( 'NONE', #12103 ) ;
#21356=PLANE ( 'NONE',  #12269 ) ;
#21362=AXIS2_PLACEMENT_3D ( 'NONE', #9450, #11393, #11745 ) ;
#21364=EDGE_CURVE ( 'NONE', #13406, #11582, #15311, .T. ) ;
#21368=DIRECTION ( 'NONE',  ( -0.000000000000000000, -1.000000000000000000, -0.000000000000000000 ) ) ;
#21369=ORIENTED_EDGE ( 'NONE', *, *, #22155, .T. ) ;
#21371=DIRECTION ( 'NONE',  ( 0.000000000000000000, -1.000000000000000000, 0.000000000000000000 ) ) ;
#21381=CARTESIAN_POINT ( 'NONE',  ( -1.963937914100636117, 30.14918992299582712, -0.8991143373722088050 ) ) ;
#21383=ADVANCED_FACE ( 'NONE', ( #11328 ), #11465, .T. ) ;
#21389=CARTESIAN_POINT ( 'NONE',  ( 1.562692578156580359, 24.13277580623734409, -1.623334903882450275 ) ) ;
#21390=CARTESIAN_POINT ( 'NONE',  ( 0.000000000000000000, 24.39999999221199900, 0.000000000000000000 ) ) ;
#21391=AXIS2_PLACEMENT_3D ( 'NONE', #9913, #16938, #18646 ) ;
#21395=ADVANCED_FACE ( 'NONE', ( #3816 ), #16891, .T. ) ;
#21397=CARTESIAN_POINT ( 'NONE',  ( 2.169242523261438294, 26.43540112775283291, -0.09789572399922988333 ) ) ;
#21407=CARTESIAN_POINT ( 'NONE',  ( 2.202026052408534440, 28.19497807538909129, 0.1713982358229051983 ) ) ;
#21408=CARTESIAN_POINT ( 'NONE',  ( 2.817565069457256932, 26.44682129341587995, -2.992080202207100470 ) ) ;
#21411=ORIENTED_EDGE ( 'NONE', *, *, #11337, .F. ) ;
#21414=CARTESIAN_POINT ( 'NONE',  ( 1.332518472557000067, 28.02369850838000076, 1.834054417453000019 ) ) ;
#21425=CARTESIAN_POINT ( 'NONE',  ( 0.000000000000000000, 24.65000000000000213, 0.000000000000000000 ) ) ;
#21426=EDGE_CURVE ( 'NONE', #6143, #8305, #18940, .T. ) ;
#21427=B_SPLINE_CURVE_WITH_KNOTS ( 'NONE', 3,
 ( #17642, #6247, #6124, #1040, #4810, #12196, #19586, #17152 ),
 .UNSPECIFIED., .F., .F.,
 ( 4, 2, 2, 4 ),
 ( 0.000000000000000000, 0.2500000000000000555, 0.5000000000000000000, 1.000000000000000000 ),
 .UNSPECIFIED. ) ;
#21429=B_SPLINE_CURVE_WITH_KNOTS ( 'NONE', 3,
 ( #14394, #21551, #8952, #5198, #3504, #8471, #10772, #23710, #4965, #7116, #17673, #12351, #21900, #3611, #5653, #3724, #7465, #13276, #18272, #14849, #7586, #11115, #9061, #9300, #13041, #16432, #20317, #10994, #18380, #23820, #20204, #12921, #16673, #18499, #20436 ),
 .UNSPECIFIED., .F., .F.,
 ( 4, 1, 1, 1, 1, 1, 1, 1, 1, 1, 1, 1, 1, 1, 1, 1, 1, 1, 1, 1, 1, 1, 1, 1, 1, 1, 1, 1, 1, 1, 1, 1, 4 ),
 ( 0.000000000000000000, 0.01250433631178367658, 0.04500407098468133665, 0.07750380565757906959, 0.1100035403304767956, 0.1425032750033744522, 0.1750030096762721921, 0.2075027443491698487, 0.2400024790222033133, 0.2725022136951010809, 0.3050019483679987098, 0.3375016830408962831, 0.3700014177137940785, 0.4025011523866917629, 0.4350008870595893917, 0.4675006217326229119, 0.5000003564055205407, 0.5325000910784183361, 0.5649998257513160205, 0.5974995604242137048, 0.6299992950971115002, 0.6624990297700089625, 0.6949987644430426492, 0.7274984991159403336, 0.7599982337888380179, 0.7924979684617357023, 0.8249977031346332756, 0.8574974378075309600, 0.8899971724805646467, 0.9224969071534622200, 0.9549966418263599044, 0.9874963764992575888, 1.000000000000000000 ),
 .UNSPECIFIED. ) ;
#21436=CARTESIAN_POINT ( 'NONE',  ( -2.500000000000000000, 28.80000000000000071, 0.000000000000000000 ) ) ;
#21437=CARTESIAN_POINT ( 'NONE',  ( -2.325054514425000107, 30.26436100756000158, 0.2794086195161999964 ) ) ;
#21441=DIRECTION ( 'NONE',  ( 0.000000000000000000, 1.000000000000000000, 0.000000000000000000 ) ) ;
#21442=CARTESIAN_POINT ( 'NONE',  ( 1.800000000000000044, 12.90000000000000036, -17.04402002421999995 ) ) ;
#21453=CARTESIAN_POINT ( 'NONE',  ( 2.099426398219999879, 25.23106871291000175, -1.438876042424000135 ) ) ;
#21460=ORIENTED_EDGE ( 'NONE', *, *, #1371, .T. ) ;
#21461=CARTESIAN_POINT ( 'NONE',  ( -1.259047450927242018, 29.96753006952333465, 2.184465970885648201 ) ) ;
#21463=DIRECTION ( 'NONE',  ( 0.000000000000000000, 1.000000000000000000, 0.000000000000000000 ) ) ;
#21471=CARTESIAN_POINT ( 'NONE',  ( 1.543039561260000081, 29.51287673621999730, 1.780670965265999994 ) ) ;
#21476=CARTESIAN_POINT ( 'NONE',  ( -0.6018193462441471242, 29.56788224182974645, 2.074376258238080251 ) ) ;
#21477=ORIENTED_EDGE ( 'NONE', *, *, #19169, .T. ) ;
#21478=CARTESIAN_POINT ( 'NONE',  ( -1.259047450927251566, 29.46666666666666856, -2.184465970885643316 ) ) ;
#21479=CIRCLE ( 'NONE', #2118, 4.549999999999999822 ) ;
#21481=B_SPLINE_CURVE_WITH_KNOTS ( 'NONE', 3,
 ( #10458, #1608, #6806, #1365, #6932, #17847, #21716, #14200 ),
 .UNSPECIFIED., .F., .F.,
 ( 4, 2, 2, 4 ),
 ( 0.000000000000000000, 0.2500000000000000000, 0.5000000000000000000, 1.000000000000000000 ),
 .UNSPECIFIED. ) ;
#21490=CARTESIAN_POINT ( 'NONE',  ( 4.549999861571000004, 21.99999986157541798, -6.289351278164000247E-08 ) ) ;
#21491=EDGE_CURVE ( 'NONE', #10829, #15998, #15330, .T. ) ;
#21492=ORIENTED_EDGE ( 'NONE', *, *, #9766, .T. ) ;
#21499=LINE ( 'NONE', #10844, #3666 ) ;
#21500=DIRECTION ( 'NONE',  ( 0.000000000000000000, -1.000000000000000000, 0.000000000000000000 ) ) ;
#21502=CARTESIAN_POINT ( 'NONE',  ( 1.055729715565287385, 26.42936170367563875, 4.009276318043866638 ) ) ;
#21504=EDGE_CURVE ( 'NONE', #14207, #8305, #14197, .T. ) ;
#21505=CARTESIAN_POINT ( 'NONE',  ( -1.896736228727305740, 30.14027807355979505, -1.033228027540613381 ) ) ;
#21506=EDGE_LOOP ( 'NONE', ( #9452, #9999, #11407, #4567 ) ) ;
#21507=CARTESIAN_POINT ( 'NONE',  ( -2.293740706879999980, 25.43854303844000242, 0.4406523845536999828 ) ) ;
#21511=VERTEX_POINT ( 'NONE', #11561 ) ;
#21515=CARTESIAN_POINT ( 'NONE',  ( 0.000000000000000000, 18.10000000000000142, 0.000000000000000000 ) ) ;
#21519=ORIENTED_EDGE ( 'NONE', *, *, #12532, .F. ) ;
#21531=CARTESIAN_POINT ( 'NONE',  ( 0.000000000000000000, 16.89999999999999858, 0.000000000000000000 ) ) ;
#21532=AXIS2_PLACEMENT_3D ( 'NONE', #23706, #15172, #13007 ) ;
#21533=AXIS2_PLACEMENT_3D ( 'NONE', #10422, #8355, #6650 ) ;
#21535=EDGE_CURVE ( 'NONE', #8278, #7192, #22294, .T. ) ;
#21538=CARTESIAN_POINT ( 'NONE',  ( -1.306994031390692035, 26.46241504948189771, -3.864208797664315576 ) ) ;
#21539=DIRECTION ( 'NONE',  ( 0.000000000000000000, 0.000000000000000000, -1.000000000000000000 ) ) ;
#21540=CARTESIAN_POINT ( 'NONE',  ( -2.256099604565999783, 27.73119850838000033, -0.2222064166828000287 ) ) ;
#21546=ORIENTED_EDGE ( 'NONE', *, *, #8110, .F. ) ;
#21550=AXIS2_PLACEMENT_3D ( 'NONE', #5572, #9445, #22395 ) ;
#21551=CARTESIAN_POINT ( 'NONE',  ( -2.165649008596949088, 30.83057276060822360, 0.005272181257143124418 ) ) ;
#21553=ADVANCED_FACE ( 'NONE', ( #13721 ), #6337, .F. ) ;
#21558=ORIENTED_EDGE ( 'NONE', *, *, #8171, .F. ) ;
#21560=CARTESIAN_POINT ( 'NONE',  ( -0.8187651254961000324, 29.01927641826999960, 2.471853669016999877 ) ) ;
#21565=CARTESIAN_POINT ( 'NONE',  ( -0.5244086596060245631, 26.50000000000000000, -2.383357424156489657 ) ) ;
#21573=AXIS2_PLACEMENT_3D ( 'NONE', #15783, #21368, #4785 ) ;
#21578=CARTESIAN_POINT ( 'NONE',  ( 1.716093532388071496, 30.62679492094257228, 1.703340837445145306 ) ) ;
#21579=CARTESIAN_POINT ( 'NONE',  ( 1.719784723310866736, 12.95979884212811939, 1.059170354069117970 ) ) ;
#21580=ORIENTED_EDGE ( 'NONE', *, *, #21491, .F. ) ;
#21581=CARTESIAN_POINT ( 'NONE',  ( -1.361252172549999973, 24.88271731528999808, 2.150569224523000145 ) ) ;
#21590=CARTESIAN_POINT ( 'NONE',  ( 2.500000000000001776, 30.21753006952333109, 0.3272492347489266429 ) ) ;
#21595=CARTESIAN_POINT ( 'NONE',  ( -3.099999776787000005, 16.99999977679100027, -5.570936493763999179E-07 ) ) ;
#21598=CARTESIAN_POINT ( 'NONE',  ( 2.133199474671000129, 30.51333916994999740, -0.3868384114466000279 ) ) ;
#21601=ORIENTED_EDGE ( 'NONE', *, *, #10771, .F. ) ;
#21603=CARTESIAN_POINT ( 'NONE',  ( -0.2387898408332101985, 29.21801578594281068, -2.146576094895672693 ) ) ;
#21607=ORIENTED_EDGE ( 'NONE', *, *, #20329, .F. ) ;
#21608=AXIS2_PLACEMENT_3D ( 'NONE', #17691, #10061, #12001 ) ;
#21609=CARTESIAN_POINT ( 'NONE',  ( 0.000000000000000000, -1.550000000000000044, 0.000000000000000000 ) ) ;
#21615=ORIENTED_EDGE ( 'NONE', *, *, #8110, .T. ) ;
#21619=VERTEX_POINT ( 'NONE', #20882 ) ;
#21625=CIRCLE ( 'NONE', #22376, 2.000000000000000000 ) ;
#21626=CARTESIAN_POINT ( 'NONE',  ( 2.207687974961999977, 29.05785630726000335, -0.7846283158615999787 ) ) ;
#21627=AXIS2_PLACEMENT_3D ( 'NONE', #10526, #17910, #4713 ) ;
#21628=CARTESIAN_POINT ( 'NONE',  ( 0.000000000000000000, 26.20000000000000284, 4.618802153517000519 ) ) ;
#21629=CARTESIAN_POINT ( 'NONE',  ( -1.194153984485240683, 30.07849839638842226, -1.799745786739597619 ) ) ;
#21633=CARTESIAN_POINT ( 'NONE',  ( -1.894956018450759005, 23.61932460823316404, -0.9647289121299874592 ) ) ;
#21635=VERTEX_POINT ( 'NONE', #8165 ) ;
#21643=EDGE_LOOP ( 'NONE', ( #917, #19368, #12871, #2227 ) ) ;
#21650=CARTESIAN_POINT ( 'NONE',  ( 0.5031143267968901656, 26.62499557077888213, 2.497567878996554747 ) ) ;
#21651=CIRCLE ( 'NONE', #3088, 2.899999999999999911 ) ;
#21655=CARTESIAN_POINT ( 'NONE',  ( -0.8491321808595133636, 24.60222989789001957, 4.128541458487867466 ) ) ;
#21657=CARTESIAN_POINT ( 'NONE',  ( 0.9780573793134281768, 28.06247231623991212, 1.979757165466330626 ) ) ;
#21659=VECTOR ( 'NONE', #23816, 1000.000000000000000 ) ;
#21660=CARTESIAN_POINT ( 'NONE',  ( 0.000000000000000000, 19.09999999999999787, -3.000000000003983480 ) ) ;
#21661=ORIENTED_EDGE ( 'NONE', *, *, #22955, .T. ) ;
#21664=CARTESIAN_POINT ( 'NONE',  ( 1.206163983883000057, 25.98413313894999987, -2.153772461420000006 ) ) ;
#21667=CARTESIAN_POINT ( 'NONE',  ( 1.439795436514999860, 28.09437716036000410, 1.981708497821000226 ) ) ;
#21669=VERTEX_POINT ( 'NONE', #10219 ) ;
#21670=CARTESIAN_POINT ( 'NONE',  ( 0.000000000000000000, -1.550000000000000044, 0.000000000000000000 ) ) ;
#21676=CARTESIAN_POINT ( 'NONE',  ( -2.133997843432942521, 30.69809435506457262, -0.8888301093114056028 ) ) ;
#21680=ORIENTED_EDGE ( 'NONE', *, *, #22345, .F. ) ;
#21682=CARTESIAN_POINT ( 'NONE',  ( 0.2733293520537999899, 30.56833479956000232, 2.518019340826000096 ) ) ;
#21683=CARTESIAN_POINT ( 'NONE',  ( 2.593577339411000438, 23.81257639262999959, -0.8064155041328999740 ) ) ;
#21686=EDGE_CURVE ( 'NONE', #13042, #21878, #18445, .T. ) ;
#21688=CARTESIAN_POINT ( 'NONE',  ( 0.000000000000000000, -1.550000000000000044, 0.000000000000000000 ) ) ;
#21690=CARTESIAN_POINT ( 'NONE',  ( -0.6074916215089999350, 30.83999999999999986, -2.072813047478000215 ) ) ;
#21696=ORIENTED_EDGE ( 'NONE', *, *, #21686, .T. ) ;
#21697=DIRECTION ( 'NONE',  ( 1.511005137241999593E-08, -0.9999999999999997780, 8.997177532459998026E-09 ) ) ;
#21700=ORIENTED_EDGE ( 'NONE', *, *, #22451, .T. ) ;
#21701=CARTESIAN_POINT ( 'NONE',  ( -2.051653534209000096, 24.15210859155000023, 1.811817559062000038 ) ) ;
#21707=EDGE_CURVE ( 'NONE', #9729, #18970, #7216, .T. ) ;
#21712=ORIENTED_EDGE ( 'NONE', *, *, #973, .F. ) ;
#21714=DIRECTION ( 'NONE',  ( 0.000000000000000000, 0.000000000000000000, -1.000000000000000000 ) ) ;
#21716=CARTESIAN_POINT ( 'NONE',  ( 4.000000000000071942, 24.70197603011810372, 1.905018119031321566 ) ) ;
#21718=CARTESIAN_POINT ( 'NONE',  ( 0.1373810394097000065, 30.19247788257999687, 2.356548280181000266 ) ) ;
#21724=ORIENTED_EDGE ( 'NONE', *, *, #18134, .T. ) ;
#21729=FACE_OUTER_BOUND ( 'NONE', #12835, .T. ) ;
#21732=EDGE_CURVE ( 'NONE', #7192, #15097, #18820, .T. ) ;
#21733=EDGE_LOOP ( 'NONE', ( #8653, #5792, #20544, #364 ) ) ;
#21736=CYLINDRICAL_SURFACE ( 'NONE', #5137, 2.500000000000000000 ) ;
#21743=AXIS2_PLACEMENT_3D ( 'NONE', #648, #17249, #18827 ) ;
#21744=CARTESIAN_POINT ( 'NONE',  ( -1.897333882707999964, 30.29912746140999857, 1.090302715689999813 ) ) ;
#21746=CARTESIAN_POINT ( 'NONE',  ( 1.535128497521570434, 29.90306122052386328, -1.519513479630941966 ) ) ;
#21752=ORIENTED_EDGE ( 'NONE', *, *, #2874, .F. ) ;
#21754=CARTESIAN_POINT ( 'NONE',  ( 0.000000000000000000, 26.34999999328000087, 0.000000000000000000 ) ) ;
#21758=ORIENTED_EDGE ( 'NONE', *, *, #3923, .T. ) ;
#21759=AXIS2_PLACEMENT_3D ( 'NONE', #3914, #5840, #16982 ) ;
#21763=B_SPLINE_SURFACE_WITH_KNOTS ( 'NONE', 3, 3, ( 
 ( #3435, #19784, #10693, #3193, #5243, #14436, #10819, #21598, #16120, #18315, #8632, #7276, #18084, #1241, #1489, #10575, #1717, #12854, #3313, #23646, #7053, #15995, #5014, #8756, #6808, #9107, #23756, #8883, #22064, #17962, #10929, #20250, #6934, #21831, #16479 ),
 ( #20013, #3656, #1610, #14549, #8996, #21944, #23390, #1366, #23521, #14330, #21718, #5129, #19896, #20486, #2068, #12, #7396, #9222, #13315, #13202, #20595, #22174, #16602, #16833, #4004, #9459, #14778, #472, #1836, #9340, #358, #20713, #5585, #5701, #18426 ),
 ( #12967, #7511, #18896, #20363, #13087, #3893, #236, #3773, #11161, #18547, #1954, #5930, #7640, #16713, #2306, #22412, #124, #11284, #14894, #5820, #18661, #15013, #13436, #22285, #11402, #7759, #18770, #4121, #2180, #9573, #11518, #16959, #15125, #17074, #22522 ),
 ( #9693, #7875, #15243, #22635, #6047, #20838, #11042, #2539, #2917, #4361, #23116, #2797, #19127, #17567, #23242, #4736, #21321, #19257, #839, #17194, #19385, #13561, #8488, #6176, #15728, #15853, #17316, #2670, #12122, #10179, #22996, #15492, #13926, #9930, #7993 ) ),
 .UNSPECIFIED., .F., .F., .F.,
 ( 4, 4 ),
 ( 4, 1, 1, 1, 1, 1, 1, 1, 1, 1, 1, 1, 1, 1, 1, 1, 1, 1, 1, 1, 1, 1, 1, 1, 1, 1, 1, 1, 1, 1, 1, 1, 4 ),
 ( -0.3056682515952000023, 1.305668251594999996 ),
 ( 0.2487685814243000004, 0.2727048766240999789, 0.2966411718237999540, 0.3205774670234999846, 0.3445137622232000152, 0.3684500574228999903, 0.3923863526226000209, 0.4163226478222999960, 0.4402589430221000022, 0.4641952382218000328, 0.4881315334215000079, 0.5120678286211999275, 0.5360041238209000136, 0.5599404190205999887, 0.5838767142202999638, 0.6078130094200999700, 0.6317493046197999451, 0.6556855998195000312, 0.6796218950192000063, 0.7035581902188999814, 0.7274944854186000676, 0.7514307806182999316, 0.7753670758181000489, 0.7993033710178000240, 0.8232396662174999991, 0.8471759614172000852, 0.8711122566168999493, 0.8950485518166000354, 0.9189848470164000416, 0.9429211422161000167, 0.9668574374157999918, 0.9907937326154999669, 1.014730027814999991 ),
 .UNSPECIFIED. ) ;
#21764=ORIENTED_EDGE ( 'NONE', *, *, #19470, .F. ) ;
#21765=CARTESIAN_POINT ( 'NONE',  ( -0.9692852216071858873, 26.54999367254126597, 2.356152689279187307 ) ) ;
#21772=CARTESIAN_POINT ( 'NONE',  ( 1.126663271959915225, 26.47240320403346558, 1.894978555737950154 ) ) ;
#21773=CARTESIAN_POINT ( 'NONE',  ( -2.254705796085000102, 28.14500240010000098, 1.777466727206999941 ) ) ;
#21774=CARTESIAN_POINT ( 'NONE',  ( 1.065127663449546791, 30.73828402243652391, -1.880807996640347701 ) ) ;
#21775=EDGE_LOOP ( 'NONE', ( #12375, #23597, #21712, #4854 ) ) ;
#21777=CARTESIAN_POINT ( 'NONE',  ( -2.270871215252209030, 19.00000000000000000, 0.000000000000000000 ) ) ;
#21778=CARTESIAN_POINT ( 'NONE',  ( -1.876963106047000007, 26.95913313895000130, -1.603077936557000038 ) ) ;
#21779=AXIS2_PLACEMENT_3D ( 'NONE', #7749, #9213, #16592 ) ;
#21780=CARTESIAN_POINT ( 'NONE',  ( 1.117936111508999852, 25.96771896306000116, -1.996229403933999835 ) ) ;
#21789=DIRECTION ( 'NONE',  ( -3.842525697690999187E-09, -0.9999999999999998890, 1.654014171407999877E-08 ) ) ;
#21798=VERTEX_POINT ( 'NONE', #14187 ) ;
#21800=CARTESIAN_POINT ( 'NONE',  ( 0.000000000000000000, 17.89999999999999858, 0.000000000000000000 ) ) ;
#21809=CARTESIAN_POINT ( 'NONE',  ( 1.739740853794686792, 12.98133831228224899, 1.064828544757462137 ) ) ;
#21810=ORIENTED_EDGE ( 'NONE', *, *, #11754, .T. ) ;
#21811=CARTESIAN_POINT ( 'NONE',  ( 2.541521031844999889, 25.16139843338999782, -0.1364782455292000152 ) ) ;
#21816=CARTESIAN_POINT ( 'NONE',  ( 2.100000000000000089, 18.00000000000000000, 0.000000000000000000 ) ) ;
#21818=FACE_OUTER_BOUND ( 'NONE', #8405, .T. ) ;
#21821=DIRECTION ( 'NONE',  ( 0.000000000000000000, 1.000000000000000000, 0.000000000000000000 ) ) ;
#21822=DIRECTION ( 'NONE',  ( 0.000000000000000000, 1.000000000000000000, 0.000000000000000000 ) ) ;
#21824=EDGE_LOOP ( 'NONE', ( #19330, #23543, #15074, #7951, #77, #22189 ) ) ;
#21826=CARTESIAN_POINT ( 'NONE',  ( 2.104585786644999956, 25.66586702996999847, 0.4122421647189999927 ) ) ;
#21828=CIRCLE ( 'NONE', #21032, 4.000000000000000000 ) ;
#21829=CARTESIAN_POINT ( 'NONE',  ( 0.000000000000000000, 8.900000000000000355, 0.000000000000000000 ) ) ;
#21831=CARTESIAN_POINT ( 'NONE',  ( -0.3358725919101999691, 28.67024443956999846, 2.064953224512999785 ) ) ;
#21836=ORIENTED_EDGE ( 'NONE', *, *, #195, .T. ) ;
#21838=DIRECTION ( 'NONE',  ( 0.000000000000000000, 0.000000000000000000, -1.000000000000000000 ) ) ;
#21839=CARTESIAN_POINT ( 'NONE',  ( -2.500000000000000000, 29.03419673619000108, 0.000000000000000000 ) ) ;
#21840=ORIENTED_EDGE ( 'NONE', *, *, #15327, .T. ) ;
#21851=ORIENTED_EDGE ( 'NONE', *, *, #4997, .T. ) ;
#21860=CARTESIAN_POINT ( 'NONE',  ( 0.7926161359157861686, 29.95607633739005138, -2.009593667427580943 ) ) ;
#21861=ADVANCED_FACE ( 'NONE', ( #23257, #6671 ), #12385, .F. ) ;
#21866=CARTESIAN_POINT ( 'NONE',  ( -0.8696119214085413773, 23.63534625394520461, -1.950261407548883552 ) ) ;
#21872=LINE ( 'NONE', #1645, #6875 ) ;
#21874=AXIS2_PLACEMENT_3D ( 'NONE', #2673, #6179, #19512 ) ;
#21875=DIRECTION ( 'NONE',  ( 1.000000000000000000, 0.000000000000000000, 0.000000000000000000 ) ) ;
#21878=VERTEX_POINT ( 'NONE', #13071 ) ;
#21881=DIRECTION ( 'NONE',  ( 0.8947368421052591669, 0.000000000000000000, 0.4465937565388801156 ) ) ;
#21884=CARTESIAN_POINT ( 'NONE',  ( -2.156038708526037517, 26.98917566598937867, -0.2605989890222873417 ) ) ;
#21886=AXIS2_PLACEMENT_3D ( 'NONE', #5494, #18687, #16507 ) ;
#21891=CARTESIAN_POINT ( 'NONE',  ( 1.672490300650320449, 24.75097662330977144, 1.349479665860685351 ) ) ;
#21892=VECTOR ( 'NONE', #5078, 1000.000000000000000 ) ;
#21893=CARTESIAN_POINT ( 'NONE',  ( 2.256729627096000002, 27.96614211382000192, 0.4030006639746999686 ) ) ;
#21894=B_SPLINE_CURVE_WITH_KNOTS ( 'NONE', 3,
 ( #4878, #12266, #3068, #23748, #8987, #6926, #7151, #3538 ),
 .UNSPECIFIED., .F., .F.,
 ( 4, 2, 2, 4 ),
 ( 0.000000000000000000, 0.2499999999999998890, 0.4999999999999997780, 1.000000000000000000 ),
 .UNSPECIFIED. ) ;
#21897=ORIENTED_CLOSED_SHELL ( 'NONE', *, #5759, .F. );
#21900=CARTESIAN_POINT ( 'NONE',  ( -1.997969690258423858, 30.09406483207807526, 1.094238623052827819 ) ) ;
#21902=DIRECTION ( 'NONE',  ( 1.000000000000000000, 0.000000000000000000, 0.000000000000000000 ) ) ;
#21903=DIRECTION ( 'NONE',  ( -0.5000000000000169864, 0.000000000000000000, 0.8660254037844289376 ) ) ;
#21907=DIRECTION ( 'NONE',  ( 0.000000000000000000, -1.000000000000000000, 0.000000000000000000 ) ) ;
#21908=CARTESIAN_POINT ( 'NONE',  ( -1.980830272035999817, 30.09274665651000191, -0.8378900331165000104 ) ) ;
#21921=DIRECTION ( 'NONE',  ( 1.000000000000000000, 0.000000000000000000, 0.000000000000000000 ) ) ;
#21922=CIRCLE ( 'NONE', #18061, 3.000000000000000000 ) ;
#21923=CARTESIAN_POINT ( 'NONE',  ( 1.717816858030654537, 12.95705652094089366, 1.058607149792009094 ) ) ;
#21924=ORIENTED_EDGE ( 'NONE', *, *, #1695, .F. ) ;
#21926=CARTESIAN_POINT ( 'NONE',  ( 0.3414794497234999726, 24.32349665651000237, -2.134113711687000148 ) ) ;
#21930=CARTESIAN_POINT ( 'NONE',  ( 1.536366799937286087, 27.71666666666666501, -1.999167105995451665 ) ) ;
#21931=ORIENTED_EDGE ( 'NONE', *, *, #16453, .T. ) ;
#21934=AXIS2_PLACEMENT_3D ( 'NONE', #3422, #10803, #18196 ) ;
#21936=ORIENTED_EDGE ( 'NONE', *, *, #22523, .T. ) ;
#21937=EDGE_CURVE ( 'NONE', #4988, #3964, #1938, .T. ) ;
#21939=AXIS2_PLACEMENT_3D ( 'NONE', #519, #9618, #17002 ) ;
#21940=CARTESIAN_POINT ( 'NONE',  ( -1.450143669890000098, 24.38504474195000071, -1.580009328412999903 ) ) ;
#21942=PLANE ( 'NONE',  #22977 ) ;
#21944=CARTESIAN_POINT ( 'NONE',  ( 0.6146774451941000583, 30.55152231057000023, -2.279116712825999702 ) ) ;
#21947=CARTESIAN_POINT ( 'NONE',  ( 4.749999884653000493, 15.09999988465641074, -5.093549567505999500E-08 ) ) ;
#21950=LINE ( 'NONE', #21839, #23525 ) ;
#21952=ORIENTED_EDGE ( 'NONE', *, *, #13333, .T. ) ;
#21953=EDGE_CURVE ( 'NONE', #23163, #17341, #12841, .T. ) ;
#21954=CARTESIAN_POINT ( 'NONE',  ( -2.408749103101126554, 30.34919033230260865, -1.018899445479910071 ) ) ;
#21965=EDGE_CURVE ( 'NONE', #9936, #3685, #12663, .T. ) ;
#21969=AXIS2_PLACEMENT_3D ( 'NONE', #14123, #20059, #12317 ) ;
#21972=CARTESIAN_POINT ( 'NONE',  ( 2.095803007753000102, 29.79556831668999806, 0.6294804420801000111 ) ) ;
#21976=CARTESIAN_POINT ( 'NONE',  ( 0.3068592026817785201, 29.98565460010522443, -2.141133321009449642 ) ) ;
#21978=CARTESIAN_POINT ( 'NONE',  ( -0.5691252486112998721, 23.64706705728999836, -2.185498830599999831 ) ) ;
#21981=ORIENTED_EDGE ( 'NONE', *, *, #5128, .T. ) ;
#21985=EDGE_CURVE ( 'NONE', #8412, #17309, #10730, .T. ) ;
#21986=CIRCLE ( 'NONE', #21206, 4.750000000000000000 ) ;
#21988=VERTEX_POINT ( 'NONE', #3640 ) ;
#21989=DIRECTION ( 'NONE',  ( -0.000000000000000000, -1.000000000000000000, -0.000000000000000000 ) ) ;
#21991=FACE_OUTER_BOUND ( 'NONE', #1483, .T. ) ;
#21992=CARTESIAN_POINT ( 'NONE',  ( -4.749999884653000493, 15.09999988465641074, 5.093549627072000020E-08 ) ) ;
#22002=CARTESIAN_POINT ( 'NONE',  ( 2.139890459600042316, 27.42644467189214907, -0.3715313211230960588 ) ) ;
#22004=DIRECTION ( 'NONE',  ( -1.000000000000000000, 0.000000000000000000, 0.000000000000000000 ) ) ;
#22009=CARTESIAN_POINT ( 'NONE',  ( 1.248966013227574168, 24.78517284287330114, 1.711384895940772699 ) ) ;
#22011=DIRECTION ( 'NONE',  ( 0.000000000000000000, -1.000000000000000000, 0.000000000000000000 ) ) ;
#22012=CARTESIAN_POINT ( 'NONE',  ( -1.996229403933999835, 28.69771896306000158, 1.117936111508999852 ) ) ;
#22020=ORIENTED_EDGE ( 'NONE', *, *, #3228, .T. ) ;
#22022=DIRECTION ( 'NONE',  ( 0.000000000000000000, -1.000000000000000000, 0.000000000000000000 ) ) ;
#22029=CARTESIAN_POINT ( 'NONE',  ( 1.846653654530999944, 29.93346240518999934, -1.440075676530000015 ) ) ;
#22033=EDGE_LOOP ( 'NONE', ( #17278, #3725, #5902, #15528 ) ) ;
#22038=CARTESIAN_POINT ( 'NONE',  ( 1.600000000000000089, 9.000000000000000000, 0.000000000000000000 ) ) ;
#22039=CARTESIAN_POINT ( 'NONE',  ( 4.724999999999999645, 13.10000000000000142, 0.000000000000000000 ) ) ;
#22041=CARTESIAN_POINT ( 'NONE',  ( -1.127947703010715230, 29.27359719799922999, -1.846395287258788098 ) ) ;
#22042=FACE_OUTER_BOUND ( 'NONE', #6970, .T. ) ;
#22044=CARTESIAN_POINT ( 'NONE',  ( 2.394884942776999814, 23.89488494277999919, 0.000000000000000000 ) ) ;
#22045=ORIENTED_EDGE ( 'NONE', *, *, #2462, .T. ) ;
#22046=CARTESIAN_POINT ( 'NONE',  ( 2.053067944554000324, 24.18415609745999717, -0.6752492679973999268 ) ) ;
#22049=CARTESIAN_POINT ( 'NONE',  ( -4.624999999996013855, 15.00000000000000000, 0.000000000000000000 ) ) ;
#22057=VERTEX_POINT ( 'NONE', #22049 ) ;
#22059=CARTESIAN_POINT ( 'NONE',  ( -1.802411599998000158, 25.21757922916000183, -1.162178362301999890 ) ) ;
#22064=CARTESIAN_POINT ( 'NONE',  ( 1.344136286029000038, 29.00535257235999964, -1.701023518473999907 ) ) ;
#22068=VERTEX_POINT ( 'NONE', #7220 ) ;
#22072=DIRECTION ( 'NONE',  ( 1.000000000000000000, 0.000000000000000000, 0.000000000000000000 ) ) ;
#22074=EDGE_CURVE ( 'NONE', #12394, #4710, #16506, .T. ) ;
#22078=CARTESIAN_POINT ( 'NONE',  ( -2.665093312283999705, 26.68712896666999868, 0.1571687770952999719 ) ) ;
#22089=CARTESIAN_POINT ( 'NONE',  ( 0.3908479946973999475, 29.99303757602000076, -2.310142352749000150 ) ) ;
#22091=CARTESIAN_POINT ( 'NONE',  ( 2.145295876472778751, 29.81890497885072833, -0.2554101685241636499 ) ) ;
#22093=CARTESIAN_POINT ( 'NONE',  ( -2.322746915978000093, 24.60096985244999956, -0.2454950339001999993 ) ) ;
#22095=CARTESIAN_POINT ( 'NONE',  ( 0.000000000000000000, 19.00000000000000000, 0.000000000000000000 ) ) ;
#22103=ORIENTED_EDGE ( 'NONE', *, *, #14723, .F. ) ;
#22108=VERTEX_POINT ( 'NONE', #7106 ) ;
#22117=CARTESIAN_POINT ( 'NONE',  ( -1.549481145645184021, 27.90346540521953145, 1.523379885845690618 ) ) ;
#22119=CARTESIAN_POINT ( 'NONE',  ( 1.687576972922000040, 28.34000240010000127, 2.322750540216000026 ) ) ;
#22120=CARTESIAN_POINT ( 'NONE',  ( 1.766725490425707035, 30.68186832659927532, -1.242484399774119508 ) ) ;
#22123=DIRECTION ( 'NONE',  ( -1.351954405892998782E-08, -0.9999999999999990008, -4.357971222333990821E-08 ) ) ;
#22125=CARTESIAN_POINT ( 'NONE',  ( -1.195388535980999922, 28.50271896306000485, -1.950678319476999878 ) ) ;
#22127=CARTESIAN_POINT ( 'NONE',  ( -2.130581439410940359, 30.85744147019555328, 0.2262312255918205728 ) ) ;
#22138=CARTESIAN_POINT ( 'NONE',  ( 0.000000000000000000, 24.50000000000000000, 0.000000000000000000 ) ) ;
#22139=CARTESIAN_POINT ( 'NONE',  ( 2.214406098997000250, 29.00694631853999894, 0.7617925945809999044 ) ) ;
#22140=ADVANCED_FACE ( 'NONE', ( #12184 ), #13056, .F. ) ;
#22145=CARTESIAN_POINT ( 'NONE',  ( -1.259047450927232026, 28.93333333333333712, 2.184465970885653974 ) ) ;
#22148=ORIENTED_EDGE ( 'NONE', *, *, #22393, .F. ) ;
#22152=CARTESIAN_POINT ( 'NONE',  ( 0.3047452333598806851, 29.18569219383820013, -2.138379523722714115 ) ) ;
#22155=EDGE_CURVE ( 'NONE', #19900, #9967, #23461, .T. ) ;
#22156=CARTESIAN_POINT ( 'NONE',  ( -1.767805011140364924, 26.50018596745192312, 1.767686163102024643 ) ) ;
#22158=CARTESIAN_POINT ( 'NONE',  ( -2.193166068984999661, 23.80189877136000121, -0.8531035950795999856 ) ) ;
#22162=DIRECTION ( 'NONE',  ( -1.000000000000000000, 0.000000000000000000, 0.000000000000000000 ) ) ;
#22164=EDGE_LOOP ( 'NONE', ( #10638, #19034, #19519, #9938 ) ) ;
#22166=CARTESIAN_POINT ( 'NONE',  ( 0.000000000000000000, 31.00000000000000000, 0.000000000000000000 ) ) ;
#22168=ORIENTED_EDGE ( 'NONE', *, *, #4039, .T. ) ;
#22170=CARTESIAN_POINT ( 'NONE',  ( 2.103662084068000038, 24.72789791218000133, 1.013534942017999985 ) ) ;
#22172=DIRECTION ( 'NONE',  ( 0.000000000000000000, -1.000000000000000000, 0.000000000000000000 ) ) ;
#22174=CARTESIAN_POINT ( 'NONE',  ( 0.3237282180201000448, 29.40258014098999695, 2.338245789995000212 ) ) ;
#22180=CARTESIAN_POINT ( 'NONE',  ( -1.944991678923578826, 24.14582603393633775, -1.623355076449641388 ) ) ;
#22188=CARTESIAN_POINT ( 'NONE',  ( -0.6232602838478999985, 25.81756359724000305, -2.388357610153000188 ) ) ;
#22189=ORIENTED_EDGE ( 'NONE', *, *, #6674, .F. ) ;
#22193=DIRECTION ( 'NONE',  ( 0.000000000000000000, 1.000000000000000000, 0.000000000000000000 ) ) ;
#22200=CARTESIAN_POINT ( 'NONE',  ( 1.545690893027000135, 28.68824721936999822, 1.555291323814000037 ) ) ;
#22202=CARTESIAN_POINT ( 'NONE',  ( -0.05303640295588081532, 29.60074729647491409, 2.159234738230836559 ) ) ;
#22204=CARTESIAN_POINT ( 'NONE',  ( -1.617171946415000061, 25.28260575739999894, 1.470668775339999845 ) ) ;
#22206=CARTESIAN_POINT ( 'NONE',  ( -1.963703823225463774, 26.25920717875808563, 0.8995588027868727243 ) ) ;
#22213=CARTESIAN_POINT ( 'NONE',  ( -0.3272492347489122655, 28.41753006952333749, 2.500000000000003553 ) ) ;
#22216=DIRECTION ( 'NONE',  ( -8.881784197001252323E-16, 0.000000000000000000, 1.000000000000000000 ) ) ;
#22225=DIRECTION ( 'NONE',  ( 0.7071067811864258923, 0.7071067811862259411, 7.917084081357289653E-07 ) ) ;
#22228=ORIENTED_EDGE ( 'NONE', *, *, #6087, .F. ) ;
#22230=CARTESIAN_POINT ( 'NONE',  ( 1.649278745378622180, 24.74235546451014400, 1.391239989081180406 ) ) ;
#22232=CARTESIAN_POINT ( 'NONE',  ( 0.1346854910757999679, 27.62521896306000357, -2.283846754818999791 ) ) ;
#22233=CONICAL_SURFACE ( 'NONE', #2931, 4.309401076758999416, 1.119376321708719590 ) ;
#22235=EDGE_LOOP ( 'NONE', ( #23622, #13171, #9638, #16347, #13838, #17984 ) ) ;
#22239=DIRECTION ( 'NONE',  ( 0.000000000000000000, -1.000000000000000000, 0.000000000000000000 ) ) ;
#22240=ORIENTED_EDGE ( 'NONE', *, *, #5417, .T. ) ;
#22246=CARTESIAN_POINT ( 'NONE',  ( -0.4122572571062000368, 29.27166520044000109, -2.305209684642999690 ) ) ;
#22251=CARTESIAN_POINT ( 'NONE',  ( -2.500000000000000000, 28.80000000000000071, 0.000000000000000000 ) ) ;
#22253=DIRECTION ( 'NONE',  ( 0.7071067811823850136, 0.7071067811898851252, 1.080116765722976056E-06 ) ) ;
#22254=ORIENTED_EDGE ( 'NONE', *, *, #7702, .T. ) ;
#22258=CARTESIAN_POINT ( 'NONE',  ( 1.960055799040040236, 29.05894037691824394, -0.9073345561690950856 ) ) ;
#22263=B_SPLINE_CURVE_WITH_KNOTS ( 'NONE', 3,
 ( #8413, #13847, #10224, #2962 ),
 .UNSPECIFIED., .F., .F.,
 ( 4, 4 ),
 ( 0.000000000000000000, 1.000000000000000000 ),
 .UNSPECIFIED. ) ;
#22264=CARTESIAN_POINT ( 'NONE',  ( -0.6416724176654999834, 23.68578163881999998, -2.183283362266000172 ) ) ;
#22265=ADVANCED_FACE ( 'NONE', ( #23652, #10468 ), #21356, .T. ) ;
#22267=CARTESIAN_POINT ( 'NONE',  ( 1.603022320644999832, 27.19049822781000003, 1.603022320644999832 ) ) ;
#22268=FACE_OUTER_BOUND ( 'NONE', #16141, .T. ) ;
#22269=ADVANCED_FACE ( 'NONE', ( #14443 ), #16520, .F. ) ;
#22270=AXIS2_PLACEMENT_3D ( 'NONE', #11703, #4433, #23063 ) ;
#22274=DIRECTION ( 'NONE',  ( 0.5000000000000169864, 0.000000000000000000, 0.8660254037844289376 ) ) ;
#22278=EDGE_CURVE ( 'NONE', #6193, #11323, #4140, .T. ) ;
#22281=CARTESIAN_POINT ( 'NONE',  ( -0.5541245210720000536, 24.21556899698000009, -2.268390014031999691 ) ) ;
#22285=CARTESIAN_POINT ( 'NONE',  ( -2.135020154818999760, 29.15352773921999940, 1.400017537060999961 ) ) ;
#22289=CARTESIAN_POINT ( 'NONE',  ( -2.500000000000000444, 26.65086340285667177, 0.3272492347489422415 ) ) ;
#22290=AXIS2_PLACEMENT_3D ( 'NONE', #2600, #1274, #12301 ) ;
#22292=ORIENTED_EDGE ( 'NONE', *, *, #1828, .F. ) ;
#22293=CARTESIAN_POINT ( 'NONE',  ( 0.4737338993650556107, 24.45831145367538895, 2.488861676985053784 ) ) ;
#22294=B_SPLINE_CURVE_WITH_KNOTS ( 'NONE', 3,
 ( #10100, #15778, #8038, #11799 ),
 .UNSPECIFIED., .F., .F.,
 ( 4, 4 ),
 ( 0.000000000000000000, 1.000000000000000000 ),
 .UNSPECIFIED. ) ;
#22295=CARTESIAN_POINT ( 'NONE',  ( 2.218255378514000675, 23.92992329518563821, -1.026110373679216536 ) ) ;
#22296=EDGE_LOOP ( 'NONE', ( #21411, #11854, #8239, #18137, #12543, #15363, #11708, #23678, #6614, #22454, #7896, #22870 ) ) ;
#22302=AXIS2_PLACEMENT_3D ( 'NONE', #11626, #19113, #15229 ) ;
#22303=CARTESIAN_POINT ( 'NONE',  ( 1.304555153736000062, 25.61462896666999711, -2.329463490920999913 ) ) ;
#22305=ORIENTED_EDGE ( 'NONE', *, *, #22539, .T. ) ;
#22306=VECTOR ( 'NONE', #7553, 1000.000000000000114 ) ;
#22309=LINE ( 'NONE', #2089, #7866 ) ;
#22310=ORIENTED_EDGE ( 'NONE', *, *, #1640, .T. ) ;
#22316=CARTESIAN_POINT ( 'NONE',  ( 1.349135513845000078, 29.14813513062999917, -1.722924400667999789 ) ) ;
#22319=CARTESIAN_POINT ( 'NONE',  ( 0.9601661138225395797, 29.66260720285410812, 1.934687070640197737 ) ) ;
#22322=CARTESIAN_POINT ( 'NONE',  ( -2.142313624094999813, 25.45688484113999905, 0.4115616050618999822 ) ) ;
#22331=VECTOR ( 'NONE', #17404, 1000.000000000000114 ) ;
#22335=ORIENTED_EDGE ( 'NONE', *, *, #22345, .T. ) ;
#22342=CARTESIAN_POINT ( 'NONE',  ( 0.000000000000000000, -1.550000000000000044, 0.000000000000000000 ) ) ;
#22343=FILL_AREA_STYLE_COLOUR ( '', #13077 ) ;
#22345=EDGE_CURVE ( 'NONE', #16051, #21619, #20546, .T. ) ;
#22346=CARTESIAN_POINT ( 'NONE',  ( 2.022356098371595134, 30.55380357660929747, 0.8395515573483458560 ) ) ;
#22347=EDGE_LOOP ( 'NONE', ( #1802, #9437, #7180, #5200 ) ) ;
#22350=CARTESIAN_POINT ( 'NONE',  ( -2.143277222256999792, 23.64327722226000006, 4.118360636503000477E-13 ) ) ;
#22352=AXIS2_PLACEMENT_3D ( 'NONE', #23653, #7060, #12859 ) ;
#22354=CARTESIAN_POINT ( 'NONE',  ( 1.854615231836999945, 26.30864211382000306, 1.347456777940000183 ) ) ;
#22355=CARTESIAN_POINT ( 'NONE',  ( -2.131902921039358745, 30.85616845379279383, 0.2258430825467815373 ) ) ;
#22357=VERTEX_POINT ( 'NONE', #7402 ) ;
#22358=TOROIDAL_SURFACE ( 'NONE', #21608, 2.500000000000000000, 0.5500000000000000444 ) ;
#22363=AXIS2_PLACEMENT_3D ( 'NONE', #890, #1015, #20889 ) ;
#22364=DIRECTION ( 'NONE',  ( 0.000000000000000000, 0.7071067811866525998, -0.7071067811864425456 ) ) ;
#22365=ORIENTED_EDGE ( 'NONE', *, *, #477, .T. ) ;
#22369=DIRECTION ( 'NONE',  ( 0.000000000000000000, 1.000000000000000000, 0.000000000000000000 ) ) ;
#22372=CARTESIAN_POINT ( 'NONE',  ( -1.657661551580862591, 30.87634082601233132, -1.328962299251567059 ) ) ;
#22376=AXIS2_PLACEMENT_3D ( 'NONE', #2156, #2512, #3980 ) ;
#22383=CARTESIAN_POINT ( 'NONE',  ( 1.982538622003251705, 29.05572842088777463, -0.8582355642374253080 ) ) ;
#22387=CARTESIAN_POINT ( 'NONE',  ( 1.699997194034733150, 11.63334146140299907, 1.053569902902707689 ) ) ;
#22390=CARTESIAN_POINT ( 'NONE',  ( 0.8867402482005000142, 25.08986973128999765, -1.970974702784000110 ) ) ;
#22392=CARTESIAN_POINT ( 'NONE',  ( 0.4858445502738999999, 28.26299822781000159, -2.214344957515000267 ) ) ;
#22393=EDGE_CURVE ( 'NONE', #3216, #14191, #7234, .T. ) ;
#22395=DIRECTION ( 'NONE',  ( 1.000000000000000000, 0.000000000000000000, 0.000000000000000000 ) ) ;
#22396=DIRECTION ( 'NONE',  ( 0.000000000000000000, -1.000000000000000000, 0.000000000000000000 ) ) ;
#22397=DIRECTION ( 'NONE',  ( 0.000000000000000000, -1.000000000000000000, 0.000000000000000000 ) ) ;
#22398=AXIS2_PLACEMENT_3D ( 'NONE', #8246, #17320, #6660 ) ;
#22400=AXIS2_PLACEMENT_3D ( 'NONE', #5297, #14608, #22004 ) ;
#22405=EDGE_LOOP ( 'NONE', ( #8925, #3481, #12815, #17437 ) ) ;
#22407=CARTESIAN_POINT ( 'NONE',  ( 1.327909667750000189, 24.70915199424000264, -2.369304801069999744 ) ) ;
#22409=DIRECTION ( 'NONE',  ( 0.000000000000000000, -0.7071067811866525998, -0.7071067811864425456 ) ) ;
#22412=CARTESIAN_POINT ( 'NONE',  ( -0.9467533411658000109, 29.72799882400999749, -2.371079559876999809 ) ) ;
#22416=AXIS2_PLACEMENT_3D ( 'NONE', #9893, #22369, #437 ) ;
#22422=CARTESIAN_POINT ( 'NONE',  ( 2.500000000000000000, 27.83419673618999823, 0.000000000000000000 ) ) ;
#22425=AXIS2_PLACEMENT_3D ( 'NONE', #6290, #13921, #15848 ) ;
#22427=DIRECTION ( 'NONE',  ( 0.000000000000000000, 0.7071067811866525998, -0.7071067811864425456 ) ) ;
#22428=CARTESIAN_POINT ( 'NONE',  ( 1.887779699469000150, 26.97962896666999910, 1.887779699469000150 ) ) ;
#22432=DIRECTION ( 'NONE',  ( -9.309572557292000170E-11, 0.000000000000000000, 1.000000000000000000 ) ) ;
#22440=CARTESIAN_POINT ( 'NONE',  ( -1.020771968315000056, 30.12698763284999970, 1.940619092743999907 ) ) ;
#22442=CARTESIAN_POINT ( 'NONE',  ( 1.417757377811232677, 29.69484876337556045, 1.629552333889765281 ) ) ;
#22444=CARTESIAN_POINT ( 'NONE',  ( -0.6125396999611999460, 25.59648037213999672, 2.093726834476999699 ) ) ;
#22447=ORIENTED_EDGE ( 'NONE', *, *, #751, .T. ) ;
#22451=EDGE_CURVE ( 'NONE', #15250, #14519, #6703, .T. ) ;
#22454=ORIENTED_EDGE ( 'NONE', *, *, #3763, .F. ) ;
#22456=DIRECTION ( 'NONE',  ( 0.000000000000000000, 0.000000000000000000, -1.000000000000000000 ) ) ;
#22459=CARTESIAN_POINT ( 'NONE',  ( 3.100000000000000089, 20.00000000000000000, 0.000000000000000000 ) ) ;
#22463=CARTESIAN_POINT ( 'NONE',  ( 4.624999963076000142, 12.99999996307999872, 4.214403195776000249E-08 ) ) ;
#22465=CARTESIAN_POINT ( 'NONE',  ( -2.000000000000000000, 26.50000000000000355, -3.464101615137999968 ) ) ;
#22467=CARTESIAN_POINT ( 'NONE',  ( 1.536366799937286087, 27.95086340285666537, -1.999167105995451221 ) ) ;
#22468=CARTESIAN_POINT ( 'NONE',  ( -0.8956276177791392401, 30.34935011684900985, 1.967630924038994422 ) ) ;
#22469=EDGE_LOOP ( 'NONE', ( #12514, #1852, #9243 ) ) ;
#22475=FACE_OUTER_BOUND ( 'NONE', #8320, .T. ) ;
#22485=LINE ( 'NONE', #2631, #14285 ) ;
#22488=CARTESIAN_POINT ( 'NONE',  ( -0.8612498596054259936, 30.84999136413794218, -1.988030992341762504 ) ) ;
#22501=CIRCLE ( 'NONE', #7050, 2.270871215252209030 ) ;
#22505=CARTESIAN_POINT ( 'NONE',  ( -2.193530619437999984, 28.45799822781000188, -0.5724186824819998964 ) ) ;
#22512=AXIS2_PLACEMENT_3D ( 'NONE', #3537, #10920, #16111 ) ;
#22517=CARTESIAN_POINT ( 'NONE',  ( 2.478439802523999980, 25.45499776881999665, 0.4854719611819000580 ) ) ;
#22522=CARTESIAN_POINT ( 'NONE',  ( -0.8235893797016999862, 28.43543888322000157, 2.276936129739000059 ) ) ;
#22523=EDGE_CURVE ( 'NONE', #2273, #13340, #4945, .T. ) ;
#22525=DIRECTION ( 'NONE',  ( 0.000000000000000000, 1.000000000000000000, 0.000000000000000000 ) ) ;
#22527=CARTESIAN_POINT ( 'NONE',  ( 0.6543697108981985089, 29.60086340285667461, -2.434931691670790599 ) ) ;
#22531=EDGE_CURVE ( 'NONE', #9729, #12880, #8015, .T. ) ;
#22533=CARTESIAN_POINT ( 'NONE',  ( -0.3396743697608000101, 25.47584390253999942, -2.715985394886999860 ) ) ;
#22538=DIRECTION ( 'NONE',  ( 1.000000000000000000, 0.000000000000000000, 0.000000000000000000 ) ) ;
#22539=EDGE_CURVE ( 'NONE', #20510, #551, #6266, .T. ) ;
#22540=CARTESIAN_POINT ( 'NONE',  ( -2.276308483783000103, 25.80962896666999740, -1.394936847711000016 ) ) ;
#22545=DIRECTION ( 'NONE',  ( -0.5000000000000169864, 0.000000000000000000, -0.8660254037844288266 ) ) ;
#22547=ORIENTED_EDGE ( 'NONE', *, *, #9047, .T. ) ;
#22554=CARTESIAN_POINT ( 'NONE',  ( 0.2174393203624000181, 28.97599530207000029, -2.181902348697000171 ) ) ;
#22558=CARTESIAN_POINT ( 'NONE',  ( 0.6136530736515161122, 29.64045887480123653, 2.071129839369229675 ) ) ;
#22560=CARTESIAN_POINT ( 'NONE',  ( 2.296839136161000106, 25.59511910883000141, 0.4914911606428001289 ) ) ;
#22561=CARTESIAN_POINT ( 'NONE',  ( 2.270871215252209030, 19.00000000000000000, 0.000000000000000000 ) ) ;
#22571=B_SPLINE_CURVE_WITH_KNOTS ( 'NONE', 3,
 ( #2745, #17514, #908, #4686, #12072, #1166, #19455, #17637, #1035, #23195, #6611, #21389, #4804, #2985, #15316, #12550, #18347, #7198, #18002, #10854, #18236 ),
 .UNSPECIFIED., .F., .F.,
 ( 4, 1, 1, 1, 1, 1, 1, 1, 1, 1, 1, 1, 1, 1, 1, 1, 1, 1, 4 ),
 ( 0.4517522507388516129, 0.4675004193362445881, 0.5000002515996020414, 0.5325000838631117617, 0.5649999161264690484, 0.5974997483898265571, 0.6299995806531840659, 0.6624994129165413526, 0.6949992451800510729, 0.7274990774434085816, 0.7599989097067658683, 0.7924987419701232660, 0.8249985742334806638, 0.8574984064968381725, 0.8899982387603480039, 0.9224980710237052905, 0.9549979032870627993, 0.9874977355504200860, 1.000000000000000000 ),
 .UNSPECIFIED. ) ;
#22573=CARTESIAN_POINT ( 'NONE',  ( 0.000000000000000000, 21.94999982584599962, 0.000000000000000000 ) ) ;
#22583=ADVANCED_FACE ( 'NONE', ( #10480 ), #21736, .T. ) ;
#22585=CARTESIAN_POINT ( 'NONE',  ( 2.000000000000000000, 26.50000000000000355, -3.464101615137999968 ) ) ;
#22586=CARTESIAN_POINT ( 'NONE',  ( -1.259047450927251788, 28.10086340285667106, -2.184465970885643316 ) ) ;
#22587=CARTESIAN_POINT ( 'NONE',  ( 0.9083774594092118848, 30.45919981329474879, 1.959565387789651059 ) ) ;
#22593=DIRECTION ( 'NONE',  ( 0.000000000000000000, 1.000000000000000000, 0.000000000000000000 ) ) ;
#22594=CIRCLE ( 'NONE', #19903, 2.750000000000000000 ) ;
#22599=TOROIDAL_SURFACE ( 'NONE', #20298, 3.000000000000000000, 1.000000000000000000 ) ;
#22600=CARTESIAN_POINT ( 'NONE',  ( 2.126485824405467628, 28.06267154637892247, -0.5579182477979972576 ) ) ;
#22602=ORIENTED_EDGE ( 'NONE', *, *, #4489, .F. ) ;
#22611=DIRECTION ( 'NONE',  ( 0.000000000000000000, 1.000000000000000000, 0.000000000000000000 ) ) ;
#22613=DIRECTION ( 'NONE',  ( 0.000000000000000000, 0.000000000000000000, -1.000000000000000000 ) ) ;
#22614=CARTESIAN_POINT ( 'NONE',  ( -1.595084814687000030, 26.58500240009999871, 2.387212940976999764 ) ) ;
#22620=FACE_OUTER_BOUND ( 'NONE', #22164, .T. ) ;
#22623=CARTESIAN_POINT ( 'NONE',  ( -0.7160459369171999766, 28.54756359724000347, 2.361836001938000251 ) ) ;
#22624=CYLINDRICAL_SURFACE ( 'NONE', #10361, 4.724999999999999645 ) ;
#22628=CARTESIAN_POINT ( 'NONE',  ( 0.000000000000000000, 19.00000000000000000, 0.000000000000000000 ) ) ;
#22631=CARTESIAN_POINT ( 'NONE',  ( 2.712095028381999562, 24.58106976543999878, -0.1465942787552000082 ) ) ;
#22634=CARTESIAN_POINT ( 'NONE',  ( 0.000000000000000000, 26.35000000000000142, 0.000000000000000000 ) ) ;
#22635=CARTESIAN_POINT ( 'NONE',  ( -2.088906529886999763, 30.48427082063000171, -1.781945689819999901 ) ) ;
#22641=DIRECTION ( 'NONE',  ( 1.000000000000000000, 0.000000000000000000, 0.000000000000000000 ) ) ;
#22644=DIRECTION ( 'NONE',  ( -1.000000000000000000, 0.000000000000000000, 0.000000000000000000 ) ) ;
#22645=EDGE_LOOP ( 'NONE', ( #2859, #19851, #13066, #6736 ) ) ;
#22648=CARTESIAN_POINT ( 'NONE',  ( -0.8638410262558590125, 23.95255680022374989, 2.016069985583057722 ) ) ;
#22660=FACE_OUTER_BOUND ( 'NONE', #4895, .T. ) ;
#22661=ORIENTED_EDGE ( 'NONE', *, *, #20223, .F. ) ;
#22668=CARTESIAN_POINT ( 'NONE',  ( 0.3657816702587000091, 29.76730252947999844, -2.161985579530000035 ) ) ;
#22670=EDGE_CURVE ( 'NONE', #8412, #12128, #15160, .T. ) ;
#22671=CARTESIAN_POINT ( 'NONE',  ( 0.4174375083360183369, 29.62843580719651015, 2.119604069544729796 ) ) ;
#22674=CARTESIAN_POINT ( 'NONE',  ( 2.091247443629999925, 24.02624597840999954, -0.6362363528857999384 ) ) ;
#22675=DIRECTION ( 'NONE',  ( 1.351954405892998782E-08, -0.9999999999999990008, 4.357971159552991384E-08 ) ) ;
#22676=ORIENTED_EDGE ( 'NONE', *, *, #6674, .T. ) ;
#22677=CARTESIAN_POINT ( 'NONE',  ( -2.500000000000000000, 28.23419673618999681, 0.000000000000000000 ) ) ;
#22686=ORIENTED_EDGE ( 'NONE', *, *, #16370, .F. ) ;
#22687=CARTESIAN_POINT ( 'NONE',  ( 0.000000000000000000, 19.04999994433000055, 0.000000000000000000 ) ) ;
#22697=VECTOR ( 'NONE', #12291, 1000.000000000000000 ) ;
#22698=CARTESIAN_POINT ( 'NONE',  ( -1.536366799937290084, 28.91753006952332328, -1.999167105995447669 ) ) ;
#22700=ADVANCED_FACE ( 'NONE', ( #11422 ), #18794, .T. ) ;
#22701=CARTESIAN_POINT ( 'NONE',  ( -0.1032420033594618897, 30.39770183657784841, 2.157430679839748677 ) ) ;
#22702=VERTEX_POINT ( 'NONE', #9477 ) ;
#22703=EDGE_CURVE ( 'NONE', #21511, #21635, #7437, .T. ) ;
#22708=CARTESIAN_POINT ( 'NONE',  ( 2.291988582794999729, 27.18614211382000079, 0.04500887484482999495 ) ) ;
#22709=CIRCLE ( 'NONE', #1844, 1.999999999999998668 ) ;
#22713=EDGE_CURVE ( 'NONE', #1589, #14786, #9246, .T. ) ;
#22714=DIRECTION ( 'NONE',  ( 0.7071067811905932254, 0.7071067811824932603, 1.099460927037990408E-07 ) ) ;
#22716=CARTESIAN_POINT ( 'NONE',  ( -2.135272182958257492, 27.60654271691555905, -0.3931785795488860757 ) ) ;
#22718=ORIENTED_EDGE ( 'NONE', *, *, #17430, .F. ) ;
#22725=CIRCLE ( 'NONE', #12693, 4.625000000000000000 ) ;
#22728=CARTESIAN_POINT ( 'NONE',  ( 4.000000000000058620, 24.75094615492120553, -2.107036910272262364 ) ) ;
#22731=CARTESIAN_POINT ( 'NONE',  ( -0.3657850755361999884, 28.13706776952000155, 2.644546391786999795 ) ) ;
#22733=CARTESIAN_POINT ( 'NONE',  ( 2.158192071364979370, 28.99867104832394560, 0.08873628542675822406 ) ) ;
#22743=CONICAL_SURFACE ( 'NONE', #1879, 4.649999883068000273, 0.7853981633972997312 ) ;
#22750=ORIENTED_EDGE ( 'NONE', *, *, #10633, .F. ) ;
#22752=CARTESIAN_POINT ( 'NONE',  ( -2.709454201502000004, 24.96531645185000059, -0.1892281976294000190 ) ) ;
#22757=CARTESIAN_POINT ( 'NONE',  ( 0.000000000000000000, 18.50000000000000000, 0.000000000000000000 ) ) ;
#22760=DIRECTION ( 'NONE',  ( 1.000000000000000000, 0.000000000000000000, 0.000000000000000000 ) ) ;
#22766=EDGE_LOOP ( 'NONE', ( #16489, #3600, #21519, #19109 ) ) ;
#22767=CIRCLE ( 'NONE', #10033, 4.750000000000000000 ) ;
#22768=DIRECTION ( 'NONE',  ( 0.000000000000000000, 0.000000000000000000, -1.000000000000000000 ) ) ;
#22778=CARTESIAN_POINT ( 'NONE',  ( -0.1529142988638288181, 26.50000000000000355, -2.395123632968240823 ) ) ;
#22783=CARTESIAN_POINT ( 'NONE',  ( 1.724048102327889520, 12.96513651749977214, -1.060396748501814868 ) ) ;
#22788=CARTESIAN_POINT ( 'NONE',  ( 1.660950793280000060, 28.72156950879999826, 1.671267114093999862 ) ) ;
#22793=CARTESIAN_POINT ( 'NONE',  ( -0.8197724292390062839, 29.55421540811686398, 2.000496916279093540 ) ) ;
#22795=CARTESIAN_POINT ( 'NONE',  ( -0.07403871084495999844, 24.61795039184000089, 2.347720816621999607 ) ) ;
#22797=ORIENTED_EDGE ( 'NONE', *, *, #5517, .F. ) ;
#22799=CARTESIAN_POINT ( 'NONE',  ( -2.500000000000000000, 26.63419673618999894, 0.000000000000000000 ) ) ;
#22802=ORIENTED_EDGE ( 'NONE', *, *, #18262, .T. ) ;
#22808=CARTESIAN_POINT ( 'NONE',  ( 4.000000000000000000, 26.31534065533125144, -1.802053058880663805 ) ) ;
#22817=CARTESIAN_POINT ( 'NONE',  ( 0.000000000000000000, 7.100000000000000533, 0.000000000000000000 ) ) ;
#22818=B_SPLINE_CURVE_WITH_KNOTS ( 'NONE', 3,
 ( #13762, #11967, #21164, #15460, #8327, #4575, #22845, #23083, #19356, #21294, #6258, #3007, #2883, #10266, #1183, #10392, #17654, #1053, #8454, #15821, #23212, #14017, #21407, #18254, #18146, #21657, #5415, #5070, #7339, #3249, #3135, #22117, #1423, #12800, #14607, #12903, #20074, #18363, #1549, #20187, #10635, #7102, #16058, #8935, #16539, #23930, #6989, #3597, #22002, #12453, #14720, #19836, #3489, #10751, #5524, #18022, #10980, #10519, #16182, #16303, #1775, #17902, #8694, #21884, #1305, #12566, #5184, #1656, #9162, #23453, #8823, #19954, #6867, #14259, #12686, #23585, #23694, #14378, #10869, #21772, #14492, #3373, #5295, #9045, #16417, #23807 ),
 .UNSPECIFIED., .F., .F.,
 ( 4, 2, 1, 2, 2, 2, 2, 2, 2, 1, 2, 2, 2, 2, 2, 2, 1, 2, 2, 2, 2, 2, 2, 2, 2, 1, 2, 2, 2, 2, 2, 2, 1, 2, 2, 2, 2, 2, 2, 2, 1, 2, 2, 2, 2, 4 ),
 ( 0.000000000000000000, 0.01325029465915758195, 0.02650058931831516390, 0.03975088397747275626, 0.05300117863663034862, 0.07950176795494552640, 0.1060023572732606972, 0.1325029465915758820, 0.1457532412507334951, 0.1590035359098910805, 0.1722538305690486660, 0.1855041252282062791, 0.2120047145465215055, 0.2385053038648367041, 0.2650058931831518749, 0.2782561878423095436, 0.2915064825014671568, 0.3047567771606247700, 0.3180070718197824386, 0.3312573664789400518, 0.3445076611380976095, 0.3710082504564127803, 0.3975088397747280067, 0.4240094290930431775, 0.4372597237522007907, 0.4505100184113584039, 0.4637603130705159060, 0.4770106077296734637, 0.5035111970479886345, 0.5300117863663037499, 0.5565123756846189762, 0.5697626703437765894, 0.5830129650029342026, 0.5962632596620918157, 0.6095135543212493179, 0.6360141436395645442, 0.6625147329578798816, 0.6890153222761951080, 0.7155159115945103343, 0.7287662062536679475, 0.7420165009128254496, 0.7552667955719830628, 0.7685170902311406760, 0.7950176795494559023, 0.8215182688677710177, 0.8480188581860863550 ),
 .UNSPECIFIED. ) ;
#22819=CARTESIAN_POINT ( 'NONE',  ( 0.7318187998270080374, 26.37490599056236817, -4.196286372439437251 ) ) ;
#22820=CARTESIAN_POINT ( 'NONE',  ( 0.000000000000000000, 21.89999999999999858, 0.000000000000000000 ) ) ;
#22821=EDGE_CURVE ( 'NONE', #16017, #16978, #1759, .T. ) ;
#22822=CARTESIAN_POINT ( 'NONE',  ( -0.3725721029586212540, 30.38186967353806978, 2.129277066162170939 ) ) ;
#22828=CARTESIAN_POINT ( 'NONE',  ( 0.1349572241792000027, 27.38114211381999752, -2.288454502553999959 ) ) ;
#22837=EDGE_CURVE ( 'NONE', #5348, #11953, #16331, .T. ) ;
#22845=CARTESIAN_POINT ( 'NONE',  ( -1.874306020383145643, 28.67199880806925094, 1.099966823684755957 ) ) ;
#22848=EDGE_CURVE ( 'NONE', #22108, #23527, #10323, .T. ) ;
#22851=CARTESIAN_POINT ( 'NONE',  ( -3.000000000000000000, 17.89999999999999858, 0.000000000000000000 ) ) ;
#22852=CARTESIAN_POINT ( 'NONE',  ( 2.219793368323999871, 28.42956776951999842, -1.483218624018999954 ) ) ;
#22855=CARTESIAN_POINT ( 'NONE',  ( 2.156475325630220485, 28.99669585034901331, 0.1219500803027313146 ) ) ;
#22861=CARTESIAN_POINT ( 'NONE',  ( -4.000000000000000000, 26.50000000000000355, 0.000000000000000000 ) ) ;
#22863=CARTESIAN_POINT ( 'NONE',  ( -0.6074916215089999350, 30.83999999999999986, -2.072813047478000215 ) ) ;
#22869=CARTESIAN_POINT ( 'NONE',  ( 1.536366799937295413, 27.48333333333333073, 1.999167105995444338 ) ) ;
#22870=ORIENTED_EDGE ( 'NONE', *, *, #3583, .T. ) ;
#22872=CARTESIAN_POINT ( 'NONE',  ( 1.937464785723999938, 25.39095665442000183, 1.620130890068999907 ) ) ;
#22877=CARTESIAN_POINT ( 'NONE',  ( 1.699999999999999956, 13.00000000000000000, 1.053565375285000050 ) ) ;
#22884=CARTESIAN_POINT ( 'NONE',  ( -1.999167105995453442, 29.75086340285666253, -1.536366799937283645 ) ) ;
#22890=CARTESIAN_POINT ( 'NONE',  ( 1.626223296995356726, 24.10999786935245837, 1.471899765573001506 ) ) ;
#22894=CARTESIAN_POINT ( 'NONE',  ( 0.000000000000000000, 17.95000004008999994, 0.000000000000000000 ) ) ;
#22895=CARTESIAN_POINT ( 'NONE',  ( -2.183184479328999839, 26.48419433609999984, -1.864615697012000028 ) ) ;
#22900=FACE_OUTER_BOUND ( 'NONE', #22766, .T. ) ;
#22901=ORIENTED_EDGE ( 'NONE', *, *, #17675, .T. ) ;
#22903=CARTESIAN_POINT ( 'NONE',  ( -2.000000000000000000, 31.00000000000000000, 0.000000000000000000 ) ) ;
#22909=AXIS2_PLACEMENT_3D ( 'NONE', #22166, #12957, #20355 ) ;
#22911=CARTESIAN_POINT ( 'NONE',  ( -1.517536029622082783, 29.50471637792290025, 1.536878451077771768 ) ) ;
#22912=EDGE_LOOP ( 'NONE', ( #9982, #8953, #7254 ) ) ;
#22913=CARTESIAN_POINT ( 'NONE',  ( 2.247188694785000163, 24.05956826785000047, -0.6836795634928000132 ) ) ;
#22916=CARTESIAN_POINT ( 'NONE',  ( -3.574282176492461098E-06, 28.76916452463145291, 2.098900968869932715 ) ) ;
#22918=CARTESIAN_POINT ( 'NONE',  ( -2.141135906240991371, 30.84841738671447331, 0.2119206051068452390 ) ) ;
#22921=ORIENTED_EDGE ( 'NONE', *, *, #12669, .F. ) ;
#22922=AXIS2_PLACEMENT_3D ( 'NONE', #13306, #3885, #7503 ) ;
#22924=CARTESIAN_POINT ( 'NONE',  ( -1.259047450927251566, 27.06666666666667354, -2.184465970885643316 ) ) ;
#22927=VERTEX_POINT ( 'NONE', #15390 ) ;
#22930=DIRECTION ( 'NONE',  ( -1.000000000000000000, 0.000000000000000000, 0.000000000000000000 ) ) ;
#22940=CARTESIAN_POINT ( 'NONE',  ( -0.7323698196505201707, 30.04763029221750514, -2.036741068021854506 ) ) ;
#22944=CARTESIAN_POINT ( 'NONE',  ( -1.177500171710576859, 23.61738672577268972, -1.759779639892373959 ) ) ;
#22948=AXIS2_PLACEMENT_3D ( 'NONE', #6343, #9861, #13726 ) ;
#22953=LINE ( 'NONE', #2496, #15231 ) ;
#22954=CARTESIAN_POINT ( 'NONE',  ( 0.000000000000000000, 23.00000000000000000, 0.000000000000000000 ) ) ;
#22955=EDGE_CURVE ( 'NONE', #14560, #3493, #20676, .T. ) ;
#22964=DIRECTION ( 'NONE',  ( 1.000000000000000000, 0.000000000000000000, 0.000000000000000000 ) ) ;
#22970=CARTESIAN_POINT ( 'NONE',  ( 2.429928970624000151, 28.22663313894999959, 0.4339301335947000626 ) ) ;
#22972=CARTESIAN_POINT ( 'NONE',  ( 2.050437535749142448, 28.96303242407652689, 0.6788312481738240090 ) ) ;
#22973=EDGE_CURVE ( 'NONE', #18970, #7614, #7059, .T. ) ;
#22977=AXIS2_PLACEMENT_3D ( 'NONE', #16364, #5126, #10574 ) ;
#22987=CARTESIAN_POINT ( 'NONE',  ( -0.6543697108981931798, 27.36666666666666359, 2.434931691670791043 ) ) ;
#22992=CIRCLE ( 'NONE', #16823, 2.750000000000000000 ) ;
#22996=CARTESIAN_POINT ( 'NONE',  ( 2.675893616224000127, 28.54543090945000117, 0.6150008616569999642 ) ) ;
#23000=CARTESIAN_POINT ( 'NONE',  ( 2.000000000000000000, 26.50000000000000355, -3.464101615137999968 ) ) ;
#23001=EDGE_CURVE ( 'NONE', #4139, #12867, #20585, .T. ) ;
#23002=CARTESIAN_POINT ( 'NONE',  ( -2.434931691670790155, 29.80086340285666680, -0.6543697108981963995 ) ) ;
#23003=ORIENTED_EDGE ( 'NONE', *, *, #11455, .F. ) ;
#23004=CARTESIAN_POINT ( 'NONE',  ( 0.000000000000000000, 26.34999999328000087, -2.249999993279999888 ) ) ;
#23005=EDGE_CURVE ( 'NONE', #6143, #22927, #852, .T. ) ;
#23009=CARTESIAN_POINT ( 'NONE',  ( -2.156733561231868990, 24.62730423855435902, 0.3971439080199647975 ) ) ;
#23011=CIRCLE ( 'NONE', #15642, 3.000000000000000000 ) ;
#23016=ORIENTED_EDGE ( 'NONE', *, *, #19554, .T. ) ;
#23018=ADVANCED_FACE ( 'NONE', ( #8986 ), #13626, .F. ) ;
#23021=DIRECTION ( 'NONE',  ( 0.9947502446910230223, 0.000000000000000000, -0.1023325494999024060 ) ) ;
#23028=CARTESIAN_POINT ( 'NONE',  ( 0.000000000000000000, 9.050044887908999414, 0.000000000000000000 ) ) ;
#23030=CIRCLE ( 'NONE', #17226, 4.000000000000000000 ) ;
#23031=DIRECTION ( 'NONE',  ( 0.000000000000000000, 1.000000000000000000, 0.000000000000000000 ) ) ;
#23032=CARTESIAN_POINT ( 'NONE',  ( -1.465621426440372410, 29.50897963818352920, 1.586551976367980732 ) ) ;
#23034=CARTESIAN_POINT ( 'NONE',  ( -1.737762083858999995, 25.31592804684000342, 1.580334386437000083 ) ) ;
#23036=EDGE_LOOP ( 'NONE', ( #23042, #7129, #17729, #6582 ) ) ;
#23042=ORIENTED_EDGE ( 'NONE', *, *, #23913, .F. ) ;
#23043=AXIS2_PLACEMENT_3D ( 'NONE', #3258, #22011, #10642 ) ;
#23044=CARTESIAN_POINT ( 'NONE',  ( -2.434931691670790155, 27.16666666666666785, -0.6543697108981958444 ) ) ;
#23046=VERTEX_POINT ( 'NONE', #17952 ) ;
#23047=CARTESIAN_POINT ( 'NONE',  ( -4.724999999999999645, 14.90000000000000036, 0.000000000000000000 ) ) ;
#23058=CARTESIAN_POINT ( 'NONE',  ( -1.237648089123723594, 30.08161986502327423, -1.770177328435171393 ) ) ;
#23063=DIRECTION ( 'NONE',  ( 0.9970458808888235103, 0.000000000000000000, 0.07680827691486176445 ) ) ;
#23068=CARTESIAN_POINT ( 'NONE',  ( 0.5364167134210068300, 26.26145275469147222, 2.093854992564738282 ) ) ;
#23070=CARTESIAN_POINT ( 'NONE',  ( 4.749999884653000493, 20.09999988465641252, -5.093549567505999500E-08 ) ) ;
#23072=AXIS2_PLACEMENT_3D ( 'NONE', #1911, #22239, #20672 ) ;
#23075=CARTESIAN_POINT ( 'NONE',  ( -2.749999993363999806, 22.20000000663619844, 7.185653392336999782E-09 ) ) ;
#23083=CARTESIAN_POINT ( 'NONE',  ( -1.978431099119786207, 28.65874823216689293, 0.8981439385142484522 ) ) ;
#23085=FACE_OUTER_BOUND ( 'NONE', #18679, .T. ) ;
#23087=DIRECTION ( 'NONE',  ( 0.000000000000000000, 1.000000000000000000, 0.000000000000000000 ) ) ;
#23088=CARTESIAN_POINT ( 'NONE',  ( -2.583184600869000036, 28.72206776951999885, -0.6741018852137000694 ) ) ;
#23093=EDGE_CURVE ( 'NONE', #1412, #10853, #3912, .T. ) ;
#23098=DIRECTION ( 'NONE',  ( 0.000000000000000000, -1.000000000000000000, 0.000000000000000000 ) ) ;
#23101=DIRECTION ( 'NONE',  ( -0.7071067811905932254, 0.7071067811824932603, -1.099460837533990473E-07 ) ) ;
#23110=CARTESIAN_POINT ( 'NONE',  ( 2.500000000000000000, 28.40000000000000213, 0.000000000000000000 ) ) ;
#23111=CARTESIAN_POINT ( 'NONE',  ( 0.9599026219552000416, 30.10507675623999901, -2.343868003748000195 ) ) ;
#23115=DIRECTION ( 'NONE',  ( 0.000000000000000000, -0.7071067811866525998, -0.7071067811864425456 ) ) ;
#23116=CARTESIAN_POINT ( 'NONE',  ( 0.1597943784973999970, 29.98160862143000216, 2.741012656831999905 ) ) ;
#23123=ORIENTED_EDGE ( 'NONE', *, *, #3498, .F. ) ;
#23126=CONICAL_SURFACE ( 'NONE', #3800, 1.449999902385000095, 0.7853981633972997312 ) ;
#23128=CARTESIAN_POINT ( 'NONE',  ( 1.709519496923999959, 25.75266659807000025, 1.617190848266999881 ) ) ;
#23129=CARTESIAN_POINT ( 'NONE',  ( -1.042632460611140788, 24.73976796275902146, 1.891962004173780576 ) ) ;
#23135=CARTESIAN_POINT ( 'NONE',  ( 1.777466727206999941, 26.28919433609999956, -2.254705796085000102 ) ) ;
#23136=ORIENTED_EDGE ( 'NONE', *, *, #5128, .F. ) ;
#23151=CARTESIAN_POINT ( 'NONE',  ( 1.452663470816000002, 28.93738057083000115, -1.855135613986000021 ) ) ;
#23156=CARTESIAN_POINT ( 'NONE',  ( -1.716601787089840903, 29.32076057752635734, -1.311645278114084823 ) ) ;
#23162=B_SPLINE_CURVE_WITH_KNOTS ( 'NONE', 3,
 ( #2892, #1190, #1314, #2770, #23338, #13901, #12339, #10156, #3142, #15701 ),
 .UNSPECIFIED., .F., .F.,
 ( 4, 1, 1, 2, 2, 4 ),
 ( 0.000000000000000000, 0.2500000000000000000, 0.3749999999999996114, 0.4374999999999996669, 0.4999999999999996669, 1.000000000000000000 ),
 .UNSPECIFIED. ) ;
#23163=VERTEX_POINT ( 'NONE', #5464 ) ;
#23169=ORIENTED_EDGE ( 'NONE', *, *, #2737, .F. ) ;
#23170=CARTESIAN_POINT ( 'NONE',  ( 0.000000000000000000, 30.50000000000000000, 0.000000000000000000 ) ) ;
#23174=ADVANCED_FACE ( 'NONE', ( #20475 ), #19440, .T. ) ;
#23175=EDGE_LOOP ( 'NONE', ( #1507, #21810, #13474, #18915, #15834 ) ) ;
#23188=CARTESIAN_POINT ( 'NONE',  ( -2.154922498786136398, 30.19489467509957947, -0.1487298284546440252 ) ) ;
#23193=CARTESIAN_POINT ( 'NONE',  ( 4.549999999999859490, 22.00000000000000000, 0.000000000000000000 ) ) ;
#23195=CARTESIAN_POINT ( 'NONE',  ( -0.5347081996567876194, 24.26085803503821836, -2.188906454050921546 ) ) ;
#23197=CARTESIAN_POINT ( 'NONE',  ( -2.649379677059598759, 24.52555747447238943, -3.089210087443399200 ) ) ;
#23202=CONICAL_SURFACE ( 'NONE', #10846, 4.699999872533999756, 0.7853981633972997312 ) ;
#23203=CARTESIAN_POINT ( 'NONE',  ( 2.066886497620839869, 27.27369194946930619, -0.7492713746921416673 ) ) ;
#23212=CARTESIAN_POINT ( 'NONE',  ( 1.959918021306048308, 28.26123095495162474, -0.9363544129381041747 ) ) ;
#23217=CARTESIAN_POINT ( 'NONE',  ( -1.042632460611140788, 24.73976796275902146, 1.891962004173780576 ) ) ;
#23224=DIRECTION ( 'NONE',  ( 1.000000000000000000, 0.000000000000000000, 0.000000000000000000 ) ) ;
#23233=ORIENTED_EDGE ( 'NONE', *, *, #7146, .F. ) ;
#23234=CARTESIAN_POINT ( 'NONE',  ( 0.6543697108981982868, 28.56666666666666288, -2.434931691670790155 ) ) ;
#23235=CARTESIAN_POINT ( 'NONE',  ( -2.514717642077000104, 30.36979563812999672, 0.3022009937774000066 ) ) ;
#23236=CARTESIAN_POINT ( 'NONE',  ( 0.7071356748185000374, 23.94065862142999990, -2.622386026786000190 ) ) ;
#23238=VECTOR ( 'NONE', #7015, 1000.000000000000000 ) ;
#23240=CARTESIAN_POINT ( 'NONE',  ( 0.000000000000000000, 16.89999999999999858, 0.000000000000000000 ) ) ;
#23241=CARTESIAN_POINT ( 'NONE',  ( -2.948682383037576571, 22.00131761696259503, 1.025729208553000805E-08 ) ) ;
#23242=CARTESIAN_POINT ( 'NONE',  ( -2.223554292220999873, 29.69437307903999823, -1.610742350496999986 ) ) ;
#23244=B_SPLINE_CURVE_WITH_KNOTS ( 'NONE', 3,
 ( #3166, #12246, #8855, #6543, #16091, #16224 ),
 .UNSPECIFIED., .F., .F.,
 ( 4, 2, 4 ),
 ( 5.225908718322005276E-15, 0.0003975433753701282488, 0.0007950867507350306432 ),
 .UNSPECIFIED. ) ;
#23250=CARTESIAN_POINT ( 'NONE',  ( 2.000000000000000000, 18.89999999999999858, 5.041407240605999832E-11 ) ) ;
#23254=CARTESIAN_POINT ( 'NONE',  ( -1.545527083999999940, 23.83766312239999863, -2.022132869220999662 ) ) ;
#23257=FACE_BOUND ( 'NONE', #17218, .T. ) ;
#23259=CARTESIAN_POINT ( 'NONE',  ( 0.000000000000000000, 24.65000000674550051, -2.249999993254999886 ) ) ;
#23261=CARTESIAN_POINT ( 'NONE',  ( 1.536366799937295413, 30.11753006952333322, 1.999167105995444338 ) ) ;
#23265=EDGE_CURVE ( 'NONE', #16017, #12276, #9406, .T. ) ;
#23270=CARTESIAN_POINT ( 'NONE',  ( 2.268823611850999455, 29.65675077756000277, -0.6357669325499000212 ) ) ;
#23277=CARTESIAN_POINT ( 'NONE',  ( -1.029500669195184459, 29.54047064446312731, 1.898863408676955356 ) ) ;
#23279=CARTESIAN_POINT ( 'NONE',  ( 0.3272492347489343589, 29.38333333333332575, -2.500000000000000444 ) ) ;
#23286=CARTESIAN_POINT ( 'NONE',  ( -0.3381971108622000011, 27.76756359723999878, 2.445091418594000032 ) ) ;
#23288=VERTEX_POINT ( 'NONE', #13075 ) ;
#23292=ADVANCED_FACE ( 'NONE', ( #16469 ), #870, .T. ) ;
#23295=AXIS2_PLACEMENT_3D ( 'NONE', #12168, #10354, #1146 ) ;
#23300=CARTESIAN_POINT ( 'NONE',  ( 1.306994031390692035, 26.46241504948189416, 3.864208797664315576 ) ) ;
#23301=DIRECTION ( 'NONE',  ( 0.000000000000000000, 0.000000000000000000, -1.000000000000000000 ) ) ;
#23302=CARTESIAN_POINT ( 'NONE',  ( -2.113979557940886433, 30.23090653331247069, 0.4557372042204370088 ) ) ;
#23303=VERTEX_POINT ( 'NONE', #7266 ) ;
#23304=CARTESIAN_POINT ( 'NONE',  ( 2.283928009913000157, 25.78753186594000013, 0.4887283618359000159 ) ) ;
#23313=CIRCLE ( 'NONE', #15560, 1.500000000000000000 ) ;
#23319=CARTESIAN_POINT ( 'NONE',  ( 1.746727228398754050, 27.31067536807444185, -1.289094695068520702 ) ) ;
#23321=VERTEX_POINT ( 'NONE', #5811 ) ;
#23322=EDGE_CURVE ( 'NONE', #23589, #19360, #480, .T. ) ;
#23323=CARTESIAN_POINT ( 'NONE',  ( 1.805925435571642979, 26.69999746901650894, 1.797109528431422465 ) ) ;
#23325=CARTESIAN_POINT ( 'NONE',  ( 0.000000000000000000, 22.00000000000000000, -3.099999999999983213 ) ) ;
#23331=( GEOMETRIC_REPRESENTATION_CONTEXT ( 3 ) GLOBAL_UNCERTAINTY_ASSIGNED_CONTEXT ( ( #14465 ) ) GLOBAL_UNIT_ASSIGNED_CONTEXT ( ( #11147, #9329, #16821 ) ) REPRESENTATION_CONTEXT ( 'NONE', 'WORKASPACE' ) );
#23332=CARTESIAN_POINT ( 'NONE',  ( 2.693005968609320622, 26.46241504948188705, -3.063994432611676810 ) ) ;
#23335=CARTESIAN_POINT ( 'NONE',  ( -1.055729715565287385, 26.42936170367563875, -4.009276318043866638 ) ) ;
#23337=CARTESIAN_POINT ( 'NONE',  ( -1.371352433351999744, 26.37413313894999689, 2.052373795670999979 ) ) ;
#23338=CARTESIAN_POINT ( 'NONE',  ( 3.145406728938545449, 26.39685207198634487, 2.802800731853388516 ) ) ;
#23341=ORIENTED_EDGE ( 'NONE', *, *, #5543, .F. ) ;
#23342=APPLICATION_CONTEXT ( 'automotive_design' ) ;
#23343=FACE_OUTER_BOUND ( 'NONE', #23735, .T. ) ;
#23348=DIRECTION ( 'NONE',  ( 0.000000000000000000, 1.000000000000000000, 0.000000000000000000 ) ) ;
#23354=CARTESIAN_POINT ( 'NONE',  ( -0.4795158958135000149, 29.48253446158999935, -2.681298310498000159 ) ) ;
#23359=DIRECTION ( 'NONE',  ( -1.000000000000000000, 0.000000000000000000, -9.309561455062024044E-11 ) ) ;
#23362=CARTESIAN_POINT ( 'NONE',  ( -2.999999964324536972, 20.10000000000040998, -1.175584031498074967E-07 ) ) ;
#23369=CARTESIAN_POINT ( 'NONE',  ( 0.8117579086199240290, 23.79701621662123401, 2.166923507885120781 ) ) ;
#23372=CARTESIAN_POINT ( 'NONE',  ( -1.464281862760000053, 25.33464492091999887, -1.842154207471000005 ) ) ;
#23374=DIRECTION ( 'NONE',  ( 0.000000000000000000, -1.000000000000000000, 0.000000000000000000 ) ) ;
#23376=CARTESIAN_POINT ( 'NONE',  ( 1.259047450927246903, 27.73333333333333073, -2.184465970885645536 ) ) ;
#23379=CARTESIAN_POINT ( 'NONE',  ( -1.999167105995446780, 29.91753006952333394, 1.536366799937292305 ) ) ;
#23380=AXIS2_PLACEMENT_3D ( 'NONE', #8972, #23500, #3413 ) ;
#23382=FACE_OUTER_BOUND ( 'NONE', #21643, .T. ) ;
#23383=EDGE_LOOP ( 'NONE', ( #9592, #23169, #22547, #19846 ) ) ;
#23387=CONICAL_SURFACE ( 'NONE', #12944, 4.699999872533999756, 0.7853981633972997312 ) ;
#23390=CARTESIAN_POINT ( 'NONE',  ( 1.737805054697000084, 30.47971342496999725, -1.597568792902000157 ) ) ;
#23395=CARTESIAN_POINT ( 'NONE',  ( -1.317653730136605361, 29.28743615884798501, -1.711479633934526845 ) ) ;
#23397=CARTESIAN_POINT ( 'NONE',  ( -0.3272492347489393549, 29.41666666666667140, -2.499999999999999556 ) ) ;
#23400=VERTEX_POINT ( 'NONE', #23325 ) ;
#23407=ORIENTED_EDGE ( 'NONE', *, *, #9835, .F. ) ;
#23411=ORIENTED_EDGE ( 'NONE', *, *, #14821, .T. ) ;
#23415=AXIS2_PLACEMENT_3D ( 'NONE', #13929, #17198, #22760 ) ;
#23420=FACE_BOUND ( 'NONE', #11893, .T. ) ;
#23422=CARTESIAN_POINT ( 'NONE',  ( -1.500156801936728845, 30.10144942661541023, -1.558200670483578687 ) ) ;
#23426=DIRECTION ( 'NONE',  ( -1.000000000000000000, 0.000000000000000000, 0.000000000000000000 ) ) ;
#23427=CARTESIAN_POINT ( 'NONE',  ( -0.3272492347489284192, 27.61753006952333322, 2.500000000000001332 ) ) ;
#23429=ORIENTED_EDGE ( 'NONE', *, *, #5373, .F. ) ;
#23430=DIRECTION ( 'NONE',  ( 1.000000000000000000, 0.000000000000000000, 0.000000000000000000 ) ) ;
#23431=CIRCLE ( 'NONE', #10678, 3.100000000000000089 ) ;
#23433=EDGE_CURVE ( 'NONE', #6008, #6590, #16345, .T. ) ;
#23435=CARTESIAN_POINT ( 'NONE',  ( -2.329590180155310719, 24.49999999999985079, -3.273812635903178059 ) ) ;
#23439=ORIENTED_EDGE ( 'NONE', *, *, #1705, .T. ) ;
#23440=CARTESIAN_POINT ( 'NONE',  ( -1.399330729071998958, 26.71894067039222875, -1.658981764594649411 ) ) ;
#23453=CARTESIAN_POINT ( 'NONE',  ( 0.6971734275731837904, 26.76391587493858637, -2.091919652565851440 ) ) ;
#23454=VECTOR ( 'NONE', #21083, 1000.000000000000000 ) ;
#23455=AXIS2_PLACEMENT_3D ( 'NONE', #16025, #21500, #14106 ) ;
#23456=CARTESIAN_POINT ( 'NONE',  ( 3.643546194520564274, 26.29977277844447414, -2.515199777306226903 ) ) ;
#23457=CARTESIAN_POINT ( 'NONE',  ( 0.000000000000000000, 20.10000000000000142, 0.000000000000000000 ) ) ;
#23461=B_SPLINE_CURVE_WITH_KNOTS ( 'NONE', 3,
 ( #8764, #13962, #8530, #14208, #14084, #5022, #1131, #15888, #23279, #23397, #10583, #21478, #20020, #8890, #18090, #16004, #10701, #23528 ),
 .UNSPECIFIED., .F., .F.,
 ( 4, 2, 2, 2, 2, 2, 2, 2, 4 ),
 ( 0.000000000000000000, 0.1250000000000000555, 0.2500000000000001110, 0.3750000000000000555, 0.5000000000000000000, 0.6249999999999998890, 0.7499999999999998890, 0.8749999999999998890, 1.000000000000000000 ),
 .UNSPECIFIED. ) ;
#23462=CARTESIAN_POINT ( 'NONE',  ( 1.603022320644999832, 27.24369850838000318, 1.603022320644999832 ) ) ;
#23463=CARTESIAN_POINT ( 'NONE',  ( 3.099999776787000005, 21.99999977679100027, 5.570936506502000395E-07 ) ) ;
#23466=CIRCLE ( 'NONE', #11091, 4.750000000000000000 ) ;
#23476=CARTESIAN_POINT ( 'NONE',  ( -2.499999999999988898, 24.01666666666666217, 0.3272492347490136844 ) ) ;
#23483=CARTESIAN_POINT ( 'NONE',  ( -0.7613436424516999423, 28.91384178769000357, 2.298498088615000157 ) ) ;
#23484=CARTESIAN_POINT ( 'NONE',  ( 0.000000000000000000, 14.90000000000000036, 0.000000000000000000 ) ) ;
#23497=PLANE ( 'NONE',  #1910 ) ;
#23500=DIRECTION ( 'NONE',  ( 0.000000000000000000, -1.000000000000000000, 0.000000000000000000 ) ) ;
#23502=CARTESIAN_POINT ( 'NONE',  ( -4.000000000000000000, 26.39685207198629158, 1.322601766568779924 ) ) ;
#23504=CARTESIAN_POINT ( 'NONE',  ( -2.048929151683000160, 24.67370647670999873, -1.509915493683999799 ) ) ;
#23506=DIRECTION ( 'NONE',  ( 0.000000000000000000, 1.000000000000000000, 0.000000000000000000 ) ) ;
#23510=CARTESIAN_POINT ( 'NONE',  ( 0.3272492347489343589, 27.78333333333333854, -2.500000000000000444 ) ) ;
#23514=CARTESIAN_POINT ( 'NONE',  ( -0.5252141218270467427, 26.22790185010774522, 2.065890903574498338 ) ) ;
#23521=CARTESIAN_POINT ( 'NONE',  ( 2.188113818431999924, 30.33609565378000283, 0.8856361526165000830 ) ) ;
#23525=VECTOR ( 'NONE', #12634, 1000.000000000000000 ) ;
#23527=VERTEX_POINT ( 'NONE', #17595 ) ;
#23528=CARTESIAN_POINT ( 'NONE',  ( -2.500000000000000000, 29.60000000000000142, 0.000000000000000000 ) ) ;
#23531=AXIS2_PLACEMENT_3D ( 'NONE', #16769, #178, #7569 ) ;
#23532=DIRECTION ( 'NONE',  ( 0.000000000000000000, 1.000000000000000000, 0.000000000000000000 ) ) ;
#23535=CIRCLE ( 'NONE', #7290, 3.100000000000000089 ) ;
#23537=EDGE_CURVE ( 'NONE', #15489, #13137, #8231, .T. ) ;
#23538=ORIENTED_EDGE ( 'NONE', *, *, #6317, .T. ) ;
#23543=ORIENTED_EDGE ( 'NONE', *, *, #11048, .T. ) ;
#23551=CARTESIAN_POINT ( 'NONE',  ( 1.409996887616000283, 30.49659672073000038, 1.871210455765000003 ) ) ;
#23552=CIRCLE ( 'NONE', #14270, 3.000000000000000000 ) ;
#23555=CARTESIAN_POINT ( 'NONE',  ( 1.600079875324325940, 29.89762239541055422, -1.452365398962871312 ) ) ;
#23556=CLOSED_SHELL ( 'NONE', ( #11471, #8370, #21071, #16886, #20295, #11833, #13905 ) ) ;
#23561=TOROIDAL_SURFACE ( 'NONE', #17362, 2.500000000000000000, 0.5500000000000000444 ) ;
#23563=DIRECTION ( 'NONE',  ( 0.000000000000000000, -1.000000000000000000, 0.000000000000000000 ) ) ;
#23568=EDGE_CURVE ( 'NONE', #15097, #15539, #15632, .T. ) ;
#23571=VECTOR ( 'NONE', #6664, 1000.000000000000000 ) ;
#23572=CARTESIAN_POINT ( 'NONE',  ( -0.4677043798615876380, 26.65730163938367525, -2.152092775777489475 ) ) ;
#23575=DIRECTION ( 'NONE',  ( -1.000000000000000000, 0.000000000000000000, 0.000000000000000000 ) ) ;
#23576=ORIENTED_EDGE ( 'NONE', *, *, #13514, .T. ) ;
#23577=CARTESIAN_POINT ( 'NONE',  ( 1.410165095533915336, 26.67499683627062979, 2.121886834720800419 ) ) ;
#23581=EDGE_CURVE ( 'NONE', #15097, #15489, #6523, .T. ) ;
#23585=CARTESIAN_POINT ( 'NONE',  ( 2.147641545635635030, 26.57840781165250021, 0.4457964343191409551 ) ) ;
#23588=CARTESIAN_POINT ( 'NONE',  ( 2.121777613921716821, 30.62783393162584389, -0.4070726844702514668 ) ) ;
#23589=VERTEX_POINT ( 'NONE', #22903 ) ;
#23591=CARTESIAN_POINT ( 'NONE',  ( -2.464088664829000130, 27.05663313895000144, 0.1453149127352000025 ) ) ;
#23595=CARTESIAN_POINT ( 'NONE',  ( 2.426425728984999974, 26.63187716036000197, -0.3356153332445000470 ) ) ;
#23596=CARTESIAN_POINT ( 'NONE',  ( 4.000000000000000000, 26.20000000000000284, -2.309401076759000304 ) ) ;
#23597=ORIENTED_EDGE ( 'NONE', *, *, #15630, .T. ) ;
#23599=EDGE_CURVE ( 'NONE', #19778, #15589, #23313, .T. ) ;
#23603=ORIENTED_EDGE ( 'NONE', *, *, #882, .F. ) ;
#23609=CARTESIAN_POINT ( 'NONE',  ( -1.999167105995452998, 28.71666666666667211, -1.536366799937284089 ) ) ;
#23610=CARTESIAN_POINT ( 'NONE',  ( 0.3885619843355000436, 29.77417815385999944, 2.502828369449000334 ) ) ;
#23612=DIRECTION ( 'NONE',  ( -1.000000000000000000, 0.000000000000000000, 0.000000000000000000 ) ) ;
#23613=ORIENTED_EDGE ( 'NONE', *, *, #4698, .T. ) ;
#23614=CARTESIAN_POINT ( 'NONE',  ( 0.000000000000000000, 22.00000000000000000, -4.549999999999999822 ) ) ;
#23617=FACE_OUTER_BOUND ( 'NONE', #3516, .T. ) ;
#23618=CARTESIAN_POINT ( 'NONE',  ( -1.236362846991004183, 26.50000008335574719, -2.171602059085420589 ) ) ;
#23619=CARTESIAN_POINT ( 'NONE',  ( -2.818367767609784025, 24.55137445130671381, 2.991616928423203259 ) ) ;
#23622=ORIENTED_EDGE ( 'NONE', *, *, #14987, .T. ) ;
#23623=LINE ( 'NONE', #15974, #21067 ) ;
#23625=VERTEX_POINT ( 'NONE', #4510 ) ;
#23626=CARTESIAN_POINT ( 'NONE',  ( -0.3158523902254999904, 25.37040927195999984, -2.525508413827000087 ) ) ;
#23632=DIRECTION ( 'NONE',  ( -0.5000000000000169864, 0.000000000000000000, 0.8660254037844289376 ) ) ;
#23641=ADVANCED_FACE ( 'NONE', ( #20940 ), #1663, .F. ) ;
#23642=DIRECTION ( 'NONE',  ( -0.000000000000000000, 1.000000000000000000, 0.000000000000000000 ) ) ;
#23646=CARTESIAN_POINT ( 'NONE',  ( 2.067768348872000228, 29.65163254276000160, 0.6515505822407000602 ) ) ;
#23650=CARTESIAN_POINT ( 'NONE',  ( -1.911995322407668896, 26.28293724889640259, 1.064052824085054416 ) ) ;
#23651=ORIENTED_EDGE ( 'NONE', *, *, #6288, .T. ) ;
#23652=FACE_BOUND ( 'NONE', #3735, .T. ) ;
#23653=CARTESIAN_POINT ( 'NONE',  ( 0.000000000000000000, 22.10000000618969906, 0.000000000000000000 ) ) ;
#23654=ORIENTED_EDGE ( 'NONE', *, *, #477, .F. ) ;
#23662=ORIENTED_EDGE ( 'NONE', *, *, #14508, .F. ) ;
#23664=CARTESIAN_POINT ( 'NONE',  ( -2.693005968609320622, 26.46241504948188705, 3.063994432611676810 ) ) ;
#23667=CONICAL_SURFACE ( 'NONE', #13213, 4.674999969225999585, 0.7853981633972997312 ) ;
#23668=CARTESIAN_POINT ( 'NONE',  ( -0.8469014928486000571, 30.08331639939000013, -2.017769495180000483 ) ) ;
#23671=CARTESIAN_POINT ( 'NONE',  ( 0.6579082771927615703, 29.96447688474591331, -2.058286849431618659 ) ) ;
#23676=DIRECTION ( 'NONE',  ( 0.000000000000000000, -1.000000000000000000, 0.000000000000000000 ) ) ;
#23678=ORIENTED_EDGE ( 'NONE', *, *, #15166, .F. ) ;
#23684=ORIENTED_EDGE ( 'NONE', *, *, #8029, .F. ) ;
#23686=CARTESIAN_POINT ( 'NONE',  ( -1.554837348280936338, 26.73126847659393235, -1.516119970887816359 ) ) ;
#23691=CARTESIAN_POINT ( 'NONE',  ( 0.000000000000000000, 9.000000000000000000, 0.000000000000000000 ) ) ;
#23694=CARTESIAN_POINT ( 'NONE',  ( 1.988574678778234794, 26.55190665974927100, 0.8727035924344519469 ) ) ;
#23696=ADVANCED_FACE ( 'NONE', ( #221 ), #5713, .F. ) ;
#23698=ORIENTED_EDGE ( 'NONE', *, *, #9271, .F. ) ;
#23701=CARTESIAN_POINT ( 'NONE',  ( 1.996953125041000199, 26.56913313895000073, 1.450871306011999984 ) ) ;
#23702=AXIS2_PLACEMENT_3D ( 'NONE', #14189, #12616, #2933 ) ;
#23703=CARTESIAN_POINT ( 'NONE',  ( -2.000256872717999901, 28.45364211381999908, 1.120191590154000050 ) ) ;
#23706=CARTESIAN_POINT ( 'NONE',  ( 0.000000000000000000, 24.40000007355299871, 0.000000000000000000 ) ) ;
#23708=EDGE_CURVE ( 'NONE', #12888, #2468, #12582, .T. ) ;
#23710=CARTESIAN_POINT ( 'NONE',  ( 2.241434001307105017, 30.45310926007345032, -0.4064658644085604733 ) ) ;
#23711=VERTEX_POINT ( 'NONE', #492 ) ;
#23713=FACE_OUTER_BOUND ( 'NONE', #13600, .T. ) ;
#23718=CARTESIAN_POINT ( 'NONE',  ( 2.434931691670791487, 29.40086340285667887, 0.6543697108981911814 ) ) ;
#23719=CARTESIAN_POINT ( 'NONE',  ( 0.8875055740816000238, 29.99964212565999944, -2.167090567999999884 ) ) ;
#23722=B_SPLINE_CURVE_WITH_KNOTS ( 'NONE', 3,
 ( #16272, #15904, #12651, #23664, #19807, #7075, #14459, #17624, #8420, #15788 ),
 .UNSPECIFIED., .F., .F.,
 ( 4, 1, 1, 2, 2, 4 ),
 ( 0.000000000000000000, 0.2500000000000001665, 0.3750000000000001665, 0.4375000000000000555, 0.4999999999999999445, 1.000000000000000000 ),
 .UNSPECIFIED. ) ;
#23726=ADVANCED_FACE ( 'NONE', ( #6432 ), #7456, .T. ) ;
#23727=CARTESIAN_POINT ( 'NONE',  ( 1.259047450927267553, 29.06666666666666288, 2.184465970885633990 ) ) ;
#23735=EDGE_LOOP ( 'NONE', ( #2938, #16429, #2927 ) ) ;
#23736=CARTESIAN_POINT ( 'NONE',  ( -1.739863589215999928, 24.46283721557000135, -1.282156090217000166 ) ) ;
#23737=CARTESIAN_POINT ( 'NONE',  ( 0.000000000000000000, 26.50000000000000355, 0.000000000000000000 ) ) ;
#23741=CARTESIAN_POINT ( 'NONE',  ( 0.000000000000000000, 24.50000000000000000, 0.000000000000000000 ) ) ;
#23743=AXIS2_PLACEMENT_3D ( 'NONE', #2873, #12321, #5062 ) ;
#23745=CARTESIAN_POINT ( 'NONE',  ( 0.000000000000000000, 18.00000000000000000, -2.899999999999999911 ) ) ;
#23748=CARTESIAN_POINT ( 'NONE',  ( -3.999878274658704935, 24.63336607547242707, 1.519686587934140576 ) ) ;
#23751=CARTESIAN_POINT ( 'NONE',  ( -1.953659355438999823, 23.74463359794000183, 0.8845564191319000846 ) ) ;
#23756=CARTESIAN_POINT ( 'NONE',  ( -0.9609966757344999833, 29.14897034355999850, -1.943365538522000113 ) ) ;
#23766=DIRECTION ( 'NONE',  ( 1.000000000000000000, 0.000000000000000000, 0.000000000000000000 ) ) ;
#23767=EDGE_CURVE ( 'NONE', #13042, #20998, #11655, .T. ) ;
#23771=ORIENTED_EDGE ( 'NONE', *, *, #15594, .T. ) ;
#23775=DIRECTION ( 'NONE',  ( 0.7071067811905932254, -0.7071067811824932603, 1.099460906822990477E-07 ) ) ;
#23781=CARTESIAN_POINT ( 'NONE',  ( -1.947074432796000121, 29.48947843130000379, 1.303234819910000120 ) ) ;
#23784=CARTESIAN_POINT ( 'NONE',  ( 2.135618988582168143, 29.82286535022900864, -0.3226676719785777081 ) ) ;
#23788=CARTESIAN_POINT ( 'NONE',  ( -0.8574870095143278803, 23.63963447597672030, -1.960294260298593549 ) ) ;
#23794=CARTESIAN_POINT ( 'NONE',  ( 4.750000000000000000, 20.10000000000000142, 0.000000000000000000 ) ) ;
#23795=VERTEX_POINT ( 'NONE', #2557 ) ;
#23796=AXIS2_PLACEMENT_3D ( 'NONE', #5561, #18636, #5448 ) ;
#23797=CARTESIAN_POINT ( 'NONE',  ( -2.434931691670786602, 28.26753006952333536, 0.6543697108982093891 ) ) ;
#23799=CARTESIAN_POINT ( 'NONE',  ( 2.500000000000000000, 30.00000000000000000, 0.000000000000000000 ) ) ;
#23800=ORIENTED_EDGE ( 'NONE', *, *, #8515, .F. ) ;
#23807=CARTESIAN_POINT ( 'NONE',  ( -1.955724675740084795, 26.26076676662178855, 0.9180910909140133080 ) ) ;
#23815=CARTESIAN_POINT ( 'NONE',  ( -1.552970335759000120, 27.13771896306000286, 1.679993844339999987 ) ) ;
#23816=DIRECTION ( 'NONE',  ( 0.000000000000000000, -1.000000000000000000, -9.414809210018000201E-11 ) ) ;
#23819=CARTESIAN_POINT ( 'NONE',  ( 0.000000000000000000, 24.80000000000000426, -4.618802153517000519 ) ) ;
#23820=CARTESIAN_POINT ( 'NONE',  ( 2.149044184505269683, 28.87331377689345757, -0.7555511948961874946 ) ) ;
#23822=ADVANCED_FACE ( 'NONE', ( #21818 ), #10949, .F. ) ;
#23823=FACE_OUTER_BOUND ( 'NONE', #20989, .T. ) ;
#23829=CARTESIAN_POINT ( 'NONE',  ( 1.999167105995457216, 29.35086340285667106, 1.536366799937278760 ) ) ;
#23830=CARTESIAN_POINT ( 'NONE',  ( 0.4270404191337999755, 28.76915224701999918, 2.107898681223999926 ) ) ;
#23831=LINE ( 'NONE', #13048, #23238 ) ;
#23832=CARTESIAN_POINT ( 'NONE',  ( 0.000000000000000000, 12.90000000000000036, 0.000000000000000000 ) ) ;
#23840=LINE ( 'NONE', #11132, #19179 ) ;
#23842=CARTESIAN_POINT ( 'NONE',  ( -0.5478863511337975778, 29.23652871585738922, -2.091076401733357404 ) ) ;
#23844=ORIENTED_EDGE ( 'NONE', *, *, #1261, .F. ) ;
#23847=CARTESIAN_POINT ( 'NONE',  ( 0.3463667137627760018, 24.70780860099773690, -4.418706525551467479 ) ) ;
#23849=CARTESIAN_POINT ( 'NONE',  ( -2.014261560068999923, 23.69646414078999896, -0.7835128413787000312 ) ) ;
#23853=CARTESIAN_POINT ( 'NONE',  ( -1.536366799937290084, 27.88333333333333641, -1.999167105995448113 ) ) ;
#23856=DIRECTION ( 'NONE',  ( 0.000000000000000000, 0.000000000000000000, 1.000000000000000000 ) ) ;
#23857=CONICAL_SURFACE ( 'NONE', #17683, 2.849999992212000066, 0.7853981633972997312 ) ;
#23858=EDGE_LOOP ( 'NONE', ( #20426, #14976, #12732, #8172 ) ) ;
#23865=CARTESIAN_POINT ( 'NONE',  ( 0.5583575531182999319, 24.25696251314999685, -2.070647963877000119 ) ) ;
#23878=ORIENTED_EDGE ( 'NONE', *, *, #4369, .T. ) ;
#23879=DIRECTION ( 'NONE',  ( 0.000000000000000000, 0.000000000000000000, -1.000000000000000000 ) ) ;
#23882=FACE_OUTER_BOUND ( 'NONE', #11870, .T. ) ;
#23883=B_SPLINE_CURVE_WITH_KNOTS ( 'NONE', 3,
 ( #12708, #1678, #23718, #1798, #23829, #3619, #20443, #3731, #18506, #18625, #1574, #87, #10780, #9067, #9305, #7359, #11001, #13046 ),
 .UNSPECIFIED., .F., .F.,
 ( 4, 2, 2, 2, 2, 2, 2, 2, 4 ),
 ( 0.000000000000000000, 0.1250000000000000000, 0.2500000000000000000, 0.3750000000000000000, 0.5000000000000000000, 0.6250000000000000000, 0.7500000000000000000, 0.8750000000000000000, 1.000000000000000000 ),
 .UNSPECIFIED. ) ;
#23887=CARTESIAN_POINT ( 'NONE',  ( -0.3657850755361999884, 27.66212896667000010, 2.644546391786999795 ) ) ;
#23892=CARTESIAN_POINT ( 'NONE',  ( -2.899999999999999911, 19.00000000000000000, 0.000000000000000000 ) ) ;
#23893=ORIENTED_EDGE ( 'NONE', *, *, #11060, .T. ) ;
#23899=CARTESIAN_POINT ( 'NONE',  ( 2.047977397348999862, 30.58687554411000065, 0.7709893512285000972 ) ) ;
#23903=CARTESIAN_POINT ( 'NONE',  ( 2.137288283767348585, 29.82219721339723151, -0.3113321526725940647 ) ) ;
#23905=CARTESIAN_POINT ( 'NONE',  ( -0.6999264713064999865, 23.99113176564999961, 2.066154116230000337 ) ) ;
#23907=CARTESIAN_POINT ( 'NONE',  ( -1.005978889223114070, 23.62285964557008100, -1.869535163937288358 ) ) ;
#23913=EDGE_CURVE ( 'NONE', #18102, #4867, #8509, .T. ) ;
#23915=EDGE_CURVE ( 'NONE', #14322, #5160, #15732, .T. ) ;
#23917=CARTESIAN_POINT ( 'NONE',  ( -2.500000000000000000, 28.23419673618999681, 0.000000000000000000 ) ) ;
#23930=CARTESIAN_POINT ( 'NONE',  ( 1.519660212291651602, 27.50594812747459983, -1.553771826035092340 ) ) ;
#23933=CARTESIAN_POINT ( 'NONE',  ( 1.358166937795349138, 30.71719867068216203, -1.679610467239872840 ) ) ;
#23934=VERTEX_POINT ( 'NONE', #10805 ) ;
#23937=CIRCLE ( 'NONE', #13486, 3.000000000000000000 ) ;
#23939=CARTESIAN_POINT ( 'NONE',  ( 0.4306175354955999457, 26.43687716036000168, 2.411379030285999647 ) ) ;
#23940=CARTESIAN_POINT ( 'NONE',  ( -2.123863125265573526, 30.86865349149609017, 0.1785559413447701804 ) ) ;
#23946=CONICAL_SURFACE ( 'NONE', #20093, 2.249999993279999888, 0.7853981633972997312 ) ;
#23948=VERTEX_POINT ( 'NONE', #16107 ) ;
#23949=DIRECTION ( 'NONE',  ( 0.000000000000000000, 1.000000000000000000, 0.000000000000000000 ) ) ;
#23953=CARTESIAN_POINT ( 'NONE',  ( 0.000000000000000000, 15.09999999999999964, -3.000000000000416112 ) ) ;
#23954=CARTESIAN_POINT ( 'NONE',  ( 1.543604752742000041, 28.94076659806999885, 1.761054684240999979 ) ) ;
#23956=DIRECTION ( 'NONE',  ( 0.000000000000000000, -1.000000000000000000, 0.000000000000000000 ) ) ;
#23957=AXIS2_PLACEMENT_3D ( 'NONE', #1213, #16089, #1088 ) ;
#23958=ORIENTED_EDGE ( 'NONE', *, *, #17854, .T. ) ;
#23960=CARTESIAN_POINT ( 'NONE',  ( -2.184465970885638431, 28.86666666666667069, 1.259047450927259559 ) ) ;
#23963=DIRECTION ( 'NONE',  ( 0.000000000000000000, 1.000000000000000000, 0.000000000000000000 ) ) ;
#23966=CARTESIAN_POINT ( 'NONE',  ( -1.033211977243992497, 29.26718191722662965, -1.899078110007318188 ) ) ;
#23967=LINE ( 'NONE', #9199, #2283 ) ;
ENDSEC;
END-ISO-10303-21;
